ISO-10303-21;
HEADER;
/* Generated by software containing ST-Developer
 * from STEP Tools, Inc. (www.steptools.com) 
 */

FILE_DESCRIPTION(
/* description */ (''),
/* implementation_level */ '2;1');

FILE_NAME(
/* name */ 'Screw.step',
/* time_stamp */ '2026-10-06T13:05:37-07:00',
/* author */ (''),
/* organization */ (''),
/* preprocessor_version */ 'ST-DEVELOPER v20.2',
/* originating_system */ 'Autodesk Translation Framework v15.15.0.0',
/* authorisation */ '');

FILE_SCHEMA (('AUTOMOTIVE_DESIGN { 1 0 10303 214 3 1 1 }'));
ENDSEC;

DATA;
#10=MECHANICAL_DESIGN_GEOMETRIC_PRESENTATION_REPRESENTATION('',(#139),#28055);
#62=B_SPLINE_SURFACE_WITH_KNOTS('',3,3,((#20854,#20855,#20856,#20857,#20858,
#20859),(#20860,#20861,#20862,#20863,#20864,#20865),(#20866,#20867,#20868,
#20869,#20870,#20871),(#20872,#20873,#20874,#20875,#20876,#20877)),
 .UNSPECIFIED.,.F.,.F.,.F.,(4,4),(4,1,1,4),(0.,0.0494711118308268),(16.7019134878289,
17.6517088926312,18.6014255011318,19.5511421096324),.UNSPECIFIED.);
#63=B_SPLINE_SURFACE_WITH_KNOTS('',3,3,((#21117,#21118,#21119,#21120,#21121,
#21122),(#21123,#21124,#21125,#21126,#21127,#21128),(#21129,#21130,#21131,
#21132,#21133,#21134),(#21135,#21136,#21137,#21138,#21139,#21140)),
 .UNSPECIFIED.,.F.,.F.,.F.,(4,4),(4,1,1,4),(-7.87913040489834E-5,0.0493923155291723),
(13.3942556087771,14.3439722172777,15.2936888257783,16.2434842255829),
 .UNSPECIFIED.);
#64=B_SPLINE_SURFACE_WITH_KNOTS('',3,3,((#21329,#21330,#21331,#21332,#21333,
#21334,#21335,#21336,#21337,#21338,#21339,#21340,#21341,#21342,#21343,#21344,
#21345,#21346,#21347,#21348,#21349,#21350,#21351,#21352,#21353,#21354,#21355,
#21356,#21357,#21358,#21359,#21360,#21361,#21362,#21363,#21364,#21365,#21366,
#21367,#21368,#21369,#21370,#21371,#21372,#21373,#21374,#21375,#21376),
(#21377,#21378,#21379,#21380,#21381,#21382,#21383,#21384,#21385,#21386,
#21387,#21388,#21389,#21390,#21391,#21392,#21393,#21394,#21395,#21396,#21397,
#21398,#21399,#21400,#21401,#21402,#21403,#21404,#21405,#21406,#21407,#21408,
#21409,#21410,#21411,#21412,#21413,#21414,#21415,#21416,#21417,#21418,#21419,
#21420,#21421,#21422,#21423,#21424),(#21425,#21426,#21427,#21428,#21429,
#21430,#21431,#21432,#21433,#21434,#21435,#21436,#21437,#21438,#21439,#21440,
#21441,#21442,#21443,#21444,#21445,#21446,#21447,#21448,#21449,#21450,#21451,
#21452,#21453,#21454,#21455,#21456,#21457,#21458,#21459,#21460,#21461,#21462,
#21463,#21464,#21465,#21466,#21467,#21468,#21469,#21470,#21471,#21472),
(#21473,#21474,#21475,#21476,#21477,#21478,#21479,#21480,#21481,#21482,
#21483,#21484,#21485,#21486,#21487,#21488,#21489,#21490,#21491,#21492,#21493,
#21494,#21495,#21496,#21497,#21498,#21499,#21500,#21501,#21502,#21503,#21504,
#21505,#21506,#21507,#21508,#21509,#21510,#21511,#21512,#21513,#21514,#21515,
#21516,#21517,#21518,#21519,#21520)),.UNSPECIFIED.,.F.,.F.,.F.,(4,4),(4,
1,1,1,1,1,1,1,1,1,1,1,1,1,1,1,1,1,1,1,1,1,1,1,1,1,1,1,1,1,1,1,1,1,1,1,1,
1,1,1,1,1,1,1,1,4),(-0.000683464176930082,0.0823722747458684),(8.31487785380719,
8.80643119756841,9.29798454132964,10.2810912288521,11.2641979163745,12.247304603897,
13.2304112914194,14.2135179789419,15.1966246664643,16.1797313539867,17.1628380415092,
18.1459447290316,19.1290514165541,20.1121581040765,21.095264791599,22.0783714791214,
23.0614781666439,24.0445848541663,25.0276915416888,26.0107982292112,26.9939049167336,
27.9770116042561,28.9601182917785,29.943224979301,30.9263316668234,31.9094383543459,
32.8925450418683,33.8756517293908,34.8587584169132,35.8418651044356,36.8249717919581,
37.8080784794805,38.791185167003,39.7742918545254,40.7573985420479,41.7405052295703,
42.7236119170928,43.7067186046152,44.6898252921376,45.6729319796601,46.6560386671825,
47.639145354705,48.6222520422274,49.6053587297499,50.0969120735111,50.5891488814492),
 .UNSPECIFIED.);
#65=B_SPLINE_SURFACE_WITH_KNOTS('',3,3,((#21721,#21722,#21723,#21724,#21725,
#21726,#21727,#21728,#21729,#21730,#21731,#21732,#21733,#21734,#21735,#21736,
#21737,#21738,#21739,#21740,#21741,#21742,#21743,#21744,#21745,#21746,#21747,
#21748,#21749,#21750,#21751,#21752,#21753,#21754,#21755,#21756,#21757,#21758,
#21759,#21760,#21761,#21762,#21763,#21764,#21765,#21766,#21767,#21768),
(#21769,#21770,#21771,#21772,#21773,#21774,#21775,#21776,#21777,#21778,
#21779,#21780,#21781,#21782,#21783,#21784,#21785,#21786,#21787,#21788,#21789,
#21790,#21791,#21792,#21793,#21794,#21795,#21796,#21797,#21798,#21799,#21800,
#21801,#21802,#21803,#21804,#21805,#21806,#21807,#21808,#21809,#21810,#21811,
#21812,#21813,#21814,#21815,#21816),(#21817,#21818,#21819,#21820,#21821,
#21822,#21823,#21824,#21825,#21826,#21827,#21828,#21829,#21830,#21831,#21832,
#21833,#21834,#21835,#21836,#21837,#21838,#21839,#21840,#21841,#21842,#21843,
#21844,#21845,#21846,#21847,#21848,#21849,#21850,#21851,#21852,#21853,#21854,
#21855,#21856,#21857,#21858,#21859,#21860,#21861,#21862,#21863,#21864),
(#21865,#21866,#21867,#21868,#21869,#21870,#21871,#21872,#21873,#21874,
#21875,#21876,#21877,#21878,#21879,#21880,#21881,#21882,#21883,#21884,#21885,
#21886,#21887,#21888,#21889,#21890,#21891,#21892,#21893,#21894,#21895,#21896,
#21897,#21898,#21899,#21900,#21901,#21902,#21903,#21904,#21905,#21906,#21907,
#21908,#21909,#21910,#21911,#21912)),.UNSPECIFIED.,.F.,.F.,.F.,(4,4),(4,
1,1,1,1,1,1,1,1,1,1,1,1,1,1,1,1,1,1,1,1,1,1,1,1,1,1,1,1,1,1,1,1,1,1,1,1,
1,1,1,1,1,1,1,1,4),(-0.000359643560771195,0.0826961570524529),(11.6143855724915,
12.1066224675668,12.598175811328,13.5812824988505,14.5643891863729,15.5474958738954,
16.5306025614178,17.5137092489403,18.4968159364627,19.4799226239851,20.4630293115076,
21.44613599903,22.4292426865525,23.4123493740749,24.3954560615974,25.3785627491198,
26.3616694366423,27.3447761241647,28.3278828116872,29.3109894992096,30.294096186732,
31.2772028742545,32.2603095617769,33.2434162492994,34.2265229368218,35.2096296243443,
36.1927363118667,37.1758429993892,38.1589496869116,39.142056374434,40.1251630619565,
41.1082697494789,42.0913764370014,43.0744831245238,44.0575898120463,45.0406964995687,
46.0238031870912,47.0069098746136,47.9900165621361,48.9731232496585,49.956229937181,
50.9393366247034,51.9224433122258,52.9055499997483,53.3971033435095,53.8886566872707),
 .UNSPECIFIED.);
#119=SHAPE_REPRESENTATION_RELATIONSHIP('SRR','None',#28096,#129);
#129=ADVANCED_BREP_SHAPE_REPRESENTATION('',(#149),#28048);
#139=STYLED_ITEM('',(#28152),#149);
#149=MANIFOLD_SOLID_BREP('Body1',#3680);
#193=FACE_BOUND('',#709,.T.);
#194=FACE_BOUND('',#711,.T.);
#195=FACE_BOUND('',#713,.T.);
#229=PLANE('',#3978);
#230=PLANE('',#3987);
#231=PLANE('',#3988);
#232=PLANE('',#3989);
#331=CIRCLE('',#3964,3.72275);
#332=CIRCLE('',#3971,4.433);
#333=CIRCLE('',#3972,4.433);
#334=CIRCLE('',#3974,3.72275);
#335=CIRCLE('',#3976,1.77625);
#336=CIRCLE('',#3977,1.77625);
#337=CIRCLE('',#3979,2.204);
#338=CIRCLE('',#3980,2.204);
#339=CIRCLE('',#3982,2.204);
#340=CIRCLE('',#3983,2.204);
#341=CIRCLE('',#3985,5.42440960677665);
#342=CIRCLE('',#3986,5.42440960677665);
#466=FACE_OUTER_BOUND('',#692,.T.);
#467=FACE_OUTER_BOUND('',#693,.T.);
#468=FACE_OUTER_BOUND('',#694,.T.);
#469=FACE_OUTER_BOUND('',#695,.T.);
#470=FACE_OUTER_BOUND('',#696,.T.);
#471=FACE_OUTER_BOUND('',#697,.T.);
#472=FACE_OUTER_BOUND('',#698,.T.);
#473=FACE_OUTER_BOUND('',#699,.T.);
#474=FACE_OUTER_BOUND('',#700,.T.);
#475=FACE_OUTER_BOUND('',#701,.T.);
#476=FACE_OUTER_BOUND('',#702,.T.);
#477=FACE_OUTER_BOUND('',#703,.T.);
#478=FACE_OUTER_BOUND('',#704,.T.);
#479=FACE_OUTER_BOUND('',#705,.T.);
#480=FACE_OUTER_BOUND('',#706,.T.);
#481=FACE_OUTER_BOUND('',#707,.T.);
#482=FACE_OUTER_BOUND('',#708,.T.);
#483=FACE_OUTER_BOUND('',#710,.T.);
#484=FACE_OUTER_BOUND('',#712,.T.);
#692=EDGE_LOOP('',(#2760,#2761,#2762,#2763));
#693=EDGE_LOOP('',(#2764,#2765,#2766,#2767,#2768,#2769));
#694=EDGE_LOOP('',(#2770,#2771,#2772,#2773,#2774));
#695=EDGE_LOOP('',(#2775,#2776,#2777,#2778,#2779));
#696=EDGE_LOOP('',(#2780,#2781,#2782,#2783,#2784));
#697=EDGE_LOOP('',(#2785,#2786,#2787,#2788,#2789));
#698=EDGE_LOOP('',(#2790,#2791,#2792,#2793,#2794,#2795,#2796,#2797,#2798,
#2799,#2800,#2801,#2802,#2803,#2804,#2805,#2806,#2807));
#699=EDGE_LOOP('',(#2808,#2809,#2810,#2811,#2812,#2813));
#700=EDGE_LOOP('',(#2814,#2815,#2816,#2817));
#701=EDGE_LOOP('',(#2818,#2819,#2820,#2821));
#702=EDGE_LOOP('',(#2822,#2823,#2824,#2825));
#703=EDGE_LOOP('',(#2826,#2827,#2828,#2829,#2830));
#704=EDGE_LOOP('',(#2831,#2832,#2833,#2834,#2835,#2836,#2837,#2838));
#705=EDGE_LOOP('',(#2839,#2840,#2841,#2842,#2843,#2844,#2845,#2846,#2847,
#2848,#2849,#2850,#2851,#2852,#2853,#2854,#2855,#2856,#2857,#2858,#2859));
#706=EDGE_LOOP('',(#2860,#2861,#2862,#2863,#2864,#2865,#2866,#2867,#2868,
#2869,#2870,#2871,#2872,#2873,#2874,#2875,#2876,#2877,#2878,#2879,#2880));
#707=EDGE_LOOP('',(#2881,#2882,#2883,#2884));
#708=EDGE_LOOP('',(#2885));
#709=EDGE_LOOP('',(#2886,#2887,#2888,#2889));
#710=EDGE_LOOP('',(#2890,#2891,#2892,#2893));
#711=EDGE_LOOP('',(#2894,#2895,#2896,#2897));
#712=EDGE_LOOP('',(#2898));
#713=EDGE_LOOP('',(#2899));
#884=LINE('',#15686,#1042);
#885=LINE('',#15959,#1043);
#886=LINE('',#16352,#1044);
#887=LINE('',#16711,#1045);
#888=LINE('',#17052,#1046);
#889=LINE('',#17395,#1047);
#890=LINE('',#21327,#1048);
#891=LINE('',#22114,#1049);
#1042=VECTOR('',#4505,3.72275);
#1043=VECTOR('',#4510,3.72275);
#1044=VECTOR('',#4513,3.72275);
#1045=VECTOR('',#4516,3.72275);
#1046=VECTOR('',#4519,3.72275);
#1047=VECTOR('',#4522,3.72275);
#1048=VECTOR('',#4549,2.204);
#1049=VECTOR('',#4556,5.42440960677665);
#1224=B_SPLINE_CURVE_WITH_KNOTS('',3,(#15688,#15689,#15690,#15691,#15692,
#15693,#15694,#15695,#15696,#15697,#15698,#15699,#15700,#15701,#15702,#15703,
#15704,#15705,#15706,#15707,#15708,#15709,#15710,#15711,#15712,#15713,#15714,
#15715,#15716,#15717,#15718,#15719,#15720,#15721,#15722,#15723,#15724,#15725,
#15726,#15727,#15728,#15729,#15730,#15731,#15732,#15733,#15734,#15735,#15736,
#15737,#15738,#15739,#15740,#15741,#15742,#15743,#15744,#15745,#15746,#15747,
#15748,#15749,#15750,#15751,#15752,#15753,#15754,#15755,#15756,#15757,#15758,
#15759,#15760,#15761,#15762,#15763,#15764,#15765,#15766,#15767,#15768,#15769,
#15770,#15771,#15772,#15773,#15774,#15775,#15776,#15777,#15778,#15779,#15780,
#15781,#15782,#15783,#15784,#15785,#15786,#15787,#15788,#15789,#15790,#15791,
#15792,#15793,#15794,#15795,#15796,#15797,#15798,#15799,#15800,#15801,#15802,
#15803,#15804,#15805,#15806,#15807,#15808,#15809,#15810,#15811,#15812,#15813,
#15814,#15815,#15816,#15817,#15818,#15819,#15820,#15821,#15822,#15823,#15824,
#15825,#15826,#15827,#15828,#15829,#15830,#15831,#15832,#15833,#15834,#15835,
#15836,#15837,#15838,#15839,#15840,#15841),.UNSPECIFIED.,.F.,.F.,(4,3,3,
3,3,3,3,3,3,3,3,3,3,3,3,3,3,3,3,3,3,3,3,3,3,3,3,3,3,3,3,3,3,3,3,3,3,3,3,
3,3,3,3,3,3,3,3,3,3,3,3,4),(10.3761051797602,10.4641373814769,10.5520588327897,
10.6410762182378,10.7288594652779,10.8166179102709,10.9043752172213,10.9943308920096,
11.0822044534747,11.1732011849246,11.2641979163745,11.3543883418031,11.4444664958327,
11.5344565843787,11.6243852832326,11.7142815564214,11.804167167181,11.8940638650899,
11.9840486455302,12.074077267802,12.1642488110667,12.247304603897,12.337349377077,
12.4272819895897,12.517126854226,12.6069114553117,12.6966643802678,12.786407578033,
12.8761629846047,12.9660091578037,13.0559004439681,13.1459382866182,13.2304112914194,
13.3202803122904,13.4100337681398,13.4996963272619,13.5892945887802,13.6788587810357,
13.7684110716423,13.8579736136466,13.947625011734,14.0373201915803,14.1271617222868,
14.2135179789419,14.3034962162208,14.3933692649306,14.4831592957879,14.5728884092593,
14.6625930287075,14.7522802792272,14.8420075718479,14.9177889943201),
 .UNSPECIFIED.);
#1225=B_SPLINE_CURVE_WITH_KNOTS('',3,(#15844,#15845,#15846,#15847,#15848,
#15849,#15850,#15851,#15852,#15853,#15854,#15855,#15856,#15857,#15858,#15859,
#15860,#15861,#15862,#15863,#15864,#15865,#15866,#15867,#15868,#15869,#15870,
#15871,#15872,#15873,#15874,#15875,#15876,#15877,#15878,#15879,#15880,#15881,
#15882,#15883,#15884,#15885,#15886,#15887,#15888,#15889,#15890,#15891,#15892,
#15893,#15894,#15895,#15896,#15897,#15898,#15899,#15900,#15901,#15902,#15903,
#15904,#15905,#15906,#15907,#15908,#15909,#15910,#15911,#15912,#15913,#15914,
#15915,#15916,#15917,#15918,#15919,#15920,#15921,#15922,#15923,#15924,#15925,
#15926,#15927,#15928,#15929,#15930,#15931,#15932,#15933,#15934,#15935,#15936,
#15937,#15938,#15939,#15940,#15941,#15942,#15943,#15944,#15945,#15946,#15947,
#15948,#15949,#15950,#15951,#15952,#15953,#15954,#15955),.UNSPECIFIED.,
 .F.,.F.,(4,3,3,3,3,3,3,3,3,3,3,3,3,3,3,3,3,3,3,3,3,3,3,3,3,3,3,3,3,3,3,
3,3,3,3,3,3,4),(11.6150691238056,11.716887748291,11.818807396451,11.9206982029579,
12.0224123053014,12.1066224675668,12.1974625342849,12.2882944241597,12.379171523673,
12.4700739203339,12.561061507472,12.598175811328,12.6891753523971,12.7800935403341,
12.8709528368157,12.9617902529354,13.0526187338464,13.1434585576012,13.2343300061399,
13.3253148905754,13.4163587789532,13.5075598865992,13.5812824988505,13.6704071444793,
13.7594059294644,13.8483044456942,13.9378150382791,14.0265967435875,14.1153607025908,
14.2041298440541,14.2941946796338,14.3830904507549,14.4737398185639,14.5643891863729,
14.6545593024114,14.7446311850219,14.8346130791444,14.9185734639323),
 .UNSPECIFIED.);
#1226=B_SPLINE_CURVE_WITH_KNOTS('',3,(#15961,#15962,#15963,#15964,#15965,
#15966,#15967,#15968,#15969,#15970,#15971,#15972,#15973,#15974,#15975,#15976,
#15977,#15978,#15979,#15980,#15981,#15982,#15983,#15984,#15985,#15986,#15987,
#15988,#15989,#15990,#15991,#15992,#15993,#15994,#15995,#15996,#15997,#15998,
#15999,#16000,#16001,#16002,#16003,#16004,#16005,#16006,#16007,#16008,#16009,
#16010,#16011,#16012,#16013,#16014,#16015,#16016,#16017,#16018,#16019,#16020,
#16021,#16022,#16023,#16024,#16025,#16026,#16027,#16028,#16029,#16030,#16031,
#16032,#16033,#16034,#16035,#16036,#16037,#16038,#16039,#16040,#16041,#16042,
#16043,#16044,#16045,#16046,#16047,#16048,#16049,#16050,#16051,#16052,#16053,
#16054,#16055,#16056,#16057,#16058,#16059,#16060,#16061,#16062,#16063,#16064,
#16065,#16066,#16067,#16068,#16069,#16070,#16071,#16072,#16073,#16074,#16075,
#16076,#16077,#16078,#16079,#16080,#16081,#16082,#16083,#16084,#16085,#16086,
#16087,#16088,#16089,#16090,#16091,#16092,#16093,#16094,#16095,#16096,#16097,
#16098,#16099,#16100,#16101,#16102,#16103,#16104,#16105,#16106,#16107,#16108,
#16109,#16110,#16111,#16112,#16113,#16114,#16115,#16116,#16117,#16118,#16119,
#16120,#16121,#16122,#16123,#16124,#16125,#16126,#16127,#16128,#16129,#16130,
#16131,#16132,#16133,#16134,#16135,#16136,#16137,#16138,#16139,#16140,#16141,
#16142,#16143,#16144,#16145,#16146,#16147),.UNSPECIFIED.,.F.,.F.,(4,3,3,
3,3,3,3,3,3,3,3,3,3,3,3,3,3,3,3,3,3,3,3,3,3,3,3,3,3,3,3,3,3,3,3,3,3,3,3,
3,3,3,3,3,3,3,3,3,3,3,3,3,3,3,3,3,3,3,3,3,3,3,4),(15.7079632680998,15.8025806359288,
15.8974688589525,15.9924919522917,16.0877730881789,16.1797313539867,16.2696858791206,
16.3595261141865,16.4492766072458,16.5389641976932,16.6286185390501,16.7182616952449,
16.8079157161731,16.8976590020199,16.9874464303251,17.0773798515868,17.1628380415092,
17.2528079127075,17.3426637193691,17.4324299876198,17.5221335971379,17.6118041005047,
17.7014635426848,17.7911339547024,17.8808936965223,17.9706976405523,18.0606475049867,
18.1459447290316,18.2359100492805,18.3257612649324,18.4155229084801,18.5052218615178,
18.5948876907088,18.6845424465949,18.7742081657681,18.8639632336747,18.9537625072052,
19.0437077565897,19.1290514165541,19.2190155261937,19.3088654988141,19.3986258687219,
19.4883235067968,19.5779879963056,19.6676413893196,19.7573057239427,19.8470593814408,
19.9368572283733,20.026801038463,20.1121581040765,20.2021239629424,20.291975712,
20.3817378830449,20.4714373523156,20.5611036906873,20.650758948064,20.7404251603941,
20.8301807051032,20.9199804472223,21.0099261460961,21.095264791599,21.1842153811775,
21.2018918374058),.UNSPECIFIED.);
#1227=B_SPLINE_CURVE_WITH_KNOTS('',3,(#16148,#16149,#16150,#16151,#16152,
#16153,#16154,#16155,#16156,#16157,#16158,#16159,#16160,#16161,#16162,#16163,
#16164,#16165,#16166,#16167,#16168,#16169,#16170,#16171,#16172,#16173,#16174,
#16175),.UNSPECIFIED.,.F.,.F.,(4,3,3,3,3,3,3,3,3,4),(14.9177889943201,15.0076144356903,
15.1021195510773,15.1966246664643,15.2902720900812,15.3837656172365,15.4770712880676,
15.5702644610989,15.6633265890774,15.707963267949),.UNSPECIFIED.);
#1228=B_SPLINE_CURVE_WITH_KNOTS('',3,(#16177,#16178,#16179,#16180,#16181,
#16182,#16183,#16184,#16185,#16186,#16187,#16188,#16189,#16190,#16191,#16192,
#16193,#16194,#16195,#16196,#16197,#16198,#16199,#16200,#16201,#16202,#16203,
#16204),.UNSPECIFIED.,.F.,.F.,(4,3,3,3,3,3,3,3,3,4),(14.9185734639323,15.0084711991854,
15.098356819238,15.188252074111,15.2782346001737,15.3682596620585,15.4584293984242,
15.5474958738954,15.6867796530317,15.707963267949),.UNSPECIFIED.);
#1229=B_SPLINE_CURVE_WITH_KNOTS('',3,(#16205,#16206,#16207,#16208,#16209,
#16210,#16211,#16212,#16213,#16214,#16215,#16216,#16217,#16218,#16219,#16220,
#16221,#16222,#16223,#16224,#16225,#16226,#16227,#16228,#16229,#16230,#16231,
#16232,#16233,#16234,#16235,#16236,#16237,#16238,#16239,#16240,#16241,#16242,
#16243,#16244,#16245,#16246,#16247,#16248,#16249,#16250,#16251,#16252,#16253,
#16254,#16255,#16256,#16257,#16258,#16259,#16260,#16261,#16262,#16263,#16264,
#16265,#16266,#16267,#16268,#16269,#16270,#16271,#16272,#16273,#16274,#16275,
#16276,#16277,#16278,#16279,#16280,#16281,#16282,#16283,#16284,#16285,#16286,
#16287,#16288,#16289,#16290,#16291,#16292,#16293,#16294,#16295,#16296,#16297,
#16298,#16299,#16300,#16301,#16302,#16303,#16304,#16305,#16306,#16307,#16308,
#16309,#16310,#16311,#16312,#16313,#16314,#16315,#16316,#16317,#16318,#16319,
#16320,#16321,#16322,#16323,#16324,#16325,#16326,#16327,#16328,#16329,#16330,
#16331,#16332,#16333,#16334,#16335,#16336,#16337,#16338,#16339,#16340,#16341,
#16342,#16343,#16344,#16345,#16346,#16347,#16348),.UNSPECIFIED.,.F.,.F.,
(4,2,2,2,2,2,2,2,2,2,2,2,2,2,2,2,2,2,2,2,2,2,2,2,2,2,2,2,2,2,2,2,2,2,2,
2,2,2,2,2,2,2,2,2,2,2,2,2,2,2,2,2,2,2,2,2,2,2,2,2,2,2,2,2,2,2,2,2,2,2,2,
4),(-4.68834833989019,-4.65508458841591,-4.59936853516785,-4.5790813115814,
-4.56541263893702,-4.55313285952382,-4.53301523131224,-4.45452755219641,
-4.41709446190139,-4.39439056254963,-4.38478358651806,-4.37733830672561,
-4.36755283705401,-4.34526465960844,-4.26412972485333,-4.23599109014725,
-4.21340244336273,-4.19937405149395,-4.18607249207315,-4.16685171300768,
-4.08269551421159,-4.03611632283646,-4.02238977108734,-4.01437018657326,
-4.00632509367964,-3.99262969623786,-3.91813590387533,-3.86390045301744,
-3.84377785905482,-3.83011327226075,-3.817768394177,-3.79736383803744,-3.74525121754264,
-3.69946993342188,-3.67540166413208,-3.65835341595994,-3.6496444466923,
-3.64206686067612,-3.63050541430058,-3.59036829320484,-3.52605167574737,
-3.50022522337047,-3.47895023408489,-3.46511273157843,-3.45139484396221,
-3.43079594325119,-3.37345492623386,-3.32263607034887,-3.3039700925282,
-3.28972990718864,-3.28158527710179,-3.27363598766241,-3.26037006749997,
-3.19786218381033,-3.13570202782019,-3.11324768666422,-3.09919903590241,
-3.08580451090809,-3.06630060367248,-2.98415154633769,-2.93656061137152,
-2.92269674301749,-2.9146263038001,-2.90659908334924,-2.89296577665551,
-2.81812796262566,-2.77158728473206,-2.74773243946704,-2.73341867447911,
-2.71999272674547,-2.70120049750362,-2.63911108106228),.UNSPECIFIED.);
#1230=B_SPLINE_CURVE_WITH_KNOTS('',3,(#16354,#16355,#16356,#16357,#16358,
#16359,#16360,#16361,#16362,#16363,#16364,#16365,#16366,#16367,#16368,#16369,
#16370,#16371,#16372,#16373,#16374,#16375,#16376,#16377,#16378,#16379,#16380,
#16381,#16382,#16383,#16384,#16385,#16386,#16387,#16388,#16389,#16390,#16391,
#16392,#16393,#16394,#16395,#16396,#16397,#16398,#16399,#16400,#16401,#16402,
#16403,#16404,#16405,#16406,#16407,#16408,#16409,#16410,#16411,#16412,#16413,
#16414,#16415,#16416,#16417,#16418,#16419,#16420,#16421,#16422,#16423,#16424,
#16425,#16426,#16427,#16428,#16429,#16430,#16431,#16432,#16433,#16434,#16435,
#16436,#16437,#16438,#16439,#16440,#16441,#16442,#16443,#16444,#16445,#16446,
#16447,#16448,#16449,#16450,#16451,#16452,#16453,#16454,#16455,#16456,#16457,
#16458,#16459,#16460,#16461,#16462,#16463,#16464,#16465,#16466,#16467,#16468,
#16469,#16470,#16471,#16472,#16473,#16474,#16475,#16476,#16477,#16478,#16479,
#16480,#16481,#16482,#16483,#16484,#16485,#16486,#16487,#16488,#16489,#16490,
#16491,#16492,#16493,#16494,#16495,#16496,#16497,#16498,#16499,#16500,#16501,
#16502,#16503,#16504,#16505),.UNSPECIFIED.,.F.,.F.,(4,2,2,2,2,2,2,2,2,2,
2,2,2,2,2,2,2,2,2,2,2,2,2,2,2,2,2,2,2,2,2,2,2,2,2,2,2,2,2,2,2,2,2,2,2,2,
2,2,2,2,2,2,2,2,2,2,2,2,2,2,2,2,2,2,2,2,2,2,2,2,2,2,2,2,2,4),(-2.04961240608362,
-2.04846731799055,-2.03436004178467,-2.01161307201698,-1.95901316641739,
-1.88542547187917,-1.87319853180591,-1.86620666267941,-1.85804905011015,
-1.84376392206717,-1.8250195380913,-1.77373456495123,-1.71718578570372,
-1.69662030237994,-1.68290586402199,-1.66905647746236,-1.64773020420228,
-1.6218186176251,-1.55705364820425,-1.5172871902438,-1.50578779123524,-1.4982284826178,
-1.48953471339632,-1.47247022460861,-1.44835840631695,-1.40249579092161,
-1.3502259145096,-1.32981793099076,-1.31749643676501,-1.30388097758378,
-1.28388892440881,-1.23041687198386,-1.15449633129897,-1.14103176949053,
-1.13303956077813,-1.12492937753314,-1.11088048165017,-1.06161796178586,
-0.982327429975348,-0.962466786186025,-0.949008683269062,-0.935038023101868,
-0.913039766196341,-0.885971894866213,-0.813642258455964,-0.782550486682968,
-0.771683320463845,-0.764134892944955,-0.755084673027459,-0.736010379366222,
-0.707570669679222,-0.614163672308585,-0.594951686439576,-0.581598840138717,
-0.567460480065028,-0.544540495207097,-0.488926516689361,-0.419679077959112,
-0.406953607062545,-0.39987805797259,-0.391854521371385,-0.378232422063269,
-0.332772474241522,-0.246975016100116,-0.227977242725061,-0.214657643796333,
-0.200455991100291,-0.177189922589633,-0.126906508617021,-0.119577861397492,
-0.0540343017638599,-0.0407615282157486,-0.0328081263525258,-0.0259069908760486,
-0.0150954331368796,-0.000789799928729903),.UNSPECIFIED.);
#1231=B_SPLINE_CURVE_WITH_KNOTS('',3,(#16506,#16507,#16508,#16509,#16510,
#16511,#16512,#16513,#16514,#16515,#16516,#16517,#16518,#16519,#16520,#16521,
#16522,#16523,#16524,#16525,#16526,#16527,#16528,#16529,#16530,#16531,#16532,
#16533),.UNSPECIFIED.,.F.,.F.,(4,3,3,3,3,3,3,3,3,4),(21.2018918374058,21.2907068140922,
21.3794336288738,21.4681122919233,21.556765901624,21.6454175303288,21.7341402280128,
21.8228977713556,21.9117857326907,21.9911485748867),.UNSPECIFIED.);
#1232=B_SPLINE_CURVE_WITH_KNOTS('',3,(#16534,#16535,#16536,#16537,#16538,
#16539,#16540,#16541,#16542,#16543,#16544,#16545,#16546,#16547,#16548,#16549,
#16550,#16551,#16552,#16553,#16554,#16555,#16556,#16557,#16558,#16559,#16560,
#16561,#16562,#16563,#16564,#16565,#16566,#16567,#16568,#16569,#16570,#16571,
#16572,#16573,#16574,#16575,#16576,#16577,#16578,#16579,#16580,#16581,#16582,
#16583,#16584,#16585,#16586,#16587,#16588,#16589,#16590,#16591,#16592,#16593,
#16594,#16595,#16596,#16597,#16598,#16599,#16600,#16601,#16602,#16603,#16604,
#16605,#16606,#16607,#16608,#16609,#16610,#16611,#16612,#16613,#16614,#16615,
#16616,#16617,#16618,#16619,#16620,#16621,#16622,#16623,#16624,#16625,#16626,
#16627,#16628,#16629,#16630,#16631,#16632,#16633,#16634,#16635,#16636,#16637,
#16638,#16639,#16640,#16641,#16642,#16643,#16644,#16645,#16646,#16647,#16648,
#16649,#16650,#16651,#16652,#16653,#16654,#16655,#16656,#16657,#16658,#16659,
#16660,#16661,#16662,#16663,#16664,#16665,#16666,#16667,#16668,#16669,#16670,
#16671,#16672,#16673,#16674,#16675,#16676,#16677,#16678,#16679,#16680,#16681,
#16682,#16683,#16684,#16685,#16686,#16687,#16688,#16689,#16690,#16691,#16692,
#16693,#16694,#16695,#16696,#16697,#16698,#16699,#16700,#16701,#16702,#16703,
#16704,#16705,#16706,#16707),.UNSPECIFIED.,.F.,.F.,(4,2,2,2,2,2,2,2,2,2,
2,2,2,2,2,2,2,2,2,2,2,2,2,2,2,2,2,2,2,2,2,2,2,2,2,2,2,2,2,2,2,2,2,2,2,2,
2,2,2,2,2,2,2,2,2,2,2,2,2,2,2,2,2,2,2,2,2,2,2,2,2,2,2,2,2,2,2,2,2,2,2,2,
2,2,2,2,4),(-2.63911108106228,-2.61389722979619,-2.58107538358811,-2.5601522761232,
-2.550795983286,-2.54328991325651,-2.53288104898045,-2.50600697108263,-2.4295932887207,
-2.38954025089258,-2.37273638949239,-2.35967215395335,-2.34446025202537,
-2.31550887548481,-2.27478735054413,-2.20378467546804,-2.18955829491125,
-2.18141270854979,-2.17345219573091,-2.16014719142536,-2.14315008517139,
-2.10088252274014,-2.03204595619649,-2.01134104316741,-1.99760171142334,
-1.98377849291404,-1.9626008425893,-1.93694244287669,-1.87367392801601,
-1.83199842659466,-1.82042487480467,-1.81285385872645,-1.80419083149189,
-1.78729624834157,-1.76353300680594,-1.66860729576893,-1.64625056094355,
-1.6322141983133,-1.61864286052398,-1.59891660989387,-1.53138463918856,
-1.46857629414052,-1.45531358220379,-1.44736134632962,-1.43920489637716,
-1.42492578659526,-1.40619239993965,-1.3549702034927,-1.29834119110781,
-1.27777341702507,-1.26405860720962,-1.25020973837015,-1.22888621542746,
-1.20297938762556,-1.13824420357628,-1.0984372513944,-1.08693609302705,
-1.07937656536868,-1.07068367372916,-1.05362397636827,-1.02952203417856,
-0.98364443777249,-0.931370926167948,-0.910962639701207,-0.898641060894736,
-0.885025586405433,-0.865033684567714,-0.81156307559681,-0.735639094077008,
-0.722174965910665,-0.714182807345869,-0.706072383932551,-0.692022659349403,
-0.642753345690428,-0.563473062628527,-0.543610957050241,-0.530152467778737,
-0.516181876455237,-0.4941847686508,-0.467119020859666,-0.394805623179322,
-0.363695858756982,-0.352826988555971,-0.345278305435169,-0.336228972575739,
-0.31715997569338,-0.295509696228243),.UNSPECIFIED.);
#1233=B_SPLINE_CURVE_WITH_KNOTS('',3,(#16712,#16713,#16714,#16715,#16716,
#16717,#16718,#16719,#16720,#16721,#16722,#16723,#16724,#16725,#16726,#16727,
#16728,#16729,#16730,#16731,#16732,#16733,#16734,#16735,#16736,#16737,#16738,
#16739,#16740,#16741,#16742,#16743,#16744,#16745,#16746,#16747,#16748,#16749,
#16750,#16751,#16752,#16753,#16754,#16755,#16756,#16757,#16758,#16759,#16760,
#16761,#16762,#16763,#16764,#16765,#16766,#16767,#16768,#16769,#16770,#16771,
#16772,#16773,#16774,#16775,#16776,#16777,#16778,#16779,#16780,#16781,#16782,
#16783,#16784,#16785,#16786,#16787,#16788,#16789,#16790,#16791,#16792,#16793,
#16794,#16795,#16796,#16797,#16798,#16799,#16800,#16801,#16802,#16803,#16804,
#16805,#16806,#16807,#16808,#16809,#16810,#16811,#16812,#16813,#16814,#16815,
#16816,#16817,#16818,#16819,#16820,#16821,#16822,#16823,#16824,#16825,#16826,
#16827,#16828,#16829,#16830,#16831,#16832,#16833,#16834,#16835,#16836,#16837,
#16838,#16839,#16840,#16841,#16842,#16843,#16844,#16845,#16846,#16847,#16848,
#16849,#16850,#16851,#16852,#16853,#16854,#16855,#16856,#16857,#16858,#16859,
#16860,#16861,#16862,#16863,#16864,#16865,#16866,#16867,#16868,#16869,#16870,
#16871,#16872,#16873,#16874,#16875,#16876,#16877,#16878,#16879,#16880,#16881),
 .UNSPECIFIED.,.F.,.F.,(4,2,2,2,2,2,2,2,2,2,2,2,2,2,2,2,2,2,2,2,2,2,2,2,
2,2,2,2,2,2,2,2,2,2,2,2,2,2,2,2,2,2,2,2,2,2,2,2,2,2,2,2,2,2,2,2,2,2,2,2,
2,2,2,2,2,2,2,2,2,2,2,2,2,2,2,2,2,2,2,2,2,2,2,2,4),(-4.39331191224356,-4.37560145592145,
-4.3114098378457,-4.28559723109706,-4.26432706433371,-4.25048666776118,
-4.23676120924672,-4.2161396052254,-4.15758212839039,-4.10780046029863,
-4.08932156506745,-4.07518332955413,-4.06705468353004,-4.05907733379765,
-4.04569037808528,-3.96933062871353,-3.91612022710783,-3.89616390726823,
-3.88255322030396,-3.87022374256306,-3.84977313359501,-3.77616507531547,
-3.71850135239065,-3.70650134333133,-3.69878481714542,-3.69025645248449,
-3.67407947539339,-3.64217220063643,-3.57796963814975,-3.55215538960743,
-3.53088434176985,-3.51704392408621,-3.50331884229407,-3.48269860268792,
-3.42419311520387,-3.37437279924298,-3.35588700498925,-3.3417450061456,
-3.33361567696377,-3.32563914287365,-3.31225590056248,-3.23587587640272,
-3.18267746757575,-3.16272300834602,-3.14911278114548,-3.13678321930216,
-3.1163312519161,-3.06325580215698,-3.00912957786561,-2.98134994717596,
-2.97106215474424,-2.96356598998976,-2.95412369418129,-2.93263443394907,
-2.84990538773865,-2.8215710499691,-2.79885016675484,-2.78474706393444,
-2.77137168957434,-2.75202549340976,-2.6686528381238,-2.63410367221121,
-2.61888788716139,-2.60662398920565,-2.59886141854827,-2.5904255250284,
-2.574729418821,-2.49848379943591,-2.46222890543053,-2.4353573334932,-2.42050346161586,
-2.40725506197321,-2.39007210853799,-2.34835036770994,-2.34385649726276,
-2.30125828656882,-2.25500136049857,-2.24127765538967,-2.23323329900269,
-2.22517822282473,-2.21140203063287,-2.16460737724514,-2.0811651465222,
-2.06183878417439,-2.04961240608362),.UNSPECIFIED.);
#1234=B_SPLINE_CURVE_WITH_KNOTS('',3,(#16883,#16884,#16885,#16886,#16887,
#16888,#16889,#16890,#16891,#16892,#16893,#16894,#16895,#16896,#16897,#16898,
#16899,#16900,#16901,#16902),.UNSPECIFIED.,.F.,.F.,(4,2,2,2,2,2,2,2,2,4),
(-0.295509696228243,-0.288732319901063,-0.195289147016525,-0.176083510006063,
-0.162731641333534,-0.148591438424712,-0.125661485943037,-0.0784178946907411,
-0.0433454634721789,-0.000849774496175227),.UNSPECIFIED.);
#1235=B_SPLINE_CURVE_WITH_KNOTS('',3,(#16903,#16904,#16905,#16906,#16907,
#16908,#16909,#16910,#16911,#16912,#16913,#16914,#16915,#16916,#16917,#16918,
#16919,#16920,#16921,#16922,#16923,#16924,#16925,#16926,#16927,#16928,#16929,
#16930,#16931,#16932,#16933,#16934,#16935,#16936,#16937,#16938,#16939,#16940,
#16941,#16942,#16943,#16944,#16945,#16946,#16947,#16948,#16949,#16950,#16951,
#16952,#16953,#16954,#16955,#16956,#16957,#16958,#16959,#16960,#16961,#16962,
#16963,#16964,#16965,#16966,#16967,#16968,#16969,#16970,#16971,#16972,#16973,
#16974,#16975,#16976,#16977,#16978,#16979,#16980,#16981,#16982,#16983,#16984,
#16985,#16986,#16987,#16988,#16989,#16990,#16991,#16992,#16993,#16994,#16995,
#16996,#16997,#16998,#16999,#17000,#17001,#17002,#17003,#17004,#17005,#17006,
#17007,#17008,#17009,#17010,#17011,#17012,#17013,#17014,#17015,#17016,#17017,
#17018,#17019,#17020,#17021,#17022,#17023,#17024,#17025,#17026,#17027,#17028,
#17029,#17030,#17031,#17032,#17033,#17034,#17035,#17036,#17037,#17038,#17039,
#17040,#17041,#17042,#17043,#17044,#17045,#17046,#17047,#17048),
 .UNSPECIFIED.,.F.,.F.,(4,2,2,2,2,2,2,2,2,2,2,2,2,2,2,2,2,2,2,2,2,2,2,2,
2,2,2,2,2,2,2,2,2,2,2,2,2,2,2,2,2,2,2,2,2,2,2,2,2,2,2,2,2,2,2,2,2,2,2,2,
2,2,2,2,2,2,2,2,2,2,2,2,4),(-4.68759801305522,-4.6786154966478,-4.67025567535162,
-4.6628645751344,-4.65223210683701,-4.62317292131303,-4.59213647822212,
-4.52143234373722,-4.49938333712422,-4.48540599860914,-4.47195826986589,
-4.45214546014359,-4.37245518818805,-4.32342159994108,-4.30939887528759,
-4.30129530818617,-4.29330073673223,-4.27981849315781,-4.20409229043172,
-4.15057732839138,-4.13058263478209,-4.11696897906048,-4.10465114727064,
-4.0842547132693,-4.03221306536484,-3.97725754120375,-3.95789045640485,
-3.94326715242319,-3.93504326786529,-3.92714848444638,-3.91417148670484,
-3.84726916472332,-3.78980183252394,-3.76692840033962,-3.75280000279642,
-3.73944452763723,-3.72020714318806,-3.6360969864323,-3.58966282756493,
-3.5759287196203,-3.56788324248193,-3.56082448852716,-3.54819342919581,
-3.47820160032019,-3.42252834510268,-3.39998001298162,-3.38591079074289,
-3.37252052124575,-3.35306586152839,-3.27055413659815,-3.22319745262476,
-3.20935867548291,-3.20129183736159,-3.19424689712922,-3.18169770743099,
-3.11098978407951,-3.06832188780665,-3.03852247171375,-3.02317149459409,
-3.00999824711346,-2.99332968738289,-2.95718388232658,-2.89082012494614,
-2.85159959278265,-2.84030044630581,-2.83269667724201,-2.82387792395333,
-2.80612186603167,-2.73236496483843,-2.67943159839657,-2.66144687690544,
-2.6481406310148,-2.63907567363619),.UNSPECIFIED.);
#1236=B_SPLINE_CURVE_WITH_KNOTS('',3,(#17054,#17055,#17056,#17057,#17058,
#17059,#17060,#17061,#17062,#17063,#17064,#17065,#17066,#17067,#17068,#17069,
#17070,#17071,#17072,#17073,#17074,#17075,#17076,#17077,#17078,#17079,#17080,
#17081,#17082,#17083,#17084,#17085,#17086,#17087,#17088,#17089,#17090,#17091,
#17092,#17093,#17094,#17095,#17096,#17097,#17098,#17099,#17100,#17101,#17102,
#17103,#17104,#17105,#17106,#17107,#17108,#17109,#17110,#17111,#17112,#17113,
#17114,#17115,#17116,#17117,#17118,#17119,#17120,#17121,#17122,#17123,#17124,
#17125,#17126,#17127,#17128,#17129,#17130,#17131,#17132,#17133,#17134,#17135,
#17136,#17137,#17138,#17139,#17140,#17141,#17142,#17143,#17144,#17145,#17146,
#17147,#17148,#17149,#17150,#17151,#17152,#17153,#17154,#17155,#17156,#17157,
#17158,#17159,#17160,#17161,#17162,#17163,#17164,#17165,#17166,#17167,#17168,
#17169,#17170,#17171,#17172,#17173,#17174,#17175,#17176,#17177,#17178,#17179,
#17180,#17181,#17182,#17183,#17184,#17185,#17186,#17187,#17188,#17189,#17190,
#17191,#17192,#17193,#17194,#17195,#17196,#17197,#17198,#17199,#17200,#17201),
 .UNSPECIFIED.,.F.,.F.,(4,2,2,2,2,2,2,2,2,2,2,2,2,2,2,2,2,2,2,2,2,2,2,2,
2,2,2,2,2,2,2,2,2,2,2,2,2,2,2,2,2,2,2,2,2,2,2,2,2,2,2,2,2,2,2,2,2,2,2,2,
2,2,2,2,2,2,2,2,2,2,2,2,2,4),(-2.04935972616353,-2.00287868864084,-1.96348539660213,
-1.95200435192754,-1.94437392958132,-1.93564018773703,-1.91835400231652,
-1.89378364346478,-1.82847651371751,-1.78860668362923,-1.77170794880324,
-1.75849218522515,-1.74347937011549,-1.71568714435376,-1.67749745058458,
-1.60037752081791,-1.58711454399874,-1.57916308051959,-1.57100770911776,
-1.5567326033437,-1.53800606871541,-1.48681916417169,-1.43015414516619,
-1.40958628073977,-1.39587173439376,-1.38202329951776,-1.36070058607619,
-1.33479451720022,-1.27005605998517,-1.23011621418989,-1.21868834586002,
-1.21106512230926,-1.20230541250574,-1.18487847669069,-1.16001557566708,
-1.0929767775654,-1.05499434189848,-1.03822663041946,-1.02502320336602,
-1.00992791218209,-0.981656924503879,-0.942434965128106,-0.867914165428893,
-0.85422610342954,-0.846189507761945,-0.838128212684673,-0.824318846986697,
-0.777223782108126,-0.69431711325095,-0.674921111776785,-0.661539525701319,
-0.647453112958258,-0.624815189644104,-0.596623704581938,-0.515252020022513,
-0.493211842317082,-0.483437121690746,-0.475956048139001,-0.466225246491797,
-0.442774749118955,-0.40318202197825,-0.329983945530972,-0.309512549739534,
-0.297181605479188,-0.283577339444177,-0.263648092338427,-0.210617963199273,
-0.133874640825955,-0.120547771633543,-0.112583317500223,-0.104442666036868,
-0.090240784549733,-0.071647175289315,-0.000795291253163828),
 .UNSPECIFIED.);
#1237=B_SPLINE_CURVE_WITH_KNOTS('',3,(#17202,#17203,#17204,#17205,#17206,
#17207,#17208,#17209,#17210,#17211,#17212,#17213,#17214,#17215,#17216,#17217,
#17218,#17219,#17220,#17221,#17222,#17223,#17224,#17225,#17226,#17227),
 .UNSPECIFIED.,.F.,.F.,(4,2,2,2,2,2,2,2,2,2,2,2,4),(-4.68819911033501,-4.64525715217843,
-4.63117657311148,-4.6173221871197,-4.60361287686467,-4.58307549428896,
-4.48482308210793,-4.46082893190692,-4.44382216683465,-4.43513850354181,
-4.42757461095918,-4.41604906773608,-4.39331191224356),.UNSPECIFIED.);
#1238=B_SPLINE_CURVE_WITH_KNOTS('',3,(#17228,#17229,#17230,#17231,#17232,
#17233,#17234,#17235,#17236,#17237,#17238,#17239,#17240,#17241,#17242,#17243,
#17244,#17245,#17246,#17247,#17248,#17249,#17250,#17251,#17252,#17253,#17254,
#17255,#17256,#17257,#17258,#17259,#17260,#17261,#17262,#17263,#17264,#17265,
#17266,#17267,#17268,#17269,#17270,#17271,#17272,#17273,#17274,#17275,#17276,
#17277,#17278,#17279,#17280,#17281,#17282,#17283,#17284,#17285,#17286,#17287,
#17288,#17289,#17290,#17291,#17292,#17293,#17294,#17295,#17296,#17297,#17298,
#17299,#17300,#17301,#17302,#17303,#17304,#17305,#17306,#17307,#17308,#17309,
#17310,#17311,#17312,#17313,#17314,#17315,#17316,#17317,#17318,#17319,#17320,
#17321,#17322,#17323,#17324,#17325,#17326,#17327,#17328,#17329,#17330,#17331,
#17332,#17333,#17334,#17335,#17336,#17337,#17338,#17339,#17340,#17341,#17342,
#17343,#17344,#17345,#17346,#17347,#17348,#17349,#17350,#17351,#17352,#17353,
#17354,#17355,#17356,#17357,#17358,#17359,#17360,#17361,#17362,#17363,#17364,
#17365,#17366,#17367,#17368,#17369,#17370,#17371,#17372,#17373,#17374,#17375,
#17376,#17377,#17378,#17379,#17380,#17381,#17382,#17383,#17384,#17385,#17386,
#17387,#17388,#17389,#17390,#17391),.UNSPECIFIED.,.F.,.F.,(4,2,2,2,2,2,
2,2,2,2,2,2,2,2,2,2,2,2,2,2,2,2,2,2,2,2,2,2,2,2,2,2,2,2,2,2,2,2,2,2,2,2,
2,2,2,2,2,2,2,2,2,2,2,2,2,2,2,2,2,2,2,2,2,2,2,2,2,2,2,2,2,2,2,2,2,2,2,2,
2,2,2,4),(-2.63907567363619,-2.63353064505958,-2.60801751905643,-2.51818800140292,
-2.49479434972446,-2.47808392415393,-2.46945635872354,-2.46187412559938,
-2.4502223575671,-2.40612004016064,-2.34478194314754,-2.30928323673228,
-2.2926220067423,-2.27944848095648,-2.26409046468512,-2.23425393364265,
-2.19149993939338,-2.12089221799156,-2.10832363955171,-2.10127501114432,
-2.09321211442392,-2.07939549960996,-2.03223776300458,-1.94943690180683,
-1.93002619597174,-1.91664203229402,-1.90255915283176,-1.87994177010337,
-1.85178694147416,-1.7707496135778,-1.74841606446426,-1.73859433539439,
-1.73111211809046,-1.72142614200125,-1.69829122941282,-1.65960041540032,
-1.58477467030498,-1.5644394207457,-1.55212975652146,-1.53850310778816,
-1.51844223550693,-1.46447164355286,-1.38948677230892,-1.37587171732104,
-1.36784953210292,-1.35977237914557,-1.34588590918342,-1.29810522081131,
-1.21636511959362,-1.19681330354961,-1.18340621499847,-1.16936013767159,
-1.14694547490303,-1.08421091076134,-1.02219894994912,-1.00890328300781,
-1.00094508148897,-0.992797233755798,-0.978559498632532,-0.959900844567123,
-0.909097408675758,-0.851941088797705,-0.831359631322577,-0.81764288970605,
-0.803797493844524,-0.782490762786256,-0.756611941812649,-0.692038181975799,
-0.65215359208302,-0.640590333439407,-0.633021623663755,-0.624356235392163,
-0.607443723800613,-0.583642199543344,-0.537336869832293,-0.484974895067171,
-0.464563490487046,-0.452241981576471,-0.438628053287245,-0.418641583518384,
-0.365204452142173,-0.295612647763091),.UNSPECIFIED.);
#1239=B_SPLINE_CURVE_WITH_KNOTS('',3,(#17396,#17397,#17398,#17399,#17400,
#17401,#17402,#17403,#17404,#17405,#17406,#17407,#17408,#17409,#17410,#17411,
#17412,#17413,#17414,#17415,#17416,#17417,#17418,#17419,#17420,#17421,#17422,
#17423,#17424,#17425,#17426,#17427,#17428,#17429,#17430,#17431,#17432,#17433,
#17434,#17435,#17436,#17437,#17438,#17439,#17440,#17441,#17442,#17443,#17444,
#17445,#17446,#17447,#17448,#17449,#17450,#17451,#17452,#17453,#17454,#17455,
#17456,#17457,#17458,#17459,#17460,#17461,#17462,#17463,#17464,#17465,#17466,
#17467,#17468,#17469,#17470,#17471,#17472,#17473,#17474,#17475,#17476,#17477,
#17478,#17479,#17480,#17481,#17482,#17483,#17484,#17485,#17486,#17487,#17488,
#17489,#17490,#17491,#17492,#17493,#17494,#17495,#17496,#17497,#17498,#17499,
#17500,#17501,#17502,#17503,#17504,#17505,#17506,#17507,#17508,#17509,#17510,
#17511,#17512,#17513,#17514,#17515,#17516,#17517,#17518,#17519,#17520,#17521,
#17522,#17523,#17524,#17525,#17526,#17527,#17528,#17529,#17530,#17531,#17532,
#17533,#17534,#17535,#17536,#17537,#17538,#17539,#17540,#17541,#17542,#17543,
#17544,#17545,#17546,#17547,#17548,#17549,#17550,#17551,#17552,#17553,#17554,
#17555,#17556,#17557,#17558,#17559,#17560,#17561,#17562,#17563,#17564,#17565),
 .UNSPECIFIED.,.F.,.F.,(4,2,2,2,2,2,2,2,2,2,2,2,2,2,2,2,2,2,2,2,2,2,2,2,
2,2,2,2,2,2,2,2,2,2,2,2,2,2,2,2,2,2,2,2,2,2,2,2,2,2,2,2,2,2,2,2,2,2,2,2,
2,2,2,2,2,2,2,2,2,2,2,2,2,2,2,2,2,2,2,2,2,2,2,2,4),(-4.39249448366002,-4.39228442382296,
-4.36624522775283,-4.34485517680281,-4.33099492328683,-4.31729089254084,
-4.29679124486917,-4.24399423786801,-4.172528765972,-4.15602898563903,-4.14745955520206,
-4.13991509140376,-4.12831425695246,-4.08789120042157,-4.02379879994784,
-3.99803204674711,-3.97681200166545,-3.9630349475578,-3.94940204568254,
-3.92899435544657,-3.85525075729416,-3.81579601526264,-3.79240788871937,
-3.78271487454789,-3.77524925625372,-3.76548718305355,-3.74352427155699,
-3.66209112923551,-3.63388215347115,-3.61121976053594,-3.59710457897656,
-3.58368272597902,-3.56419577308114,-3.47257812657962,-3.44365114130089,
-3.42435936505704,-3.41525470764449,-3.40769761272765,-3.39684962061223,
-3.36599748914682,-3.29354789752857,-3.26647814779013,-3.24448123979525,
-3.23051506763327,-3.21706384211106,-3.19722018365833,-3.11760336747554,
-3.06841041023518,-3.05437157203105,-3.04626818824091,-3.0382849418778,
-3.02484490256617,-2.94885975518951,-2.89546622904403,-2.87549195522435,
-2.86188643880914,-2.84957298542905,-2.82917792216145,-2.77709802182455,
-2.70079830107649,-2.68727129968986,-2.67926965420796,-2.67117489870268,
-2.65720358177509,-2.60457039569869,-2.53390708957793,-2.51142016148291,
-2.49735857056104,-2.48395523679781,-2.46444270405563,-2.37267539332504,
-2.34364890820992,-2.32431707470038,-2.31522133147941,-2.30843999794085,
-2.29821281914258,-2.27093899867751,-2.21874914374114,-2.16336653594517,
-2.14283376699984,-2.12912626819679,-2.11527268489251,-2.09391646697886,
-2.06795334450763,-2.04935972616353),.UNSPECIFIED.);
#1240=B_SPLINE_CURVE_WITH_KNOTS('',3,(#17567,#17568,#17569,#17570,#17571,
#17572,#17573,#17574,#17575,#17576,#17577,#17578,#17579,#17580,#17581,#17582,
#17583,#17584,#17585,#17586,#17587,#17588,#17589,#17590,#17591,#17592),
 .UNSPECIFIED.,.F.,.F.,(4,2,2,2,2,2,2,2,2,2,2,2,4),(-0.295612647763091,
-0.289227568051325,-0.275773653121545,-0.267783893754413,-0.259672125375975,
-0.245613574134191,-0.196256444162708,-0.116878554200494,-0.0971127347560032,
-0.0836709007961119,-0.069678723514285,-0.0553703118653591,-0.000790905559261049),
 .UNSPECIFIED.);
#1241=B_SPLINE_CURVE_WITH_KNOTS('',3,(#17593,#17594,#17595,#17596,#17597,
#17598,#17599,#17600,#17601,#17602,#17603,#17604,#17605,#17606,#17607,#17608,
#17609,#17610,#17611,#17612,#17613,#17614,#17615,#17616,#17617,#17618,#17619,
#17620,#17621,#17622,#17623,#17624,#17625,#17626,#17627,#17628,#17629,#17630,
#17631,#17632,#17633,#17634,#17635,#17636,#17637,#17638,#17639,#17640,#17641,
#17642,#17643,#17644,#17645,#17646,#17647,#17648,#17649,#17650,#17651,#17652,
#17653,#17654,#17655,#17656,#17657,#17658,#17659,#17660,#17661,#17662,#17663,
#17664,#17665,#17666,#17667,#17668,#17669,#17670,#17671,#17672,#17673,#17674,
#17675,#17676,#17677,#17678,#17679,#17680,#17681,#17682,#17683,#17684,#17685,
#17686,#17687,#17688,#17689,#17690,#17691,#17692,#17693,#17694,#17695,#17696,
#17697,#17698,#17699,#17700,#17701,#17702,#17703,#17704,#17705,#17706,#17707,
#17708,#17709,#17710,#17711,#17712,#17713,#17714,#17715,#17716,#17717,#17718,
#17719,#17720,#17721,#17722,#17723,#17724,#17725,#17726,#17727,#17728,#17729,
#17730,#17731,#17732,#17733,#17734,#17735,#17736,#17737,#17738,#17739,#17740,
#17741,#17742,#17743,#17744,#17745,#17746,#17747,#17748,#17749,#17750,#17751,
#17752,#17753,#17754,#17755,#17756,#17757,#17758,#17759,#17760,#17761,#17762,
#17763,#17764,#17765,#17766,#17767,#17768,#17769,#17770,#17771,#17772,#17773,
#17774,#17775,#17776,#17777,#17778,#17779),.UNSPECIFIED.,.F.,.F.,(4,3,3,
3,3,3,3,3,3,3,3,3,3,3,3,3,3,3,3,3,3,3,3,3,3,3,3,3,3,3,3,3,3,3,3,3,3,3,3,
3,3,3,3,3,3,3,3,3,3,3,3,3,3,3,3,3,3,3,3,3,3,3,4),(40.8407044968192,40.951482526017,
41.0639840497603,41.1082697494789,41.1982356380105,41.2880874111166,41.3778496006144,
41.4675490798005,41.5572154228913,41.6468706797942,41.7365368864571,41.8262924173454,
41.9160921411777,42.0060378143554,42.0913764370014,42.1813404376952,42.2711903224086,
42.360950625365,42.450648228453,42.5403127024289,42.6299660993487,42.7196304573156,
42.8093841686622,42.8991820861551,42.9891259945089,43.0744831245238,43.1644485683026,
43.2542998832628,43.3440616019953,43.4337605934291,43.5234264386267,43.6130811881496,
43.7027468785928,43.7925018826807,43.8823010731662,43.9722462076546,44.0575898120463,
44.1475598558189,44.2374158021611,44.3271821773257,44.4168858437695,44.5065563736366,
44.5962158119131,44.6858861896211,44.7756458494045,44.8654496852523,44.9553993981455,
45.0406964995687,45.1306501229485,45.2204896313972,45.3102395722759,45.3999268766119,
45.4895810937788,45.5792242875719,45.6688785078763,45.7586222469766,45.8484102676146,
45.9383445117658,46.0238031870912,46.1137612809231,46.2036191334627,46.2933813462544,
46.3346777312564),.UNSPECIFIED.);
#1242=B_SPLINE_CURVE_WITH_KNOTS('',3,(#17783,#17784,#17785,#17786,#17787,
#17788,#17789,#17790,#17791,#17792,#17793,#17794,#17795,#17796,#17797,#17798,
#17799,#17800,#17801,#17802,#17803,#17804,#17805,#17806,#17807,#17808,#17809,
#17810,#17811,#17812,#17813,#17814,#17815,#17816,#17817,#17818,#17819,#17820,
#17821,#17822,#17823,#17824,#17825,#17826,#17827,#17828,#17829,#17830,#17831,
#17832,#17833,#17834,#17835,#17836,#17837,#17838,#17839,#17840,#17841,#17842,
#17843,#17844,#17845,#17846,#17847,#17848,#17849,#17850,#17851,#17852,#17853,
#17854,#17855,#17856,#17857,#17858),.UNSPECIFIED.,.F.,.F.,(4,3,3,3,3,3,
3,3,3,3,3,3,3,3,3,3,3,3,3,3,3,3,3,3,3,4),(-4.09289414414334,-3.95955978524779,
-3.93242675008978,-3.84608852572687,-3.75985370563718,-3.67370105299863,
-3.58315342919472,-3.49709435009809,-3.41104793156076,-3.32499509288074,
-3.2389167535879,-3.15274805448362,-3.06652690774132,-2.98018641192965,
-2.94932006256734,-2.86503523867605,-2.7808550431761,-2.69675631414078,
-2.61271378948831,-2.52869995275755,-2.44469404013561,-2.36067529736391,
-2.27657679923735,-2.1924341240595,-2.10817127163918,-2.0620931210805),
 .UNSPECIFIED.);
#1243=B_SPLINE_CURVE_WITH_KNOTS('',3,(#17862,#17863,#17864,#17865,#17866,
#17867,#17868,#17869,#17870,#17871,#17872,#17873,#17874,#17875,#17876,#17877,
#17878,#17879,#17880,#17881,#17882,#17883,#17884,#17885,#17886,#17887,#17888,
#17889,#17890,#17891,#17892,#17893,#17894,#17895,#17896,#17897,#17898),
 .UNSPECIFIED.,.F.,.F.,(4,3,3,3,3,3,3,3,3,3,3,3,4),(1.81618237516675E-14,
0.097465303689673,0.19598731370756,0.293525795470838,0.39253956961603,0.491553343761223,
0.578514655128871,0.6654680789535,0.752463591152448,0.839480487924647,0.926580031428077,
0.983106687522448,1.10990010696217),.UNSPECIFIED.);
#1244=B_SPLINE_CURVE_WITH_KNOTS('',3,(#17900,#17901,#17902,#17903,#17904,
#17905,#17906,#17907,#17908,#17909,#17910,#17911,#17912,#17913,#17914,#17915,
#17916,#17917,#17918,#17919,#17920,#17921,#17922,#17923,#17924,#17925,#17926,
#17927,#17928,#17929,#17930,#17931,#17932,#17933,#17934,#17935,#17936,#17937,
#17938,#17939,#17940,#17941,#17942,#17943,#17944,#17945,#17946,#17947,#17948,
#17949,#17950,#17951,#17952,#17953,#17954,#17955,#17956,#17957,#17958,#17959,
#17960,#17961,#17962,#17963,#17964,#17965,#17966,#17967,#17968,#17969,#17970,
#17971,#17972,#17973,#17974,#17975,#17976,#17977,#17978,#17979,#17980,#17981,
#17982,#17983,#17984,#17985,#17986,#17987,#17988,#17989,#17990,#17991,#17992,
#17993,#17994,#17995,#17996,#17997,#17998,#17999,#18000,#18001,#18002,#18003,
#18004,#18005,#18006,#18007,#18008,#18009,#18010,#18011,#18012,#18013,#18014,
#18015,#18016,#18017,#18018,#18019,#18020,#18021,#18022,#18023,#18024,#18025,
#18026,#18027,#18028,#18029,#18030,#18031,#18032,#18033,#18034,#18035,#18036,
#18037,#18038,#18039,#18040,#18041,#18042,#18043,#18044,#18045,#18046,#18047,
#18048,#18049,#18050,#18051,#18052,#18053,#18054,#18055,#18056,#18057,#18058,
#18059,#18060,#18061,#18062,#18063,#18064,#18065,#18066,#18067,#18068,#18069,
#18070,#18071,#18072,#18073,#18074,#18075,#18076,#18077,#18078,#18079,#18080,
#18081,#18082,#18083,#18084,#18085,#18086,#18087,#18088,#18089,#18090,#18091,
#18092,#18093,#18094,#18095,#18096,#18097,#18098,#18099,#18100,#18101,#18102,
#18103,#18104,#18105,#18106,#18107,#18108,#18109,#18110,#18111,#18112,#18113,
#18114,#18115,#18116,#18117,#18118,#18119,#18120,#18121,#18122,#18123,#18124,
#18125,#18126,#18127,#18128),.UNSPECIFIED.,.F.,.F.,(4,3,3,3,3,3,3,3,3,3,
3,3,3,3,3,3,3,3,3,3,3,3,3,3,3,3,3,3,3,3,3,3,3,3,3,3,3,3,3,3,3,3,3,3,3,3,
3,3,3,3,3,3,3,3,3,3,3,3,3,3,3,3,3,3,3,3,3,3,3,3,3,3,3,3,3,3,4),(1.10990010708344,
1.1961286058751,1.28229535123711,1.36843172567019,1.4545539136249,1.54068094018495,
1.62683182926768,1.71308212960078,1.79938293490773,1.88582928212476,1.96621337504489,
2.05153108173538,2.13673294970428,2.22184143229054,2.30687888662215,2.3918736400768,
2.47684792459047,2.56182185653531,2.64681554817045,2.73189761684025,2.81702879702236,
2.90228614623796,2.94932006256734,3.03565805991247,3.12189270046458,3.2080452208331,
3.29859291199018,3.38465197828492,3.47069842778444,3.55675134115351,3.64282979885581,
3.72899868109771,3.81522004855201,3.90156081956687,3.93242675008978,4.01862531663163,
4.10472062379942,4.19073408969261,4.27668705919604,4.36260993804403,4.44852003617063,
4.53443659800429,4.62037886781216,4.70641359734286,4.79250118256877,4.87871238538384,
4.91553343761223,5.00156375899611,5.08748769640701,5.17332689219006,5.25910291179368,
5.3448454961129,5.43057326880457,5.51630566495775,5.60206211830088,5.68790953458488,
5.77380869437548,5.85983139642645,5.89864012513467,5.98479447136155,6.07084407042382,
6.15681040430506,6.24271488026911,6.32858741328564,6.41444602624368,6.50031001604005,
6.58619867867155,6.67217852283113,6.75821041676436,6.84436517205843,6.88174681265712,
6.97139414465698,7.06090018627908,7.15023013756892,7.23945576258717,7.32855559990409,
7.39308541414175),.UNSPECIFIED.);
#1245=B_SPLINE_CURVE_WITH_KNOTS('',3,(#18130,#18131,#18132,#18133,#18134,
#18135,#18136,#18137,#18138,#18139,#18140,#18141,#18142,#18143,#18144,#18145,
#18146,#18147,#18148,#18149,#18150,#18151,#18152,#18153,#18154,#18155,#18156,
#18157,#18158,#18159,#18160,#18161,#18162,#18163,#18164,#18165,#18166,#18167,
#18168,#18169,#18170,#18171,#18172,#18173,#18174,#18175,#18176,#18177,#18178,
#18179,#18180,#18181,#18182,#18183,#18184,#18185,#18186,#18187,#18188,#18189,
#18190,#18191,#18192,#18193,#18194,#18195,#18196,#18197,#18198,#18199,#18200,
#18201,#18202,#18203,#18204,#18205,#18206,#18207,#18208,#18209,#18210,#18211,
#18212,#18213,#18214,#18215,#18216,#18217,#18218,#18219,#18220,#18221,#18222,
#18223,#18224,#18225,#18226,#18227,#18228,#18229,#18230,#18231,#18232,#18233,
#18234,#18235,#18236,#18237,#18238,#18239,#18240,#18241,#18242,#18243,#18244,
#18245,#18246,#18247,#18248,#18249,#18250,#18251,#18252,#18253,#18254,#18255,
#18256,#18257,#18258,#18259,#18260,#18261,#18262,#18263,#18264,#18265,#18266,
#18267,#18268,#18269,#18270,#18271,#18272,#18273,#18274,#18275,#18276,#18277,
#18278,#18279,#18280,#18281,#18282,#18283,#18284,#18285,#18286,#18287,#18288,
#18289,#18290,#18291,#18292,#18293,#18294,#18295,#18296,#18297,#18298,#18299,
#18300,#18301,#18302,#18303,#18304,#18305,#18306,#18307,#18308,#18309,#18310,
#18311,#18312,#18313,#18314,#18315,#18316,#18317,#18318,#18319,#18320,#18321,
#18322,#18323,#18324,#18325,#18326,#18327,#18328,#18329,#18330,#18331,#18332,
#18333,#18334,#18335,#18336,#18337,#18338,#18339,#18340,#18341,#18342,#18343,
#18344,#18345,#18346,#18347,#18348,#18349,#18350,#18351,#18352,#18353,#18354,
#18355,#18356,#18357,#18358,#18359,#18360,#18361),.UNSPECIFIED.,.F.,.F.,
(4,3,3,3,3,3,3,3,3,3,3,3,3,3,3,3,3,3,3,3,3,3,3,3,3,3,3,3,3,3,3,3,3,3,3,
3,3,3,3,3,3,3,3,3,3,3,3,3,3,3,3,3,3,3,3,3,3,3,3,3,3,3,3,3,3,3,3,3,3,3,3,
3,3,3,3,3,3,4),(7.3930854143344,7.48366125998094,7.5789593200306,7.66991850903281,
7.7610068757006,7.85228887176144,7.86485350017956,7.95096567356472,8.0369726336412,
8.12289591723387,8.20875698581783,8.29458574146171,8.3804003602425,8.4662201866803,
8.55206456429625,8.63800018005379,8.7239878182005,8.81009865991351,8.84796018770201,
8.93408705165396,9.02010890939336,9.10604727849447,9.19192360144347,9.27776780665372,
9.36359799193743,9.44943348524598,9.53529361359441,9.62124502178279,9.70724849768268,
9.79337510940081,9.83106687522445,9.91718938261793,10.0032068469648,10.0891407914262,
10.1750126640201,10.2608523972262,10.3466780984187,10.4325091004347,10.5183647351718,
10.604311670713,10.6903106799034,10.7764328728798,10.8141735627469,10.9002949112415,
10.9863111869436,11.0722439146069,11.1581145438086,11.2439529984951,11.3297773996506,
11.4156070814413,11.5014613770805,11.5874069521317,11.6734045867373,11.7595253953439,
11.7972802502693,11.8834032732732,11.9694212484686,12.0553556984052,12.1412280704876,
12.2270682923214,12.3128944752081,12.3987259514211,12.4845820522888,12.5705294391601,
12.6565288918185,12.7426515122888,12.7803869377918,12.8655355434748,12.9505796553732,
13.0355418164815,13.1204452668709,13.20531838703,13.2901814231804,13.3750546099121,
13.4600018316116,13.5449901073353,13.6300921524228,13.6762707211195),
 .UNSPECIFIED.);
#1246=B_SPLINE_CURVE_WITH_KNOTS('',3,(#18363,#18364,#18365,#18366,#18367,
#18368,#18369,#18370,#18371,#18372,#18373,#18374,#18375,#18376,#18377,#18378,
#18379,#18380,#18381,#18382,#18383,#18384,#18385,#18386,#18387,#18388,#18389,
#18390,#18391,#18392,#18393,#18394,#18395,#18396,#18397,#18398,#18399,#18400,
#18401,#18402,#18403,#18404,#18405,#18406,#18407,#18408,#18409,#18410,#18411,
#18412,#18413,#18414,#18415,#18416,#18417,#18418,#18419,#18420,#18421,#18422,
#18423,#18424,#18425,#18426,#18427,#18428,#18429,#18430,#18431,#18432,#18433,
#18434,#18435,#18436,#18437,#18438,#18439,#18440,#18441,#18442,#18443,#18444,
#18445,#18446,#18447,#18448,#18449,#18450,#18451,#18452,#18453,#18454,#18455,
#18456,#18457,#18458,#18459,#18460,#18461,#18462,#18463,#18464,#18465,#18466,
#18467,#18468,#18469,#18470,#18471,#18472,#18473,#18474,#18475,#18476,#18477,
#18478,#18479,#18480,#18481,#18482,#18483,#18484,#18485,#18486,#18487,#18488,
#18489,#18490,#18491,#18492,#18493,#18494,#18495,#18496,#18497,#18498,#18499,
#18500,#18501,#18502,#18503,#18504,#18505,#18506,#18507,#18508,#18509,#18510,
#18511,#18512,#18513,#18514,#18515,#18516,#18517,#18518,#18519,#18520,#18521,
#18522,#18523,#18524,#18525,#18526,#18527,#18528,#18529,#18530,#18531,#18532,
#18533,#18534,#18535,#18536,#18537,#18538,#18539,#18540,#18541,#18542,#18543,
#18544,#18545,#18546,#18547,#18548,#18549,#18550,#18551,#18552,#18553,#18554,
#18555,#18556,#18557,#18558,#18559,#18560,#18561,#18562,#18563,#18564,#18565,
#18566,#18567,#18568,#18569,#18570,#18571,#18572,#18573,#18574,#18575,#18576,
#18577,#18578,#18579,#18580,#18581,#18582,#18583,#18584,#18585,#18586,#18587,
#18588,#18589,#18590,#18591),.UNSPECIFIED.,.F.,.F.,(4,3,3,3,3,3,3,3,3,3,
3,3,3,3,3,3,3,3,3,3,3,3,3,3,3,3,3,3,3,3,3,3,3,3,3,3,3,3,3,3,3,3,3,3,3,3,
3,3,3,3,3,3,3,3,3,3,3,3,3,3,3,3,3,3,3,3,3,3,3,3,3,3,3,3,3,3,4),(13.6762707213213,
13.7634936253142,13.8496159580763,13.9356332340953,14.0215669768221,14.1074386345513,
14.1932781340374,14.2791035898167,14.3649343349407,14.4507897015138,14.536736353218,
14.6227350692125,14.7088569571122,14.7466003128367,14.8327228290312,14.9187402913841,
15.0046742231037,15.0905460722461,15.1763857660457,15.2622114178869,15.3480423606136,
15.4338979261233,15.5198447777085,15.6058436943958,15.6919657824959,15.7297070003591,
15.8158294310186,15.9018468068606,15.9877806512044,16.0736524122154,16.1594920170861,
16.2453175795288,16.3311484324836,16.4170039079444,16.5029506695495,16.5889494961742,
16.675071494867,16.7128136878816,16.7989361209402,16.8849534990149,16.9708873454232,
17.0567591083282,17.1425987148302,17.2284242787398,17.3142551329948,17.4001106095863,
17.4860573720587,17.5720561994008,17.6581781985741,17.695920375404,17.7820428278235,
17.8680602255835,17.953994091976,18.0398658751388,18.1257055022317,18.2115310869334,
18.2973619621599,18.3832174598805,18.4691642436063,18.555163092302,18.6412851127977,
18.6790270629265,18.7651495041418,18.8511668905623,18.9371007454944,19.0229725170903,
19.1088121325003,19.1946377054507,19.2804685688698,19.3663240547399,19.4522708266136,
19.5382696634402,19.6243916721438,19.6621337504489,19.7659686645438,19.8686725452676,
19.9594558713002),.UNSPECIFIED.);
#1247=B_SPLINE_CURVE_WITH_KNOTS('',3,(#18593,#18594,#18595,#18596,#18597,
#18598,#18599,#18600,#18601,#18602),.UNSPECIFIED.,.F.,.F.,(4,1,1,1,1,1,
1,4),(19.9594560285009,20.6452404379713,21.6283471254938,22.6114538130162,
23.5945605005387,24.5776671880611,25.5607738755836,26.2426413356805),
 .UNSPECIFIED.);
#1248=B_SPLINE_CURVE_WITH_KNOTS('',3,(#18604,#18605,#18606,#18607,#18608,
#18609,#18610,#18611,#18612,#18613,#18614,#18615,#18616,#18617,#18618,#18619,
#18620,#18621,#18622,#18623,#18624,#18625,#18626,#18627,#18628,#18629,#18630,
#18631,#18632,#18633,#18634,#18635,#18636,#18637,#18638,#18639,#18640,#18641,
#18642,#18643,#18644,#18645,#18646,#18647,#18648,#18649,#18650,#18651,#18652,
#18653,#18654,#18655,#18656,#18657,#18658,#18659,#18660,#18661,#18662,#18663,
#18664,#18665,#18666,#18667,#18668,#18669,#18670,#18671,#18672,#18673,#18674,
#18675,#18676,#18677,#18678,#18679,#18680,#18681,#18682,#18683,#18684,#18685,
#18686,#18687,#18688,#18689,#18690,#18691,#18692,#18693,#18694,#18695,#18696,
#18697,#18698,#18699,#18700,#18701,#18702,#18703,#18704,#18705,#18706,#18707,
#18708,#18709,#18710,#18711,#18712,#18713,#18714,#18715,#18716,#18717,#18718,
#18719,#18720,#18721,#18722,#18723,#18724,#18725,#18726,#18727,#18728,#18729,
#18730,#18731,#18732,#18733,#18734,#18735,#18736,#18737,#18738,#18739,#18740,
#18741,#18742,#18743,#18744,#18745,#18746,#18747,#18748,#18749,#18750,#18751,
#18752,#18753,#18754,#18755,#18756,#18757,#18758,#18759,#18760,#18761,#18762,
#18763,#18764,#18765,#18766,#18767,#18768,#18769,#18770,#18771,#18772,#18773,
#18774,#18775,#18776,#18777,#18778,#18779,#18780,#18781,#18782,#18783,#18784,
#18785,#18786,#18787,#18788,#18789,#18790,#18791,#18792,#18793,#18794,#18795,
#18796,#18797,#18798,#18799,#18800,#18801,#18802,#18803,#18804,#18805,#18806,
#18807,#18808,#18809,#18810,#18811,#18812,#18813,#18814,#18815,#18816,#18817,
#18818,#18819,#18820,#18821,#18822,#18823,#18824,#18825,#18826,#18827,#18828,
#18829,#18830,#18831,#18832),.UNSPECIFIED.,.F.,.F.,(4,3,3,3,3,3,3,3,3,3,
3,3,3,3,3,3,3,3,3,3,3,3,3,3,3,3,3,3,3,3,3,3,3,3,3,3,3,3,3,3,3,3,3,3,3,3,
3,3,3,3,3,3,3,3,3,3,3,3,3,3,3,3,3,3,3,3,3,3,3,3,3,3,3,3,3,3,4),(26.242641499509,
26.3446941768379,26.4478838155214,26.543880563106,26.6300030833935,26.7160205490677,
26.8019544833399,26.8878263342683,26.9736660287096,27.0594916804797,27.1453226224228,
27.2311781864362,27.3171250354588,27.4031239489703,27.4892460329838,27.5269872506285,
27.6131095715702,27.6991268379978,27.7850605733534,27.8709322259246,27.9567717235579,
28.0425971795424,28.1284279269293,28.2142832978237,28.3002299569284,28.3862286820944,
28.4723505817956,28.5100939381509,28.5962163393846,28.6822336845469,28.7681674970097,
28.8540392249894,28.9398787952556,29.025704322127,29.111535138587,29.1973905766713,
29.2833372997852,29.3693360872299,29.4554580460383,29.4932006256733,29.5793236759997,
29.6653416733656,29.7512761403407,29.8371485243456,29.9229887504622,30.0088149328743,
30.0946464038566,30.1805024947355,30.2664498645006,30.3524492959591,30.4385718891503,
30.4763073131958,30.5624285594366,30.6484447521662,30.7343774160621,30.8202480006432,
30.9060864392999,30.99191084223,31.0777405435947,31.1635948766145,31.2495405156828,
31.3355382296261,31.4216591403216,31.4594140007182,31.5455366257588,31.6315541855686,
31.7174882033962,31.8033601273273,31.8891998789751,31.9750255781243,32.0608565576179,
32.1467121493448,32.2326590112296,32.3186579291363,32.4047800046536,32.4425206882407,
32.5258266428601),.UNSPECIFIED.);
#1249=B_SPLINE_CURVE_WITH_KNOTS('',3,(#18834,#18835,#18836,#18837,#18838,
#18839,#18840,#18841,#18842,#18843,#18844,#18845,#18846,#18847,#18848,#18849,
#18850,#18851,#18852,#18853,#18854,#18855,#18856,#18857,#18858,#18859,#18860,
#18861,#18862,#18863,#18864,#18865,#18866,#18867,#18868,#18869,#18870,#18871,
#18872,#18873,#18874,#18875,#18876,#18877,#18878,#18879,#18880,#18881,#18882,
#18883,#18884,#18885,#18886,#18887,#18888,#18889,#18890,#18891,#18892,#18893,
#18894,#18895,#18896,#18897,#18898,#18899,#18900,#18901,#18902,#18903,#18904,
#18905,#18906,#18907,#18908,#18909,#18910,#18911,#18912,#18913,#18914,#18915,
#18916,#18917,#18918,#18919,#18920,#18921,#18922,#18923,#18924,#18925,#18926,
#18927,#18928,#18929,#18930,#18931,#18932,#18933,#18934,#18935,#18936,#18937,
#18938,#18939,#18940,#18941,#18942,#18943,#18944,#18945,#18946,#18947,#18948,
#18949,#18950,#18951,#18952,#18953,#18954,#18955,#18956,#18957,#18958,#18959,
#18960,#18961,#18962,#18963,#18964,#18965,#18966,#18967,#18968,#18969,#18970,
#18971,#18972,#18973,#18974,#18975,#18976,#18977,#18978,#18979,#18980,#18981,
#18982,#18983,#18984,#18985,#18986,#18987,#18988,#18989,#18990,#18991,#18992,
#18993,#18994,#18995,#18996,#18997,#18998,#18999,#19000,#19001,#19002,#19003,
#19004,#19005,#19006,#19007,#19008,#19009,#19010,#19011,#19012,#19013,#19014,
#19015,#19016,#19017,#19018,#19019,#19020,#19021,#19022,#19023,#19024,#19025,
#19026,#19027,#19028,#19029,#19030,#19031,#19032,#19033,#19034,#19035,#19036,
#19037,#19038,#19039,#19040,#19041,#19042,#19043,#19044,#19045,#19046,#19047,
#19048,#19049,#19050,#19051,#19052,#19053,#19054,#19055,#19056,#19057,#19058,
#19059,#19060,#19061,#19062,#19063,#19064,#19065),.UNSPECIFIED.,.F.,.F.,
(4,3,3,3,3,3,3,3,3,3,3,3,3,3,3,3,3,3,3,3,3,3,3,3,3,3,3,3,3,3,3,3,3,3,3,
3,3,3,3,3,3,3,3,3,3,3,3,3,3,3,3,3,3,3,3,3,3,3,3,3,3,3,3,3,3,3,3,3,3,3,3,
3,3,3,3,3,3,4),(32.5258266430566,32.6109724346887,32.6960210961378,32.7809951098591,
32.8659214354213,32.9508241749927,33.0357235442058,33.1206397523944,33.2056408545587,
33.2906886895505,33.3758609577714,33.4256273757631,33.5117386977598,33.5977449669701,
33.6836677195876,33.7695284165969,33.8553570387069,33.9411716721801,34.0269916614943,
34.1128363502318,34.1987724988946,34.2847607974944,34.3708724891257,34.4087340632856,
34.4948626039088,34.5808860086697,34.6668257949821,34.7527034050599,34.8385487008752,
34.9243798543078,35.0102161927437,35.0960770425472,35.1820289830922,35.2680328840028,
35.3541597537952,35.391840750808,35.4779957931001,35.564045956927,35.6500127247878,
35.7359175043445,35.8217901462905,35.90764874693,35.9935126031944,36.0794010110302,
36.1653804190781,36.2514117725677,36.3375658326432,36.3749474383305,36.4609709985879,
36.5468894484378,36.6327244251594,36.7184974902785,36.8042390095103,36.8899668929997,
36.9757005755,37.0614594912268,37.1473111312689,37.2332155266954,37.3192449713843,
37.3580541258529,37.4442653932351,37.5303710041113,37.616392385932,37.7023508908437,
37.7882757520974,37.8741856189158,37.9600997363509,38.0460373477549,38.132064110626,
38.2181418243531,38.3043403342073,38.3411608133753,38.4323669275132,38.5265281831132,
38.6173539858577,38.7080464538249,38.7985713335135,38.8090119499132),
 .UNSPECIFIED.);
#1250=B_SPLINE_CURVE_WITH_KNOTS('',3,(#19067,#19068,#19069,#19070,#19071,
#19072,#19073,#19074,#19075,#19076,#19077,#19078,#19079,#19080,#19081,#19082,
#19083,#19084,#19085,#19086,#19087,#19088,#19089,#19090,#19091,#19092,#19093,
#19094,#19095,#19096,#19097,#19098,#19099,#19100,#19101,#19102,#19103,#19104,
#19105,#19106,#19107,#19108,#19109,#19110,#19111,#19112,#19113,#19114,#19115,
#19116,#19117,#19118),.UNSPECIFIED.,.F.,.F.,(4,3,3,3,3,3,3,3,3,3,3,3,3,
3,3,3,3,4),(38.8090119500397,38.8986001599551,38.9882861023177,39.0781574059986,
39.1681251672574,39.2582803096457,39.3242675008978,39.4085522045926,39.4927322947236,
39.5768309331739,39.6608734290088,39.7448872573002,39.8288931818936,39.9129119571121,
39.9970107280833,40.0811536853461,40.1654173637519,40.2123859659494),
 .UNSPECIFIED.);
#1251=B_SPLINE_CURVE_WITH_KNOTS('',3,(#19122,#19123,#19124,#19125),
 .UNSPECIFIED.,.F.,.F.,(4,4),(-42.2735875634651,-41.7920059872209),
 .UNSPECIFIED.);
#1252=B_SPLINE_CURVE_WITH_KNOTS('',3,(#19127,#19128,#19129,#19130,#19131,
#19132,#19133,#19134,#19135,#19136,#19137,#19138,#19139,#19140,#19141,#19142,
#19143,#19144,#19145,#19146,#19147,#19148,#19149,#19150,#19151,#19152,#19153,
#19154,#19155,#19156,#19157,#19158,#19159,#19160,#19161,#19162,#19163,#19164,
#19165,#19166,#19167,#19168,#19169,#19170,#19171,#19172,#19173,#19174,#19175,
#19176,#19177,#19178,#19179,#19180,#19181,#19182,#19183,#19184,#19185,#19186,
#19187,#19188,#19189,#19190,#19191,#19192,#19193,#19194,#19195,#19196,#19197,
#19198,#19199,#19200,#19201,#19202,#19203,#19204,#19205,#19206,#19207,#19208,
#19209,#19210,#19211,#19212,#19213,#19214,#19215,#19216,#19217,#19218,#19219,
#19220,#19221,#19222,#19223,#19224,#19225,#19226,#19227,#19228,#19229,#19230,
#19231,#19232,#19233,#19234,#19235,#19236,#19237,#19238,#19239,#19240,#19241,
#19242,#19243,#19244,#19245,#19246,#19247,#19248,#19249,#19250,#19251,#19252,
#19253,#19254,#19255,#19256,#19257,#19258,#19259,#19260,#19261,#19262,#19263,
#19264,#19265,#19266,#19267,#19268,#19269,#19270,#19271,#19272,#19273,#19274,
#19275,#19276,#19277,#19278,#19279,#19280,#19281,#19282,#19283,#19284,#19285,
#19286,#19287,#19288,#19289,#19290,#19291,#19292,#19293,#19294,#19295,#19296,
#19297,#19298,#19299,#19300,#19301,#19302,#19303,#19304,#19305,#19306,#19307,
#19308,#19309,#19310,#19311,#19312,#19313,#19314,#19315,#19316,#19317,#19318,
#19319,#19320,#19321,#19322,#19323,#19324,#19325,#19326,#19327,#19328,#19329,
#19330,#19331,#19332,#19333,#19334,#19335,#19336,#19337,#19338,#19339,#19340,
#19341,#19342,#19343,#19344,#19345,#19346,#19347,#19348,#19349,#19350,#19351,
#19352,#19353,#19354,#19355,#19356,#19357,#19358,#19359,#19360,#19361),
 .UNSPECIFIED.,.F.,.F.,(4,3,3,3,3,3,3,3,3,3,3,3,3,3,3,3,3,3,3,3,3,3,3,3,
3,3,3,3,3,3,3,3,3,3,3,3,3,3,3,3,3,3,3,3,3,3,3,3,3,3,3,3,3,3,3,3,3,3,3,3,
3,3,3,3,3,3,3,3,3,3,3,3,3,3,3,3,3,3,4),(-41.79200593275,-41.7820342197039,
-41.6950743300943,-41.6081223321859,-41.5211282447415,-41.4341127720792,
-41.3470146427639,-41.2904808759427,-41.20336832383,-41.1163307621064,-41.0293484847566,
-40.9391016977146,-40.852152878242,-40.7651965641577,-40.6782149646209,
-40.5911902746634,-40.5040544223173,-40.4168531658136,-40.329521224308,
-40.3073741884203,-40.2220564467519,-40.1368545416153,-40.0517460197423,
-39.9667085240719,-39.8817137263903,-39.7967393958665,-39.7117654161815,
-39.6267716751265,-39.5416895547738,-39.4565583215444,-39.3713009176492,
-39.3242675008978,-39.2379295253732,-39.1516949070862,-39.0655424093964,
-38.9749947098938,-38.8889356671652,-38.8028892415144,-38.7168363522496,
-38.6307579188814,-38.5445890611926,-38.4583677184446,-38.3720269721772,
-38.3411608133754,-38.2549622066264,-38.1688668587652,-38.0828533517434,
-37.9969003407262,-37.9109774199415,-37.8250672796277,-37.7391506754001,
-37.6532083630363,-37.567173590932,-37.4810859630649,-37.3948747178714,
-37.3580541258529,-37.2720238464053,-37.1860999512967,-37.1002607981332,
-37.0144848214179,-36.9287422802383,-36.8430145508322,-36.7572821980678,
-36.6715257881743,-36.5856784152043,-36.4997792987108,-36.4137566395602,
-36.3749474383305,-36.2899292270807,-36.2050152151128,-36.1179908982539,
-36.0332183657195,-35.9484752386565,-35.8637411740814,-35.7750110506216,
-35.6901947599964,-35.6053351568716,-35.5203766098291,-35.5088206802422),
 .UNSPECIFIED.);
#1253=B_SPLINE_CURVE_WITH_KNOTS('',3,(#19363,#19364,#19365,#19366,#19367,
#19368,#19369,#19370,#19371,#19372,#19373,#19374,#19375,#19376,#19377,#19378,
#19379,#19380,#19381,#19382,#19383,#19384,#19385,#19386,#19387,#19388,#19389,
#19390,#19391,#19392,#19393,#19394,#19395,#19396,#19397,#19398,#19399,#19400,
#19401,#19402,#19403,#19404,#19405,#19406,#19407,#19408,#19409,#19410,#19411,
#19412,#19413,#19414,#19415,#19416,#19417,#19418,#19419,#19420,#19421,#19422,
#19423,#19424,#19425,#19426,#19427,#19428,#19429,#19430,#19431,#19432,#19433,
#19434,#19435,#19436,#19437,#19438,#19439,#19440,#19441,#19442,#19443,#19444,
#19445,#19446,#19447,#19448,#19449,#19450,#19451,#19452,#19453,#19454,#19455,
#19456,#19457,#19458,#19459,#19460,#19461,#19462,#19463,#19464,#19465,#19466,
#19467,#19468,#19469,#19470,#19471,#19472,#19473,#19474,#19475,#19476,#19477,
#19478,#19479,#19480,#19481,#19482,#19483,#19484,#19485,#19486,#19487,#19488,
#19489,#19490,#19491,#19492,#19493,#19494,#19495,#19496,#19497,#19498,#19499,
#19500,#19501,#19502,#19503,#19504,#19505,#19506,#19507,#19508,#19509,#19510,
#19511,#19512,#19513,#19514,#19515,#19516,#19517,#19518,#19519,#19520,#19521,
#19522,#19523,#19524,#19525,#19526,#19527,#19528,#19529,#19530,#19531,#19532,
#19533,#19534,#19535,#19536,#19537,#19538,#19539,#19540,#19541,#19542,#19543,
#19544,#19545,#19546,#19547,#19548,#19549,#19550,#19551,#19552,#19553,#19554,
#19555,#19556,#19557,#19558,#19559,#19560,#19561,#19562,#19563,#19564,#19565,
#19566,#19567,#19568,#19569,#19570,#19571,#19572,#19573,#19574,#19575,#19576,
#19577,#19578,#19579,#19580,#19581,#19582,#19583,#19584,#19585,#19586,#19587,
#19588,#19589,#19590,#19591),.UNSPECIFIED.,.F.,.F.,(4,3,3,3,3,3,3,3,3,3,
3,3,3,3,3,3,3,3,3,3,3,3,3,3,3,3,3,3,3,3,3,3,3,3,3,3,3,3,3,3,3,3,3,3,3,3,
3,3,3,3,3,3,3,3,3,3,3,3,3,3,3,3,3,3,3,3,3,3,3,3,3,3,3,3,3,3,4),(-35.5088206800413,
-35.391840750808,-35.3057134673612,-35.2196910812655,-35.1337520760534,
-35.0478750102457,-34.9620299050909,-34.8761987221089,-34.7903621339832,
-34.7045008142665,-34.6185480744502,-34.5325431848047,-34.4464150450444,
-34.4087340632856,-34.322621901095,-34.2366149523578,-34.1506916802349,
-34.0648306232373,-33.9790018793112,-33.8931872723268,-33.8073674577515,
-33.7215230920524,-33.6355874882297,-33.5495998620446,-33.4634890322309,
-33.4256273757631,-33.3395005067057,-33.2534786438155,-33.1675402695245,
-33.0816639413529,-32.9958197308907,-32.9099895403383,-32.8241540417499,
-32.7382939081162,-32.6523424946626,-32.5663390135018,-32.480212396575,
-32.4425206882407,-32.3563981804201,-32.2703807156258,-32.1844467706973,
-32.0985748976172,-32.0127351638982,-31.9269094621762,-31.8410784596148,
-31.7552228243167,-31.6692758881938,-31.5832768784092,-31.4971546848244,
-31.4594140007183,-31.3732926541172,-31.2872763803364,-31.20134365462,-31.1154730273881,
-31.0296345746987,-30.9438101755565,-30.8579804957934,-30.7721262021939,
-30.6861806291898,-30.6001829966384,-30.514062190079,-30.4763073131958,
-30.3901842891515,-30.3041663129045,-30.2182318619066,-30.1323594887544,
-30.046519265842,-29.9606930818716,-29.8748616045711,-29.7890055026128,
-29.7030581146527,-29.6170586609049,-29.5309360393539,-29.4932006256734,
-29.3853784705262,-29.2791332454367,-29.2256353730422),.UNSPECIFIED.);
#1254=B_SPLINE_CURVE_WITH_KNOTS('',3,(#19593,#19594,#19595,#19596,#19597,
#19598,#19599,#19600,#19601,#19602,#19603,#19604,#19605,#19606,#19607,#19608,
#19609,#19610,#19611,#19612,#19613,#19614,#19615,#19616,#19617,#19618,#19619,
#19620,#19621,#19622,#19623,#19624,#19625,#19626,#19627,#19628,#19629,#19630,
#19631,#19632,#19633,#19634,#19635,#19636,#19637,#19638,#19639,#19640,#19641,
#19642,#19643,#19644,#19645,#19646,#19647,#19648,#19649,#19650,#19651,#19652,
#19653,#19654,#19655,#19656,#19657,#19658,#19659,#19660,#19661,#19662,#19663,
#19664,#19665,#19666,#19667,#19668,#19669,#19670,#19671,#19672,#19673,#19674,
#19675,#19676,#19677,#19678,#19679,#19680,#19681,#19682,#19683,#19684,#19685,
#19686,#19687,#19688,#19689,#19690,#19691,#19692,#19693,#19694,#19695,#19696,
#19697,#19698,#19699,#19700,#19701,#19702,#19703,#19704,#19705,#19706,#19707,
#19708,#19709,#19710,#19711,#19712,#19713,#19714,#19715,#19716,#19717,#19718,
#19719,#19720,#19721,#19722,#19723,#19724,#19725,#19726,#19727,#19728,#19729,
#19730,#19731,#19732,#19733,#19734,#19735,#19736,#19737,#19738,#19739,#19740,
#19741,#19742,#19743,#19744,#19745,#19746,#19747,#19748,#19749,#19750,#19751,
#19752,#19753,#19754,#19755,#19756,#19757,#19758,#19759,#19760,#19761,#19762,
#19763,#19764,#19765,#19766,#19767,#19768,#19769,#19770,#19771,#19772,#19773,
#19774,#19775,#19776,#19777,#19778,#19779,#19780,#19781,#19782,#19783,#19784,
#19785,#19786,#19787,#19788,#19789,#19790,#19791,#19792,#19793,#19794,#19795,
#19796,#19797,#19798,#19799,#19800,#19801,#19802,#19803,#19804,#19805,#19806,
#19807,#19808,#19809,#19810,#19811,#19812,#19813,#19814,#19815,#19816,#19817,
#19818,#19819,#19820,#19821,#19822,#19823,#19824),.UNSPECIFIED.,.F.,.F.,
(4,3,3,3,3,3,3,3,3,3,3,3,3,3,3,3,3,3,3,3,3,3,3,3,3,3,3,3,3,3,3,3,3,3,3,
3,3,3,3,3,3,3,3,3,3,3,3,3,3,3,3,3,3,3,3,3,3,3,3,3,3,3,3,3,3,3,3,3,3,3,3,
3,3,3,3,3,3,4),(-29.2256353728617,-29.1361926935229,-29.0511260979808,-28.9660762328229,
-28.88102302201,-28.7959463909764,-28.7107799985853,-28.6255612560834,-28.5402214425233,
-28.5100939381509,-28.4239716056522,-28.3379543299007,-28.2520205874456,
-28.1661489299919,-28.0803094307853,-27.9944839752883,-27.9086532304487,
-27.822797864162,-27.7368512127461,-27.6508524970411,-27.5647306094304,
-27.5269872506285,-27.4408647342574,-27.3548472717257,-27.2689133398253,
-27.1830414905009,-27.0972017965172,-27.0113761444908,-26.9255452015783,
-26.8396896358817,-26.7537427841098,-26.6677438672355,-26.5816217789496,
-26.543880563106,-26.4577581324764,-26.3717407566645,-26.2858069123508,
-26.1999351513698,-26.1140955465289,-26.0282699841158,-25.9424391311903,
-25.856583655759,-25.7706368941827,-25.6846380675869,-25.598516068922,-25.5607738755836,
-25.4746514425571,-25.3886340645148,-25.3027002181393,-25.216828455268,
-25.1309888488002,-25.0451632849252,-24.9593324307051,-24.8734769541487,
-24.7875301917118,-24.7015313644052,-24.6154093652677,-24.5776671880611,
-24.4915447356144,-24.4055273378264,-24.3195934714057,-24.2337216882146,
-24.1478820610932,-24.0620564763624,-23.9762256011071,-23.8903701033575,
-23.8044233196025,-23.7184244708774,-23.6323024503526,-23.5945605005387,
-23.5084383448351,-23.4224191446739,-23.3364834599017,-23.2506119149563,
-23.1647805520879,-23.0789734309571,-22.9931527448939,-22.9424500656821),
 .UNSPECIFIED.);
#1255=B_SPLINE_CURVE_WITH_KNOTS('',3,(#19826,#19827,#19828,#19829,#19830,
#19831,#19832,#19833,#19834,#19835,#19836,#19837,#19838,#19839,#19840,#19841,
#19842,#19843,#19844,#19845,#19846,#19847,#19848,#19849,#19850,#19851,#19852,
#19853,#19854,#19855,#19856,#19857,#19858,#19859,#19860,#19861,#19862,#19863,
#19864,#19865,#19866,#19867,#19868,#19869,#19870,#19871,#19872,#19873,#19874,
#19875,#19876,#19877,#19878,#19879,#19880,#19881,#19882,#19883,#19884,#19885,
#19886,#19887,#19888,#19889,#19890,#19891,#19892,#19893,#19894,#19895,#19896,
#19897,#19898,#19899,#19900,#19901,#19902,#19903,#19904,#19905,#19906,#19907,
#19908,#19909,#19910,#19911,#19912,#19913,#19914,#19915,#19916,#19917,#19918,
#19919,#19920,#19921,#19922,#19923,#19924,#19925,#19926,#19927,#19928,#19929,
#19930,#19931,#19932,#19933,#19934,#19935,#19936,#19937,#19938,#19939,#19940,
#19941,#19942,#19943,#19944,#19945,#19946,#19947,#19948,#19949,#19950,#19951,
#19952,#19953,#19954,#19955,#19956,#19957,#19958,#19959,#19960,#19961,#19962,
#19963,#19964,#19965,#19966,#19967,#19968,#19969,#19970,#19971,#19972,#19973,
#19974,#19975,#19976,#19977,#19978,#19979,#19980,#19981,#19982,#19983,#19984,
#19985,#19986,#19987,#19988,#19989,#19990,#19991,#19992,#19993,#19994,#19995,
#19996,#19997,#19998,#19999,#20000,#20001,#20002,#20003,#20004,#20005,#20006,
#20007,#20008,#20009,#20010,#20011,#20012,#20013,#20014,#20015,#20016,#20017,
#20018,#20019,#20020,#20021,#20022,#20023,#20024,#20025,#20026,#20027,#20028,
#20029,#20030,#20031,#20032,#20033,#20034,#20035,#20036,#20037,#20038,#20039,
#20040,#20041,#20042,#20043,#20044,#20045,#20046,#20047,#20048,#20049,#20050,
#20051,#20052,#20053,#20054,#20055,#20056,#20057),.UNSPECIFIED.,.F.,.F.,
(4,3,3,3,3,3,3,3,3,3,3,3,3,3,3,3,3,3,3,3,3,3,3,3,3,3,3,3,3,3,3,3,3,3,3,
3,3,3,3,3,3,3,3,3,3,3,3,3,3,3,3,3,3,3,3,3,3,3,3,3,3,3,3,3,3,3,3,3,3,3,3,
3,3,3,3,3,3,4),(-22.9424500654921,-22.8432492269214,-22.743518032141,-22.6431790088504,
-22.6114538130162,-22.525331370706,-22.4393139831972,-22.3533801271849,
-22.2675083545179,-22.1816687380548,-22.0958431640629,-22.0100122996148,
-21.92415681273,-21.838210039868,-21.7522112020671,-21.6660891924192,-21.6283471254938,
-21.5422246798375,-21.4562072889451,-21.370273429516,-21.2844016534033,
-21.1985620334634,-21.1127364559765,-21.0269055880192,-20.9410500976143,
-20.855103321235,-20.7691044799135,-20.6829824667704,-20.6452404379714,
-20.5591179957949,-20.4731006083946,-20.3871667524656,-20.3012949798572,
-20.215455363415,-20.1296297894206,-20.0437989249469,-19.9579434380131,
-19.8719966650674,-19.7859978271626,-19.6998758173811,-19.6621337504489,
-19.5760113092192,-19.4899939227884,-19.4040600678502,-19.3181882962524,
-19.2323486808462,-19.1465231079036,-19.0606922444959,-18.9748367586413,
-18.8888899867884,-18.8028911499858,-18.716769141311,-18.6790270629265,
-18.5929046099203,-18.5068872116786,-18.4209533449092,-18.3350815614742,
-18.2492419342651,-18.1634163495443,-18.0775854743959,-17.9917299768508,
-17.905783193446,-17.8197843451551,-17.733662325189,-17.695920375404,-17.609797943694,
-17.5237805667203,-17.4378467211662,-17.3519749588694,-17.2661353526079,
-17.18030978871,-17.0944789342378,-17.0086234572,-16.9226766939388,-16.8366778656107,
-16.7505558651585,-16.7128136878816,-16.6592647585025),.UNSPECIFIED.);
#1256=B_SPLINE_CURVE_WITH_KNOTS('',3,(#20059,#20060,#20061,#20062,#20063,
#20064,#20065,#20066,#20067,#20068,#20069,#20070,#20071,#20072,#20073,#20074,
#20075,#20076,#20077,#20078,#20079,#20080,#20081,#20082,#20083,#20084,#20085,
#20086,#20087,#20088,#20089,#20090,#20091,#20092,#20093,#20094,#20095,#20096,
#20097,#20098,#20099,#20100,#20101,#20102,#20103,#20104,#20105,#20106,#20107,
#20108,#20109,#20110,#20111,#20112,#20113,#20114,#20115,#20116,#20117,#20118,
#20119,#20120,#20121,#20122,#20123,#20124,#20125,#20126,#20127,#20128,#20129,
#20130,#20131,#20132,#20133,#20134,#20135,#20136,#20137,#20138,#20139,#20140,
#20141,#20142,#20143,#20144,#20145,#20146,#20147,#20148,#20149,#20150,#20151,
#20152,#20153,#20154,#20155,#20156,#20157,#20158,#20159,#20160,#20161,#20162,
#20163,#20164,#20165,#20166,#20167,#20168,#20169,#20170,#20171,#20172,#20173,
#20174,#20175,#20176,#20177,#20178,#20179,#20180,#20181,#20182,#20183,#20184,
#20185,#20186,#20187,#20188,#20189,#20190,#20191,#20192,#20193,#20194,#20195,
#20196,#20197,#20198,#20199,#20200,#20201,#20202,#20203,#20204,#20205,#20206,
#20207,#20208,#20209,#20210,#20211,#20212,#20213,#20214,#20215,#20216,#20217,
#20218,#20219,#20220,#20221,#20222,#20223,#20224,#20225,#20226,#20227,#20228,
#20229,#20230,#20231,#20232,#20233,#20234,#20235,#20236,#20237,#20238,#20239,
#20240,#20241,#20242,#20243,#20244,#20245,#20246,#20247,#20248,#20249,#20250,
#20251,#20252,#20253,#20254,#20255,#20256,#20257,#20258,#20259,#20260,#20261,
#20262,#20263,#20264,#20265,#20266,#20267,#20268,#20269,#20270,#20271,#20272,
#20273,#20274,#20275,#20276,#20277,#20278,#20279,#20280,#20281,#20282,#20283,
#20284,#20285,#20286,#20287),.UNSPECIFIED.,.F.,.F.,(4,3,3,3,3,3,3,3,3,3,
3,3,3,3,3,3,3,3,3,3,3,3,3,3,3,3,3,3,3,3,3,3,3,3,3,3,3,3,3,3,3,3,3,3,3,3,
3,3,3,3,3,3,3,3,3,3,3,3,3,3,3,3,3,3,3,3,3,3,3,3,3,3,3,3,3,3,4),(-16.6592647583472,
-16.5738430149373,-16.4885227334712,-16.4032816523275,-16.3180945864984,
-16.2329356250115,-16.1477847574117,-16.0626219831902,-15.9773761668429,
-15.8920884458071,-15.8066680671297,-15.7297070003591,-15.6435844798867,
-15.5575670140271,-15.471633079569,-15.3857612284546,-15.2999215338279,
-15.2140958818728,-15.1282649397453,-15.0424093755484,-14.9564625263443,
-14.8704636126523,-14.7843415284612,-14.7466003128367,-14.6604779921827,
-14.5744607260426,-14.4885269909739,-14.4026553386888,-14.3168158413389,
-14.2309903856361,-14.145159638529,-14.0593042679126,-13.9733576090808,
-13.8873588841852,-13.8012369847486,-13.7634936253142,-13.6773712241262,
-13.5913538790123,-13.5054200666001,-13.4195483386733,-13.3337087684636,
-13.2478832416506,-13.162052425251,-13.0761969872289,-12.99025026418,-12.9042514768019,
-12.8181295180617,-12.7803869377918,-12.6942638863894,-12.6082458879433,
-12.5223114198845,-12.4364390347946,-12.3505988075939,-12.2647726240988,
-12.1789411520357,-12.0930850600792,-12.0071376892478,-11.9211382567276,
-11.8350156624911,-11.7972802502693,-11.7111590060667,-11.6251428153763,
-11.5392101535174,-11.4533395709698,-11.367501134333,-11.2816767334135,
-11.195847034049,-11.1099927030158,-11.0240470659038,-10.9380493539021,
-10.851928445109,-10.8141735627469,-10.7213212232863,-10.6287599994176,
-10.5363786705168,-10.4442738471014,-10.3760794514417),.UNSPECIFIED.);
#1257=B_SPLINE_CURVE_WITH_KNOTS('',3,(#20288,#20289,#20290,#20291,#20292,
#20293,#20294,#20295,#20296,#20297,#20298,#20299,#20300,#20301,#20302,#20303,
#20304,#20305,#20306,#20307,#20308,#20309,#20310,#20311,#20312,#20313,#20314,
#20315,#20316,#20317,#20318,#20319,#20320,#20321,#20322,#20323,#20324,#20325,
#20326,#20327,#20328,#20329,#20330,#20331,#20332,#20333,#20334,#20335,#20336,
#20337,#20338,#20339,#20340,#20341,#20342,#20343,#20344,#20345,#20346,#20347,
#20348,#20349,#20350,#20351,#20352,#20353,#20354,#20355,#20356,#20357,#20358,
#20359,#20360,#20361,#20362,#20363,#20364,#20365,#20366,#20367,#20368,#20369,
#20370,#20371,#20372,#20373,#20374,#20375,#20376,#20377,#20378,#20379,#20380,
#20381,#20382,#20383,#20384,#20385,#20386,#20387,#20388,#20389,#20390,#20391,
#20392,#20393,#20394,#20395,#20396,#20397,#20398,#20399,#20400,#20401,#20402,
#20403,#20404,#20405,#20406,#20407,#20408,#20409,#20410,#20411,#20412,#20413,
#20414,#20415,#20416,#20417,#20418,#20419,#20420,#20421,#20422,#20423,#20424,
#20425,#20426,#20427,#20428,#20429,#20430,#20431,#20432,#20433,#20434,#20435,
#20436,#20437,#20438,#20439,#20440,#20441,#20442,#20443,#20444,#20445,#20446,
#20447,#20448,#20449,#20450,#20451,#20452,#20453,#20454,#20455,#20456,#20457,
#20458,#20459,#20460,#20461,#20462,#20463,#20464,#20465,#20466,#20467,#20468,
#20469,#20470,#20471,#20472,#20473,#20474,#20475,#20476,#20477,#20478,#20479,
#20480,#20481,#20482,#20483,#20484,#20485,#20486,#20487,#20488,#20489,#20490,
#20491,#20492,#20493,#20494,#20495,#20496,#20497,#20498,#20499,#20500,#20501,
#20502,#20503,#20504,#20505,#20506,#20507,#20508,#20509,#20510,#20511,#20512,
#20513,#20514,#20515,#20516,#20517,#20518,#20519),.UNSPECIFIED.,.F.,.F.,
(4,3,3,3,3,3,3,3,3,3,3,3,3,3,3,3,3,3,3,3,3,3,3,3,3,3,3,3,3,3,3,3,3,3,3,
3,3,3,3,3,3,3,3,3,3,3,3,3,3,3,3,3,3,3,3,3,3,3,3,3,3,3,3,3,3,3,3,3,3,3,3,
3,3,3,3,3,3,4),(-10.3760794513229,-10.2880145295059,-10.1998923966073,-10.1076860162616,
-10.0193432467952,-9.93091491142239,-9.84233871959151,-9.83106687522445,
-9.74493984606962,-9.65891785327206,-9.57297937914544,-9.48710298111784,
-9.40125874556535,-9.31542855780065,-9.22959308987034,-9.14373301477612,
-9.05778170156634,-8.97177834463815,-8.88565188756136,-8.84796018770201,
-8.76184887755315,-8.67584262021201,-8.58991987947197,-8.50405919433414,
-8.41823058404444,-8.33241596235659,-8.24659598478001,-8.16075130772062,
-8.07481517058394,-7.98882688343906,-7.90271520305529,-7.86485350017956,
-7.77872495169094,-7.69270153910995,-7.60676174503123,-7.52088412724879,
-7.4350388238479,-7.34920766290605,-7.26337131704426,-7.17751045990625,
-7.09155851220294,-7.00555460422482,-6.91942772756424,-6.88174681265712,
-6.79559175471683,-6.70954157508135,-6.62357479127157,-6.53766999564482,
-6.45179733750838,-6.36593872060825,-6.2800748480303,-6.19418642384597,
-6.10820699948371,-6.02217562967714,-5.936021553422,-5.89864012513467,-5.8126166075868,
-5.72669820066755,-5.64086326704925,-5.55509024515823,-5.46934876919013,
-5.38362092897648,-5.2978872897214,-5.21212841716633,-5.12627681995917,
-5.04037246723583,-4.95434306467912,-4.91553343761223,-4.83052634717772,
-4.74562463000397,-4.66081596132364,-4.57605895127486,-4.49133320716937,
-4.40661836557381,-4.32185837814588,-4.23707535482957,-4.15219887483577,
-4.09289414427482),.UNSPECIFIED.);
#1258=B_SPLINE_CURVE_WITH_KNOTS('',3,(#20522,#20523,#20524,#20525,#20526,
#20527,#20528,#20529,#20530,#20531,#20532,#20533,#20534,#20535,#20536,#20537,
#20538,#20539,#20540,#20541,#20542,#20543,#20544,#20545,#20546,#20547,#20548,
#20549),.UNSPECIFIED.,.F.,.F.,(4,3,3,3,3,3,3,3,3,4),(46.3346777312564,46.4243645657982,
46.5140283060791,46.6036909880087,46.6933746409546,46.7831528323428,46.8729842216755,
46.9629495988034,47.0069098746136,47.1238898038469),.UNSPECIFIED.);
#1259=B_SPLINE_CURVE_WITH_KNOTS('',3,(#20551,#20552,#20553,#20554,#20555,
#20556,#20557,#20558,#20559,#20560,#20561,#20562,#20563,#20564,#20565,#20566,
#20567,#20568,#20569,#20570,#20571,#20572,#20573,#20574,#20575,#20576,#20577,
#20578,#20579,#20580,#20581,#20582,#20583,#20584,#20585,#20586,#20587,#20588,
#20589,#20590,#20591,#20592,#20593,#20594,#20595,#20596,#20597,#20598,#20599,
#20600,#20601,#20602,#20603,#20604,#20605,#20606,#20607,#20608,#20609,#20610,
#20611,#20612,#20613,#20614,#20615,#20616,#20617,#20618,#20619,#20620,#20621,
#20622,#20623,#20624,#20625,#20626,#20627,#20628,#20629,#20630,#20631,#20632,
#20633,#20634,#20635,#20636,#20637,#20638,#20639,#20640,#20641,#20642,#20643,
#20644,#20645,#20646,#20647,#20648,#20649,#20650,#20651,#20652,#20653,#20654,
#20655,#20656,#20657,#20658,#20659,#20660,#20661,#20662,#20663,#20664,#20665,
#20666,#20667,#20668,#20669,#20670,#20671,#20672,#20673,#20674,#20675,#20676,
#20677,#20678,#20679,#20680,#20681,#20682,#20683,#20684,#20685,#20686,#20687,
#20688,#20689,#20690,#20691,#20692,#20693,#20694,#20695,#20696,#20697,#20698,
#20699,#20700,#20701,#20702,#20703,#20704,#20705,#20706,#20707,#20708,#20709,
#20710),.UNSPECIFIED.,.F.,.F.,(4,3,3,3,3,3,3,3,3,3,3,3,3,3,3,3,3,3,3,3,
3,3,3,3,3,3,3,3,3,3,3,3,3,3,3,3,3,3,3,3,3,3,3,3,3,3,3,3,3,3,3,3,3,4),(47.1238898040851,
47.212634310815,47.3012804954036,47.3898536706167,47.4783881657889,47.5669071783758,
47.6554338879542,47.7440444285322,47.8326984185048,47.9214901286793,47.9900165621361,
48.079878475582,48.1696262134622,48.2592844383872,48.3488804771275,48.4384437308739,
48.5279963661167,48.6175605357571,48.707215576596,48.7969155021056,48.8867636103351,
48.9731232496585,49.0631813344679,49.1531246430108,49.2429775986181,49.3327663197129,
49.4225209467818,49.5122634308969,49.6020157083635,49.6918549669428,49.7817372622351,
49.8717626820065,49.956229937181,50.0464205997571,50.1364989391249,50.2264891614412,
50.3164179156243,50.4063141963529,50.4961997669363,50.5860963769902,50.6760809951302,
50.766109414171,50.8562806870504,50.9393366247034,51.0273822113533,51.1153142003882,
51.2043285952813,51.2921153635596,51.379874703757,51.4676302816496,51.5575800511205,
51.6454454055357,51.7364373825343,51.8274293595329),.UNSPECIFIED.);
#1260=B_SPLINE_CURVE_WITH_KNOTS('',3,(#20714,#20715,#20716,#20717,#20718,
#20719,#20720,#20721,#20722,#20723,#20724,#20725,#20726,#20727,#20728,#20729,
#20730,#20731,#20732,#20733,#20734,#20735,#20736,#20737,#20738,#20739,#20740,
#20741,#20742,#20743,#20744,#20745,#20746,#20747,#20748,#20749,#20750,#20751,
#20752,#20753,#20754,#20755,#20756,#20757,#20758,#20759,#20760,#20761,#20762,
#20763,#20764,#20765,#20766,#20767,#20768,#20769,#20770,#20771,#20772,#20773,
#20774,#20775,#20776,#20777,#20778,#20779,#20780,#20781,#20782,#20783,#20784,
#20785,#20786,#20787,#20788,#20789,#20790,#20791,#20792,#20793,#20794,#20795,
#20796,#20797,#20798,#20799,#20800,#20801,#20802,#20803,#20804,#20805,#20806,
#20807,#20808,#20809,#20810,#20811,#20812,#20813,#20814,#20815,#20816,#20817,
#20818,#20819,#20820,#20821,#20822,#20823,#20824,#20825,#20826,#20827,#20828,
#20829,#20830,#20831),.UNSPECIFIED.,.F.,.F.,(4,3,3,3,3,3,3,3,3,3,3,3,3,
3,3,3,3,3,3,3,3,3,3,3,3,3,3,3,3,3,3,3,3,3,3,3,3,3,3,4),(47.1238898038469,
47.2174754673338,47.3111680100548,47.4050579725487,47.4990543518043,47.5932435711771,
47.639145354705,47.7282111079036,47.8171624892304,47.9060250358962,47.9955534116876,
48.0843273344302,48.1730941115943,48.2618766705276,48.3519705134526,48.4409057141138,
48.5315788781706,48.6222520422274,48.7134731108222,48.8045685913688,48.8955611216527,
48.9864649966019,49.0773190413066,49.1681435703031,49.2589588697564,49.3498243415436,
49.4407136971665,49.5317037438762,49.6053587297499,49.69634898757,49.7872668551369,
49.8781345589675,49.9689726175072,50.0598150491269,50.0969120735111,50.1985524169299,
50.3004232260078,50.4023379611143,50.5041923151378,50.5884654172723),
 .UNSPECIFIED.);
#1261=B_SPLINE_CURVE_WITH_KNOTS('',3,(#20832,#20833,#20834,#20835,#20836,
#20837,#20838,#20839,#20840,#20841,#20842,#20843,#20844,#20845,#20846,#20847,
#20848,#20849,#20850,#20851,#20852,#20853),.UNSPECIFIED.,.F.,.F.,(4,2,2,
2,2,2,2,2,2,2,4),(-4.68690655991433,-4.676968004902,-4.66334057591782,-4.57050127017845,
-4.54307441119981,-4.52441781843419,-4.51528697313272,-4.50756272912277,
-4.49611705684078,-4.45806694667936,-4.39249448366002),.UNSPECIFIED.);
#1262=B_SPLINE_CURVE_WITH_KNOTS('',3,(#20880,#20881,#20882,#20883,#20884,
#20885,#20886,#20887,#20888,#20889,#20890,#20891,#20892,#20893,#20894,#20895,
#20896,#20897,#20898,#20899,#20900,#20901,#20902,#20903,#20904,#20905,#20906,
#20907,#20908,#20909,#20910,#20911,#20912,#20913,#20914,#20915,#20916,#20917,
#20918,#20919,#20920,#20921,#20922,#20923,#20924,#20925,#20926,#20927,#20928,
#20929,#20930,#20931,#20932,#20933,#20934,#20935,#20936,#20937,#20938,#20939,
#20940,#20941,#20942,#20943,#20944,#20945,#20946,#20947,#20948,#20949,#20950,
#20951,#20952,#20953,#20954,#20955,#20956,#20957,#20958,#20959,#20960,#20961,
#20962,#20963,#20964,#20965,#20966,#20967),.UNSPECIFIED.,.F.,.F.,(4,3,3,
3,3,3,3,3,3,3,3,3,3,3,3,3,3,3,3,3,3,3,3,3,3,3,3,3,3,4),(2.05878368674717E-14,
0.023405447201913,0.0471352136112047,0.0707669153637672,0.0840367480408261,
0.0878713467795278,0.110975706691734,0.133712282270125,0.150709160734639,
0.158060268187143,0.163470733062873,0.167953178850733,0.189907599318317,
0.201793217244577,0.224252520133955,0.234752288110081,0.240507487537732,
0.24411168274315,0.265861093328888,0.287518743439702,0.309003455419039,
0.317294467212432,0.321188873214287,0.341934990903991,0.362478952452641,
0.367608141617428,0.372096895882347,0.385217611626515,0.405963257762497,
0.415993328865176),.UNSPECIFIED.);
#1263=B_SPLINE_CURVE_WITH_KNOTS('',3,(#20969,#20970,#20971,#20972),
 .UNSPECIFIED.,.F.,.F.,(4,4),(-2.84914982550175,-2.06894047480313),
 .UNSPECIFIED.);
#1264=B_SPLINE_CURVE_WITH_KNOTS('',3,(#20974,#20975,#20976,#20977,#20978,
#20979,#20980,#20981,#20982,#20983,#20984,#20985,#20986,#20987,#20988,#20989,
#20990,#20991,#20992,#20993,#20994,#20995,#20996,#20997,#20998,#20999,#21000,
#21001,#21002,#21003,#21004,#21005,#21006,#21007,#21008,#21009,#21010,#21011,
#21012,#21013,#21014,#21015,#21016,#21017,#21018,#21019,#21020,#21021,#21022,
#21023,#21024,#21025,#21026,#21027,#21028,#21029,#21030,#21031,#21032,#21033,
#21034,#21035,#21036,#21037,#21038,#21039,#21040,#21041,#21042,#21043,#21044,
#21045,#21046,#21047,#21048,#21049,#21050,#21051,#21052,#21053,#21054,#21055,
#21056,#21057,#21058,#21059,#21060,#21061),.UNSPECIFIED.,.F.,.F.,(4,3,3,
3,3,3,3,3,3,3,3,3,3,3,3,3,3,3,3,3,3,3,3,3,3,3,3,3,3,4),(-0.413490722097494,
-0.390374461965417,-0.376956788739721,-0.364612854506389,-0.357223081629536,
-0.353167632297454,-0.329816475307035,-0.3110173587975,-0.300922997939596,
-0.297410089408388,-0.274622870922315,-0.252197899215606,-0.232987043189295,
-0.22435563742345,-0.220563464855743,-0.216970640358496,-0.195389510663287,
-0.179453841006409,-0.157360826323377,-0.146597972574468,-0.141428288189789,
-0.120042549964023,-0.0987340253119133,-0.0775979223516053,-0.0725581786302476,
-0.0680299217253234,-0.0474532857852412,-0.0272139184783649,-0.00761976281229705,
0.),.UNSPECIFIED.);
#1265=B_SPLINE_CURVE_WITH_KNOTS('',3,(#21062,#21063,#21064,#21065,#21066,
#21067,#21068,#21069,#21070,#21071,#21072,#21073,#21074,#21075,#21076,#21077,
#21078,#21079,#21080,#21081,#21082,#21083,#21084,#21085,#21086),
 .UNSPECIFIED.,.F.,.F.,(4,3,3,3,3,3,3,3,4),(16.7019922841306,16.810649070825,
16.9192297222185,17.0277712030643,17.1410987082733,17.2497327354331,17.3584254886797,
17.467270185633,17.4810812239006),.UNSPECIFIED.);
#1266=B_SPLINE_CURVE_WITH_KNOTS('',3,(#21092,#21093,#21094,#21095,#21096,
#21097,#21098,#21099,#21100,#21101,#21102,#21103,#21104,#21105,#21106,#21107,
#21108,#21109,#21110,#21111,#21112,#21113,#21114,#21115,#21116),
 .UNSPECIFIED.,.F.,.F.,(4,3,3,3,3,3,3,3,4),(15.4643166016706,15.573136451511,
15.6818269380766,15.7904251770487,15.9036702413563,16.0122290128815,16.1208010500588,
16.2294623722504,16.2434054342788),.UNSPECIFIED.);
#1267=B_SPLINE_CURVE_WITH_KNOTS('',3,(#21142,#21143,#21144,#21145,#21146,
#21147,#21148,#21149,#21150,#21151,#21152,#21153,#21154,#21155,#21156,#21157,
#21158,#21159,#21160,#21161,#21162,#21163,#21164,#21165,#21166,#21167,#21168,
#21169,#21170,#21171,#21172,#21173,#21174,#21175,#21176,#21177,#21178,#21179,
#21180,#21181,#21182,#21183,#21184,#21185,#21186,#21187,#21188,#21189,#21190,
#21191,#21192,#21193,#21194,#21195,#21196,#21197,#21198,#21199,#21200,#21201,
#21202,#21203,#21204,#21205,#21206,#21207,#21208,#21209,#21210,#21211,#21212,
#21213,#21214,#21215,#21216,#21217,#21218,#21219,#21220,#21221,#21222,#21223,
#21224,#21225,#21226,#21227,#21228,#21229),.UNSPECIFIED.,.F.,.F.,(4,3,3,
3,3,3,3,3,3,3,3,3,3,3,3,3,3,3,3,3,3,3,3,3,3,3,3,3,3,4),(9.94883000103285E-15,
0.019616691656509,0.0399302769755012,0.0573080150775109,0.0651965825194071,
0.0692472851263457,0.0727586240116996,0.0938674469417637,0.115267103019471,
0.136627386511764,0.139448576973331,0.143452860461702,0.147424687779491,
0.169517815215389,0.179453841006421,0.200870095742099,0.220290031668888,
0.22390552179017,0.245971799155713,0.268703017816031,0.291434236476348,
0.297317452472671,0.303372200521482,0.326746258431751,0.349433290040221,
0.355210854434181,0.359640172217466,0.37695678873974,0.400080606868808,
0.414094136780462),.UNSPECIFIED.);
#1268=B_SPLINE_CURVE_WITH_KNOTS('',3,(#21231,#21232,#21233,#21234,#21235,
#21236,#21237,#21238,#21239,#21240,#21241,#21242,#21243,#21244,#21245,#21246,
#21247,#21248,#21249,#21250,#21251,#21252,#21253,#21254,#21255,#21256,#21257,
#21258,#21259,#21260,#21261,#21262,#21263,#21264,#21265,#21266,#21267,#21268,
#21269,#21270,#21271,#21272,#21273,#21274,#21275,#21276,#21277,#21278,#21279,
#21280,#21281,#21282,#21283,#21284,#21285,#21286,#21287,#21288,#21289,#21290,
#21291,#21292,#21293,#21294,#21295,#21296,#21297,#21298,#21299,#21300,#21301,
#21302,#21303,#21304,#21305,#21306,#21307,#21308,#21309,#21310,#21311,#21312,
#21313,#21314,#21315),.UNSPECIFIED.,.F.,.F.,(4,3,3,3,3,3,3,3,3,3,3,3,3,
3,3,3,3,3,3,3,3,3,3,3,3,3,3,3,4),(-0.415993328865187,-0.395247681143785,
-0.385217611626505,-0.373753586977634,-0.368797025934534,-0.36502116844561,
-0.344384137829435,-0.326531494809057,-0.320844694700121,-0.315794800692042,
-0.294447216742868,-0.27264031880428,-0.255006113686598,-0.246851849353904,
-0.243114662305886,-0.220650412226406,-0.201793217244566,-0.179843818696151,
-0.168406146924892,-0.164760369659269,-0.142479944942064,-0.11944136986474,
-0.0964027947874157,-0.086570173338417,-0.0816436307916124,-0.0579861482237484,
-0.0343081270358223,-0.0108824362787603,0.),.UNSPECIFIED.);
#1269=B_SPLINE_CURVE_WITH_KNOTS('',3,(#21316,#21317,#21318,#21319),
 .UNSPECIFIED.,.F.,.F.,(4,4),(0.,0.780209350698613),.UNSPECIFIED.);
#1270=B_SPLINE_CURVE_WITH_KNOTS('',3,(#21521,#21522,#21523,#21524,#21525,
#21526,#21527,#21528,#21529,#21530,#21531,#21532,#21533,#21534,#21535,#21536,
#21537,#21538,#21539,#21540,#21541,#21542,#21543,#21544,#21545,#21546,#21547,
#21548,#21549,#21550,#21551,#21552,#21553,#21554,#21555,#21556,#21557,#21558,
#21559,#21560,#21561,#21562,#21563,#21564,#21565,#21566,#21567,#21568,#21569,
#21570,#21571,#21572,#21573,#21574,#21575,#21576,#21577,#21578,#21579,#21580,
#21581,#21582,#21583,#21584,#21585,#21586,#21587,#21588,#21589,#21590,#21591,
#21592,#21593,#21594,#21595,#21596,#21597,#21598,#21599,#21600,#21601,#21602,
#21603,#21604,#21605,#21606,#21607,#21608,#21609,#21610,#21611,#21612,#21613,
#21614,#21615,#21616,#21617,#21618,#21619,#21620,#21621,#21622,#21623,#21624,
#21625,#21626),.UNSPECIFIED.,.F.,.F.,(4,3,3,3,3,3,3,3,3,3,3,3,3,3,3,3,3,
3,3,3,3,3,3,3,3,3,3,3,3,3,3,3,3,3,3,4),(4.87579287875967E-5,0.0396105854411369,
0.0421684740053724,0.082059122742856,0.12338177968178,0.164704436620703,
0.170094771591715,0.175319647983374,0.214784946467228,0.254291541803321,
0.293151938468816,0.325136464664712,0.334844260977463,0.340168266397053,
0.359707602090094,0.397735946899136,0.434801284779746,0.46134294969662,
0.485996360447615,0.493345060083779,0.498524669937982,0.535408882651194,
0.572734961962543,0.609820594328277,0.632520778240444,0.644430130512825,
0.650618647569442,0.655220962152611,0.658570235704578,0.695166161431644,
0.731571524795797,0.744958227452224,0.754067922795179,0.78988127496075,
0.825088562663305,0.847325527525853),.UNSPECIFIED.);
#1271=B_SPLINE_CURVE_WITH_KNOTS('',3,(#21627,#21628,#21629,#21630,#21631,
#21632,#21633,#21634,#21635,#21636,#21637,#21638,#21639,#21640,#21641,#21642,
#21643,#21644,#21645,#21646,#21647,#21648,#21649,#21650,#21651,#21652,#21653,
#21654,#21655,#21656,#21657,#21658,#21659,#21660,#21661,#21662,#21663,#21664,
#21665,#21666,#21667,#21668,#21669,#21670,#21671,#21672,#21673,#21674,#21675,
#21676,#21677,#21678,#21679,#21680,#21681,#21682,#21683,#21684,#21685,#21686,
#21687,#21688,#21689,#21690,#21691,#21692,#21693,#21694,#21695,#21696,#21697,
#21698,#21699,#21700,#21701,#21702,#21703,#21704,#21705,#21706,#21707,#21708,
#21709,#21710,#21711,#21712,#21713,#21714,#21715,#21716,#21717,#21718,#21719,
#21720),.UNSPECIFIED.,.F.,.F.,(4,3,3,3,3,3,3,3,3,3,3,3,3,3,3,3,3,3,3,3,
3,3,3,3,3,3,3,3,3,3,3,4),(-0.847325527525843,-0.811503753623457,-0.776442908990808,
-0.753769402338684,-0.745431135913051,-0.709753628192895,-0.673219987554428,
-0.651138320105864,-0.645616024847356,-0.608466815738069,-0.57090382277613,
-0.533372849367635,-0.505758215660538,-0.497488333365585,-0.491961441323387,
-0.453421092885502,-0.422238544386844,-0.384505330263272,-0.346772116139701,
-0.33539303508032,-0.33016070262821,-0.291919157069796,-0.252839602001601,
-0.215142387780448,-0.175907489429898,-0.170455452500928,-0.160225010582203,
-0.120305086436378,-0.0801631965284521,-0.0402999487969805,-0.00225557790275668,
-8.80689562460376E-15),.UNSPECIFIED.);
#1272=B_SPLINE_CURVE_WITH_KNOTS('',3,(#21913,#21914,#21915,#21916,#21917,
#21918,#21919,#21920,#21921,#21922,#21923,#21924,#21925,#21926,#21927,#21928,
#21929,#21930,#21931,#21932,#21933,#21934,#21935,#21936,#21937,#21938,#21939,
#21940,#21941,#21942,#21943,#21944,#21945,#21946,#21947,#21948,#21949,#21950,
#21951,#21952,#21953,#21954,#21955,#21956,#21957,#21958,#21959,#21960,#21961,
#21962,#21963,#21964,#21965,#21966,#21967,#21968,#21969,#21970,#21971,#21972,
#21973,#21974,#21975,#21976,#21977,#21978,#21979,#21980,#21981,#21982,#21983,
#21984,#21985,#21986,#21987,#21988,#21989,#21990,#21991,#21992,#21993,#21994,
#21995,#21996,#21997,#21998,#21999,#22000,#22001,#22002,#22003,#22004,#22005,
#22006,#22007,#22008,#22009),.UNSPECIFIED.,.F.,.F.,(4,3,3,3,3,3,3,3,3,3,
3,3,3,3,3,3,3,3,3,3,3,3,3,3,3,3,3,3,3,3,3,3,4),(0.,0.0357326537857237,0.0704414344150977,
0.105764244213075,0.14171479622342,0.147192652306303,0.152214352689264,
0.188537300917028,0.225478864831264,0.26267763210979,0.282838324796318,
0.297126845802674,0.304520830993608,0.342575347752296,0.380671971213311,
0.418209942863103,0.423963173602016,0.455960576699411,0.461085295912164,
0.498135375724191,0.536332170206057,0.574942151961225,0.613574806753294,
0.619086816026134,0.624483039944413,0.630147733446615,0.669254131260838,
0.708784888651943,0.727582209613668,0.735557703752757,0.775673392238865,
0.815702463256823,0.844212290556702),.UNSPECIFIED.);
#1273=B_SPLINE_CURVE_WITH_KNOTS('',3,(#22010,#22011,#22012,#22013,#22014,
#22015,#22016,#22017,#22018,#22019,#22020,#22021,#22022,#22023,#22024,#22025,
#22026,#22027,#22028,#22029,#22030,#22031,#22032,#22033,#22034,#22035,#22036,
#22037,#22038,#22039,#22040,#22041,#22042,#22043,#22044,#22045,#22046,#22047,
#22048,#22049,#22050,#22051,#22052,#22053,#22054,#22055,#22056,#22057,#22058,
#22059,#22060,#22061,#22062,#22063,#22064,#22065,#22066,#22067,#22068,#22069,
#22070,#22071,#22072,#22073,#22074,#22075,#22076,#22077,#22078,#22079,#22080,
#22081,#22082,#22083,#22084,#22085,#22086,#22087,#22088,#22089,#22090,#22091,
#22092,#22093,#22094,#22095,#22096,#22097,#22098,#22099,#22100,#22101,#22102,
#22103,#22104,#22105,#22106,#22107,#22108,#22109),.UNSPECIFIED.,.F.,.F.,
(4,3,3,3,3,3,3,3,3,3,3,3,3,3,3,3,3,3,3,3,3,3,3,3,3,3,3,3,3,3,3,3,3,4),(-0.844212290556731,
-0.804914039435832,-0.802217933301225,-0.761983565707593,-0.738497702142073,
-0.731371284183562,-0.724667747997382,-0.685031612027754,-0.645191108329531,
-0.631145243959577,-0.622466655133243,-0.614790169492861,-0.575459911227575,
-0.536634531463482,-0.497051833947599,-0.459723508709767,-0.457469136431715,
-0.452285602603943,-0.414914580183337,-0.385002433230672,-0.347227915621759,
-0.309590191025686,-0.301425288615579,-0.295199281958322,-0.258388869024602,
-0.221724085233776,-0.188385367654945,-0.153950864306229,-0.147824231453246,
-0.142510002622108,-0.106551008289361,-0.0707579690404533,-0.0353789845202334,
-1.35445026026053E-14),.UNSPECIFIED.);
#1552=VERTEX_POINT('',#15684);
#1553=VERTEX_POINT('',#15685);
#1554=VERTEX_POINT('',#15687);
#1555=VERTEX_POINT('',#15842);
#1556=VERTEX_POINT('',#15957);
#1557=VERTEX_POINT('',#15958);
#1558=VERTEX_POINT('',#15960);
#1559=VERTEX_POINT('',#16176);
#1560=VERTEX_POINT('',#16350);
#1561=VERTEX_POINT('',#16351);
#1562=VERTEX_POINT('',#16353);
#1563=VERTEX_POINT('',#16709);
#1564=VERTEX_POINT('',#16710);
#1565=VERTEX_POINT('',#16882);
#1566=VERTEX_POINT('',#17050);
#1567=VERTEX_POINT('',#17051);
#1568=VERTEX_POINT('',#17053);
#1569=VERTEX_POINT('',#17393);
#1570=VERTEX_POINT('',#17394);
#1571=VERTEX_POINT('',#17566);
#1572=VERTEX_POINT('',#17781);
#1573=VERTEX_POINT('',#17782);
#1574=VERTEX_POINT('',#17859);
#1575=VERTEX_POINT('',#17861);
#1576=VERTEX_POINT('',#17899);
#1577=VERTEX_POINT('',#18129);
#1578=VERTEX_POINT('',#18362);
#1579=VERTEX_POINT('',#18592);
#1580=VERTEX_POINT('',#18603);
#1581=VERTEX_POINT('',#18833);
#1582=VERTEX_POINT('',#19066);
#1583=VERTEX_POINT('',#19119);
#1584=VERTEX_POINT('',#19121);
#1585=VERTEX_POINT('',#19126);
#1586=VERTEX_POINT('',#19362);
#1587=VERTEX_POINT('',#19592);
#1588=VERTEX_POINT('',#19825);
#1589=VERTEX_POINT('',#20058);
#1590=VERTEX_POINT('',#20521);
#1591=VERTEX_POINT('',#20550);
#1592=VERTEX_POINT('',#20711);
#1593=VERTEX_POINT('',#20713);
#1594=VERTEX_POINT('',#20878);
#1595=VERTEX_POINT('',#20879);
#1596=VERTEX_POINT('',#20968);
#1597=VERTEX_POINT('',#20973);
#1598=VERTEX_POINT('',#21088);
#1599=VERTEX_POINT('',#21090);
#1600=VERTEX_POINT('',#21141);
#1601=VERTEX_POINT('',#21230);
#1602=VERTEX_POINT('',#21321);
#1603=VERTEX_POINT('',#21325);
#1604=VERTEX_POINT('',#22111);
#1605=VERTEX_POINT('',#22113);
#1993=EDGE_CURVE('',#1552,#1553,#884,.T.);
#1994=EDGE_CURVE('',#1554,#1552,#1224,.T.);
#1995=EDGE_CURVE('',#1555,#1554,#331,.T.);
#1996=EDGE_CURVE('',#1555,#1553,#1225,.T.);
#1997=EDGE_CURVE('',#1556,#1557,#885,.T.);
#1998=EDGE_CURVE('',#1558,#1556,#1226,.T.);
#1999=EDGE_CURVE('',#1552,#1558,#1227,.T.);
#2000=EDGE_CURVE('',#1553,#1559,#1228,.T.);
#2001=EDGE_CURVE('',#1559,#1557,#1229,.T.);
#2002=EDGE_CURVE('',#1560,#1561,#886,.T.);
#2003=EDGE_CURVE('',#1562,#1560,#1230,.F.);
#2004=EDGE_CURVE('',#1556,#1562,#1231,.T.);
#2005=EDGE_CURVE('',#1557,#1561,#1232,.T.);
#2006=EDGE_CURVE('',#1563,#1564,#887,.T.);
#2007=EDGE_CURVE('',#1560,#1563,#1233,.F.);
#2008=EDGE_CURVE('',#1561,#1565,#1234,.T.);
#2009=EDGE_CURVE('',#1565,#1564,#1235,.T.);
#2010=EDGE_CURVE('',#1566,#1567,#888,.T.);
#2011=EDGE_CURVE('',#1568,#1566,#1236,.F.);
#2012=EDGE_CURVE('',#1563,#1568,#1237,.F.);
#2013=EDGE_CURVE('',#1564,#1567,#1238,.T.);
#2014=EDGE_CURVE('',#1569,#1570,#889,.T.);
#2015=EDGE_CURVE('',#1566,#1569,#1239,.F.);
#2016=EDGE_CURVE('',#1567,#1571,#1240,.T.);
#2017=EDGE_CURVE('',#1571,#1570,#1241,.T.);
#2018=EDGE_CURVE('',#1572,#1573,#1242,.T.);
#2019=EDGE_CURVE('',#1573,#1574,#332,.F.);
#2020=EDGE_CURVE('',#1574,#1575,#1243,.T.);
#2021=EDGE_CURVE('',#1575,#1576,#1244,.T.);
#2022=EDGE_CURVE('',#1576,#1577,#1245,.T.);
#2023=EDGE_CURVE('',#1577,#1578,#1246,.T.);
#2024=EDGE_CURVE('',#1578,#1579,#1247,.T.);
#2025=EDGE_CURVE('',#1579,#1580,#1248,.T.);
#2026=EDGE_CURVE('',#1580,#1581,#1249,.T.);
#2027=EDGE_CURVE('',#1581,#1582,#1250,.T.);
#2028=EDGE_CURVE('',#1583,#1582,#333,.F.);
#2029=EDGE_CURVE('',#1583,#1584,#1251,.T.);
#2030=EDGE_CURVE('',#1584,#1585,#1252,.T.);
#2031=EDGE_CURVE('',#1585,#1586,#1253,.T.);
#2032=EDGE_CURVE('',#1586,#1587,#1254,.T.);
#2033=EDGE_CURVE('',#1587,#1588,#1255,.T.);
#2034=EDGE_CURVE('',#1588,#1589,#1256,.T.);
#2035=EDGE_CURVE('',#1589,#1572,#1257,.T.);
#2036=EDGE_CURVE('',#1570,#1590,#1258,.T.);
#2037=EDGE_CURVE('',#1590,#1591,#1259,.T.);
#2038=EDGE_CURVE('',#1592,#1591,#334,.T.);
#2039=EDGE_CURVE('',#1593,#1592,#1260,.T.);
#2040=EDGE_CURVE('',#1569,#1593,#1261,.F.);
#2041=EDGE_CURVE('',#1594,#1595,#1262,.T.);
#2042=EDGE_CURVE('',#1594,#1596,#1263,.T.);
#2043=EDGE_CURVE('',#1596,#1597,#1264,.T.);
#2044=EDGE_CURVE('',#1597,#1595,#1265,.T.);
#2045=EDGE_CURVE('',#1595,#1598,#335,.T.);
#2046=EDGE_CURVE('',#1597,#1599,#336,.T.);
#2047=EDGE_CURVE('',#1599,#1598,#1266,.T.);
#2048=EDGE_CURVE('',#1598,#1600,#1267,.T.);
#2049=EDGE_CURVE('',#1599,#1601,#1268,.T.);
#2050=EDGE_CURVE('',#1601,#1600,#1269,.T.);
#2051=EDGE_CURVE('',#1596,#1602,#337,.T.);
#2052=EDGE_CURVE('',#1602,#1601,#338,.T.);
#2053=EDGE_CURVE('',#1603,#1603,#339,.T.);
#2054=EDGE_CURVE('',#1603,#1602,#890,.T.);
#2055=EDGE_CURVE('',#1600,#1594,#340,.T.);
#2056=EDGE_CURVE('',#1582,#1592,#1270,.T.);
#2057=EDGE_CURVE('',#1554,#1574,#1271,.T.);
#2058=EDGE_CURVE('',#1591,#1583,#1272,.T.);
#2059=EDGE_CURVE('',#1573,#1555,#1273,.T.);
#2060=EDGE_CURVE('',#1604,#1604,#341,.T.);
#2061=EDGE_CURVE('',#1604,#1605,#891,.T.);
#2062=EDGE_CURVE('',#1605,#1605,#342,.T.);
#2760=ORIENTED_EDGE('',*,*,#1993,.F.);
#2761=ORIENTED_EDGE('',*,*,#1994,.F.);
#2762=ORIENTED_EDGE('',*,*,#1995,.F.);
#2763=ORIENTED_EDGE('',*,*,#1996,.T.);
#2764=ORIENTED_EDGE('',*,*,#1997,.F.);
#2765=ORIENTED_EDGE('',*,*,#1998,.F.);
#2766=ORIENTED_EDGE('',*,*,#1999,.F.);
#2767=ORIENTED_EDGE('',*,*,#1993,.T.);
#2768=ORIENTED_EDGE('',*,*,#2000,.T.);
#2769=ORIENTED_EDGE('',*,*,#2001,.T.);
#2770=ORIENTED_EDGE('',*,*,#2002,.F.);
#2771=ORIENTED_EDGE('',*,*,#2003,.F.);
#2772=ORIENTED_EDGE('',*,*,#2004,.F.);
#2773=ORIENTED_EDGE('',*,*,#1997,.T.);
#2774=ORIENTED_EDGE('',*,*,#2005,.T.);
#2775=ORIENTED_EDGE('',*,*,#2006,.F.);
#2776=ORIENTED_EDGE('',*,*,#2007,.F.);
#2777=ORIENTED_EDGE('',*,*,#2002,.T.);
#2778=ORIENTED_EDGE('',*,*,#2008,.T.);
#2779=ORIENTED_EDGE('',*,*,#2009,.T.);
#2780=ORIENTED_EDGE('',*,*,#2010,.F.);
#2781=ORIENTED_EDGE('',*,*,#2011,.F.);
#2782=ORIENTED_EDGE('',*,*,#2012,.F.);
#2783=ORIENTED_EDGE('',*,*,#2006,.T.);
#2784=ORIENTED_EDGE('',*,*,#2013,.T.);
#2785=ORIENTED_EDGE('',*,*,#2014,.F.);
#2786=ORIENTED_EDGE('',*,*,#2015,.F.);
#2787=ORIENTED_EDGE('',*,*,#2010,.T.);
#2788=ORIENTED_EDGE('',*,*,#2016,.T.);
#2789=ORIENTED_EDGE('',*,*,#2017,.T.);
#2790=ORIENTED_EDGE('',*,*,#2018,.T.);
#2791=ORIENTED_EDGE('',*,*,#2019,.T.);
#2792=ORIENTED_EDGE('',*,*,#2020,.T.);
#2793=ORIENTED_EDGE('',*,*,#2021,.T.);
#2794=ORIENTED_EDGE('',*,*,#2022,.T.);
#2795=ORIENTED_EDGE('',*,*,#2023,.T.);
#2796=ORIENTED_EDGE('',*,*,#2024,.T.);
#2797=ORIENTED_EDGE('',*,*,#2025,.T.);
#2798=ORIENTED_EDGE('',*,*,#2026,.T.);
#2799=ORIENTED_EDGE('',*,*,#2027,.T.);
#2800=ORIENTED_EDGE('',*,*,#2028,.F.);
#2801=ORIENTED_EDGE('',*,*,#2029,.T.);
#2802=ORIENTED_EDGE('',*,*,#2030,.T.);
#2803=ORIENTED_EDGE('',*,*,#2031,.T.);
#2804=ORIENTED_EDGE('',*,*,#2032,.T.);
#2805=ORIENTED_EDGE('',*,*,#2033,.T.);
#2806=ORIENTED_EDGE('',*,*,#2034,.T.);
#2807=ORIENTED_EDGE('',*,*,#2035,.T.);
#2808=ORIENTED_EDGE('',*,*,#2014,.T.);
#2809=ORIENTED_EDGE('',*,*,#2036,.T.);
#2810=ORIENTED_EDGE('',*,*,#2037,.T.);
#2811=ORIENTED_EDGE('',*,*,#2038,.F.);
#2812=ORIENTED_EDGE('',*,*,#2039,.F.);
#2813=ORIENTED_EDGE('',*,*,#2040,.F.);
#2814=ORIENTED_EDGE('',*,*,#2041,.F.);
#2815=ORIENTED_EDGE('',*,*,#2042,.T.);
#2816=ORIENTED_EDGE('',*,*,#2043,.T.);
#2817=ORIENTED_EDGE('',*,*,#2044,.T.);
#2818=ORIENTED_EDGE('',*,*,#2045,.F.);
#2819=ORIENTED_EDGE('',*,*,#2044,.F.);
#2820=ORIENTED_EDGE('',*,*,#2046,.T.);
#2821=ORIENTED_EDGE('',*,*,#2047,.T.);
#2822=ORIENTED_EDGE('',*,*,#2048,.F.);
#2823=ORIENTED_EDGE('',*,*,#2047,.F.);
#2824=ORIENTED_EDGE('',*,*,#2049,.T.);
#2825=ORIENTED_EDGE('',*,*,#2050,.T.);
#2826=ORIENTED_EDGE('',*,*,#2051,.T.);
#2827=ORIENTED_EDGE('',*,*,#2052,.T.);
#2828=ORIENTED_EDGE('',*,*,#2049,.F.);
#2829=ORIENTED_EDGE('',*,*,#2046,.F.);
#2830=ORIENTED_EDGE('',*,*,#2043,.F.);
#2831=ORIENTED_EDGE('',*,*,#2053,.F.);
#2832=ORIENTED_EDGE('',*,*,#2054,.T.);
#2833=ORIENTED_EDGE('',*,*,#2051,.F.);
#2834=ORIENTED_EDGE('',*,*,#2042,.F.);
#2835=ORIENTED_EDGE('',*,*,#2055,.F.);
#2836=ORIENTED_EDGE('',*,*,#2050,.F.);
#2837=ORIENTED_EDGE('',*,*,#2052,.F.);
#2838=ORIENTED_EDGE('',*,*,#2054,.F.);
#2839=ORIENTED_EDGE('',*,*,#2056,.F.);
#2840=ORIENTED_EDGE('',*,*,#2027,.F.);
#2841=ORIENTED_EDGE('',*,*,#2026,.F.);
#2842=ORIENTED_EDGE('',*,*,#2025,.F.);
#2843=ORIENTED_EDGE('',*,*,#2024,.F.);
#2844=ORIENTED_EDGE('',*,*,#2023,.F.);
#2845=ORIENTED_EDGE('',*,*,#2022,.F.);
#2846=ORIENTED_EDGE('',*,*,#2021,.F.);
#2847=ORIENTED_EDGE('',*,*,#2020,.F.);
#2848=ORIENTED_EDGE('',*,*,#2057,.F.);
#2849=ORIENTED_EDGE('',*,*,#1994,.T.);
#2850=ORIENTED_EDGE('',*,*,#1999,.T.);
#2851=ORIENTED_EDGE('',*,*,#1998,.T.);
#2852=ORIENTED_EDGE('',*,*,#2004,.T.);
#2853=ORIENTED_EDGE('',*,*,#2003,.T.);
#2854=ORIENTED_EDGE('',*,*,#2007,.T.);
#2855=ORIENTED_EDGE('',*,*,#2012,.T.);
#2856=ORIENTED_EDGE('',*,*,#2011,.T.);
#2857=ORIENTED_EDGE('',*,*,#2015,.T.);
#2858=ORIENTED_EDGE('',*,*,#2040,.T.);
#2859=ORIENTED_EDGE('',*,*,#2039,.T.);
#2860=ORIENTED_EDGE('',*,*,#2058,.F.);
#2861=ORIENTED_EDGE('',*,*,#2037,.F.);
#2862=ORIENTED_EDGE('',*,*,#2036,.F.);
#2863=ORIENTED_EDGE('',*,*,#2017,.F.);
#2864=ORIENTED_EDGE('',*,*,#2016,.F.);
#2865=ORIENTED_EDGE('',*,*,#2013,.F.);
#2866=ORIENTED_EDGE('',*,*,#2009,.F.);
#2867=ORIENTED_EDGE('',*,*,#2008,.F.);
#2868=ORIENTED_EDGE('',*,*,#2005,.F.);
#2869=ORIENTED_EDGE('',*,*,#2001,.F.);
#2870=ORIENTED_EDGE('',*,*,#2000,.F.);
#2871=ORIENTED_EDGE('',*,*,#1996,.F.);
#2872=ORIENTED_EDGE('',*,*,#2059,.F.);
#2873=ORIENTED_EDGE('',*,*,#2018,.F.);
#2874=ORIENTED_EDGE('',*,*,#2035,.F.);
#2875=ORIENTED_EDGE('',*,*,#2034,.F.);
#2876=ORIENTED_EDGE('',*,*,#2033,.F.);
#2877=ORIENTED_EDGE('',*,*,#2032,.F.);
#2878=ORIENTED_EDGE('',*,*,#2031,.F.);
#2879=ORIENTED_EDGE('',*,*,#2030,.F.);
#2880=ORIENTED_EDGE('',*,*,#2029,.F.);
#2881=ORIENTED_EDGE('',*,*,#2060,.F.);
#2882=ORIENTED_EDGE('',*,*,#2061,.T.);
#2883=ORIENTED_EDGE('',*,*,#2062,.T.);
#2884=ORIENTED_EDGE('',*,*,#2061,.F.);
#2885=ORIENTED_EDGE('',*,*,#2060,.T.);
#2886=ORIENTED_EDGE('',*,*,#2059,.T.);
#2887=ORIENTED_EDGE('',*,*,#1995,.T.);
#2888=ORIENTED_EDGE('',*,*,#2057,.T.);
#2889=ORIENTED_EDGE('',*,*,#2019,.F.);
#2890=ORIENTED_EDGE('',*,*,#2058,.T.);
#2891=ORIENTED_EDGE('',*,*,#2028,.T.);
#2892=ORIENTED_EDGE('',*,*,#2056,.T.);
#2893=ORIENTED_EDGE('',*,*,#2038,.T.);
#2894=ORIENTED_EDGE('',*,*,#2048,.T.);
#2895=ORIENTED_EDGE('',*,*,#2055,.T.);
#2896=ORIENTED_EDGE('',*,*,#2041,.T.);
#2897=ORIENTED_EDGE('',*,*,#2045,.T.);
#2898=ORIENTED_EDGE('',*,*,#2062,.F.);
#2899=ORIENTED_EDGE('',*,*,#2053,.T.);
#3425=CYLINDRICAL_SURFACE('',#3963,3.72275);
#3426=CYLINDRICAL_SURFACE('',#3965,3.72275);
#3427=CYLINDRICAL_SURFACE('',#3966,3.72275);
#3428=CYLINDRICAL_SURFACE('',#3967,3.72275);
#3429=CYLINDRICAL_SURFACE('',#3968,3.72275);
#3430=CYLINDRICAL_SURFACE('',#3969,3.72275);
#3431=CYLINDRICAL_SURFACE('',#3970,4.433);
#3432=CYLINDRICAL_SURFACE('',#3973,3.72275);
#3433=CYLINDRICAL_SURFACE('',#3975,1.77625);
#3434=CYLINDRICAL_SURFACE('',#3981,2.204);
#3435=CYLINDRICAL_SURFACE('',#3984,5.42440960677665);
#3558=ADVANCED_FACE('',(#466),#3425,.T.);
#3559=ADVANCED_FACE('',(#467),#3426,.T.);
#3560=ADVANCED_FACE('',(#468),#3427,.T.);
#3561=ADVANCED_FACE('',(#469),#3428,.T.);
#3562=ADVANCED_FACE('',(#470),#3429,.T.);
#3563=ADVANCED_FACE('',(#471),#3430,.T.);
#3564=ADVANCED_FACE('',(#472),#3431,.T.);
#3565=ADVANCED_FACE('',(#473),#3432,.T.);
#3566=ADVANCED_FACE('',(#474),#62,.T.);
#3567=ADVANCED_FACE('',(#475),#3433,.F.);
#3568=ADVANCED_FACE('',(#476),#63,.T.);
#3569=ADVANCED_FACE('',(#477),#229,.F.);
#3570=ADVANCED_FACE('',(#478),#3434,.F.);
#3571=ADVANCED_FACE('',(#479),#64,.F.);
#3572=ADVANCED_FACE('',(#480),#65,.F.);
#3573=ADVANCED_FACE('',(#481),#3435,.T.);
#3574=ADVANCED_FACE('',(#482,#193),#230,.T.);
#3575=ADVANCED_FACE('',(#483,#194),#231,.T.);
#3576=ADVANCED_FACE('',(#484,#195),#232,.F.);
#3680=CLOSED_SHELL('',(#3558,#3559,#3560,#3561,#3562,#3563,#3564,#3565,
#3566,#3567,#3568,#3569,#3570,#3571,#3572,#3573,#3574,#3575,#3576));
#3962=AXIS2_PLACEMENT_3D('',#15682,#4501,#4502);
#3963=AXIS2_PLACEMENT_3D('',#15683,#4503,#4504);
#3964=AXIS2_PLACEMENT_3D('',#15843,#4506,#4507);
#3965=AXIS2_PLACEMENT_3D('',#15956,#4508,#4509);
#3966=AXIS2_PLACEMENT_3D('',#16349,#4511,#4512);
#3967=AXIS2_PLACEMENT_3D('',#16708,#4514,#4515);
#3968=AXIS2_PLACEMENT_3D('',#17049,#4517,#4518);
#3969=AXIS2_PLACEMENT_3D('',#17392,#4520,#4521);
#3970=AXIS2_PLACEMENT_3D('',#17780,#4523,#4524);
#3971=AXIS2_PLACEMENT_3D('',#17860,#4525,#4526);
#3972=AXIS2_PLACEMENT_3D('',#19120,#4527,#4528);
#3973=AXIS2_PLACEMENT_3D('',#20520,#4529,#4530);
#3974=AXIS2_PLACEMENT_3D('',#20712,#4531,#4532);
#3975=AXIS2_PLACEMENT_3D('',#21087,#4533,#4534);
#3976=AXIS2_PLACEMENT_3D('',#21089,#4535,#4536);
#3977=AXIS2_PLACEMENT_3D('',#21091,#4537,#4538);
#3978=AXIS2_PLACEMENT_3D('',#21320,#4539,#4540);
#3979=AXIS2_PLACEMENT_3D('',#21322,#4541,#4542);
#3980=AXIS2_PLACEMENT_3D('',#21323,#4543,#4544);
#3981=AXIS2_PLACEMENT_3D('',#21324,#4545,#4546);
#3982=AXIS2_PLACEMENT_3D('',#21326,#4547,#4548);
#3983=AXIS2_PLACEMENT_3D('',#21328,#4550,#4551);
#3984=AXIS2_PLACEMENT_3D('',#22110,#4552,#4553);
#3985=AXIS2_PLACEMENT_3D('',#22112,#4554,#4555);
#3986=AXIS2_PLACEMENT_3D('',#22115,#4557,#4558);
#3987=AXIS2_PLACEMENT_3D('',#22116,#4559,#4560);
#3988=AXIS2_PLACEMENT_3D('',#22117,#4561,#4562);
#3989=AXIS2_PLACEMENT_3D('',#22118,#4563,#4564);
#4501=DIRECTION('axis',(0.,0.,1.));
#4502=DIRECTION('refdir',(1.,0.,0.));
#4503=DIRECTION('center_axis',(1.,0.,0.));
#4504=DIRECTION('ref_axis',(0.,0.704081661975572,-0.710119013454587));
#4505=DIRECTION('',(-1.,0.,0.));
#4506=DIRECTION('center_axis',(-1.,0.,0.));
#4507=DIRECTION('ref_axis',(0.,1.,2.1444273868172E-14));
#4508=DIRECTION('center_axis',(1.,0.,0.));
#4509=DIRECTION('ref_axis',(0.,0.704081661975572,-0.710119013454587));
#4510=DIRECTION('',(-1.,0.,0.));
#4511=DIRECTION('center_axis',(1.,0.,0.));
#4512=DIRECTION('ref_axis',(0.,0.704081661975572,-0.710119013454587));
#4513=DIRECTION('',(-1.,0.,0.));
#4514=DIRECTION('center_axis',(1.,0.,0.));
#4515=DIRECTION('ref_axis',(0.,0.704081661975572,-0.710119013454587));
#4516=DIRECTION('',(-1.,0.,0.));
#4517=DIRECTION('center_axis',(1.,0.,0.));
#4518=DIRECTION('ref_axis',(0.,0.704081661975572,-0.710119013454587));
#4519=DIRECTION('',(-1.,0.,0.));
#4520=DIRECTION('center_axis',(1.,0.,0.));
#4521=DIRECTION('ref_axis',(0.,0.704081661975572,-0.710119013454587));
#4522=DIRECTION('',(-1.,0.,0.));
#4523=DIRECTION('center_axis',(1.,0.,0.));
#4524=DIRECTION('ref_axis',(0.,1.,0.));
#4525=DIRECTION('center_axis',(-1.,0.,0.));
#4526=DIRECTION('ref_axis',(0.,1.,0.));
#4527=DIRECTION('center_axis',(-1.,0.,0.));
#4528=DIRECTION('ref_axis',(0.,1.,0.));
#4529=DIRECTION('center_axis',(1.,0.,0.));
#4530=DIRECTION('ref_axis',(0.,0.704081661975572,-0.710119013454587));
#4531=DIRECTION('center_axis',(1.,0.,0.));
#4532=DIRECTION('ref_axis',(0.,1.,2.1444273868172E-14));
#4533=DIRECTION('center_axis',(1.,0.,0.));
#4534=DIRECTION('ref_axis',(0.,-0.692346234554118,0.72156544505591));
#4535=DIRECTION('center_axis',(-1.,0.,0.));
#4536=DIRECTION('ref_axis',(0.,9.28774802075533E-14,-1.));
#4537=DIRECTION('center_axis',(-1.,0.,0.));
#4538=DIRECTION('ref_axis',(0.,9.28774802075533E-14,-1.));
#4539=DIRECTION('center_axis',(1.,0.,0.));
#4540=DIRECTION('ref_axis',(0.,0.,-1.));
#4541=DIRECTION('center_axis',(-1.,0.,0.));
#4542=DIRECTION('ref_axis',(0.,0.,-1.));
#4543=DIRECTION('center_axis',(-1.,0.,0.));
#4544=DIRECTION('ref_axis',(0.,0.,-1.));
#4545=DIRECTION('center_axis',(1.,0.,0.));
#4546=DIRECTION('ref_axis',(0.,0.,-1.));
#4547=DIRECTION('center_axis',(1.,0.,0.));
#4548=DIRECTION('ref_axis',(0.,0.,-1.));
#4549=DIRECTION('',(1.,0.,0.));
#4550=DIRECTION('center_axis',(-1.,0.,0.));
#4551=DIRECTION('ref_axis',(0.,0.,-1.));
#4552=DIRECTION('center_axis',(1.,0.,0.));
#4553=DIRECTION('ref_axis',(0.,1.,0.));
#4554=DIRECTION('center_axis',(1.,0.,0.));
#4555=DIRECTION('ref_axis',(0.,1.,0.));
#4556=DIRECTION('',(-1.,0.,0.));
#4557=DIRECTION('center_axis',(1.,0.,0.));
#4558=DIRECTION('ref_axis',(0.,1.,0.));
#4559=DIRECTION('center_axis',(1.,0.,0.));
#4560=DIRECTION('ref_axis',(0.,1.,0.));
#4561=DIRECTION('center_axis',(1.,0.,0.));
#4562=DIRECTION('ref_axis',(0.,1.,0.));
#4563=DIRECTION('center_axis',(1.,0.,0.));
#4564=DIRECTION('ref_axis',(0.,1.,0.));
#15682=CARTESIAN_POINT('',(0.,0.,0.));
#15683=CARTESIAN_POINT('Origin',(80.1322559480305,0.,0.));
#15684=CARTESIAN_POINT('',(83.3465449346096,-2.62112000711956,2.64359555733806));
#15685=CARTESIAN_POINT('',(83.100211836361,-2.62112000711957,2.64359555733806));
#15686=CARTESIAN_POINT('',(80.1322559480305,-2.62112000711956,2.64359555733806));
#15687=CARTESIAN_POINT('',(82.4430056483001,-2.16413257099361,-3.02909190644071));
#15688=CARTESIAN_POINT('Ctrl Pts',(82.4430056483001,-2.16413257099361,-3.02909190644071));
#15689=CARTESIAN_POINT('Ctrl Pts',(82.4488434649895,-2.07571222369529,-3.09226376105495));
#15690=CARTESIAN_POINT('Ctrl Pts',(82.4546812816788,-1.98435154649692,-3.15168333584861));
#15691=CARTESIAN_POINT('Ctrl Pts',(82.4605190983682,-1.89040984780533,-3.20705755636232));
#15692=CARTESIAN_POINT('Ctrl Pts',(82.4663495706933,-1.79658633406051,-3.26236211239906));
#15693=CARTESIAN_POINT('Ctrl Pts',(82.4721800430184,-1.70018862181831,-3.31363120595717));
#15694=CARTESIAN_POINT('Ctrl Pts',(82.4780105153435,-1.60160744862291,-3.36061320937349));
#15695=CARTESIAN_POINT('Ctrl Pts',(82.4839136640581,-1.50179746867793,-3.40818083985263));
#15696=CARTESIAN_POINT('Ctrl Pts',(82.4898168127728,-1.39974957584534,-3.45135348923295));
#15697=CARTESIAN_POINT('Ctrl Pts',(82.4957199614874,-1.29589809170575,-3.48991628816701));
#15698=CARTESIAN_POINT('Ctrl Pts',(82.501541268857,-1.19348640614775,-3.5279444518605));
#15699=CARTESIAN_POINT('Ctrl Pts',(82.5073625762267,-1.08932124388746,-3.56148961867586));
#15700=CARTESIAN_POINT('Ctrl Pts',(82.5131838835963,-0.983840973759557,
-3.590393362969));
#15701=CARTESIAN_POINT('Ctrl Pts',(82.5190035462291,-0.878390505748904,
-3.61928894087448));
#15702=CARTESIAN_POINT('Ctrl Pts',(82.5248232088619,-0.771626088111857,
-3.64354558595605));
#15703=CARTESIAN_POINT('Ctrl Pts',(82.5306428714946,-0.664001330539854,
-3.66305470823755));
#15704=CARTESIAN_POINT('Ctrl Pts',(82.5364624586586,-0.556377968634886,
-3.68256357752672));
#15705=CARTESIAN_POINT('Ctrl Pts',(82.5422820458226,-0.447894718211021,
-3.69732496970828));
#15706=CARTESIAN_POINT('Ctrl Pts',(82.5481016329866,-0.339014446828578,
-3.70728158727409));
#15707=CARTESIAN_POINT('Ctrl Pts',(82.5540670039457,-0.22740666596446,-3.71748762347628));
#15708=CARTESIAN_POINT('Ctrl Pts',(82.5600323749047,-0.11538218645221,-3.72264489477563));
#15709=CARTESIAN_POINT('Ctrl Pts',(82.5659977458638,-0.00344252263953471,
-3.72274840830506));
#15710=CARTESIAN_POINT('Ctrl Pts',(82.5718250423947,0.105906186617274,-3.72284952591118));
#15711=CARTESIAN_POINT('Ctrl Pts',(82.5776523389257,0.215173525287183,-3.71812837826768));
#15712=CARTESIAN_POINT('Ctrl Pts',(82.5834796354566,0.323895920577596,-3.70863303592216));
#15713=CARTESIAN_POINT('Ctrl Pts',(82.5895140436297,0.436482487479869,-3.69880021359159));
#15714=CARTESIAN_POINT('Ctrl Pts',(82.5955484518028,0.548484139555762,-3.6838475851159));
#15715=CARTESIAN_POINT('Ctrl Pts',(82.6015828599759,0.659397897522503,-3.66388618481018));
#15716=CARTESIAN_POINT('Ctrl Pts',(82.607617268149,0.770311655489244,-3.64392478450446));
#15717=CARTESIAN_POINT('Ctrl Pts',(82.6136516763221,0.880137038913179,-3.61895480083851));
#15718=CARTESIAN_POINT('Ctrl Pts',(82.6196860844952,0.988390395894478,-3.58914362875095));
#15719=CARTESIAN_POINT('Ctrl Pts',(82.6256670228396,1.09568453893299,-3.55959660821227));
#15720=CARTESIAN_POINT('Ctrl Pts',(82.631647961184,1.20181842618435,-3.52518858032981));
#15721=CARTESIAN_POINT('Ctrl Pts',(82.6376288995284,1.30632173434007,-3.48602798165631));
#15722=CARTESIAN_POINT('Ctrl Pts',(82.6436023926444,1.41069495404613,-3.44691613111967));
#15723=CARTESIAN_POINT('Ctrl Pts',(82.6495758857604,1.51344124667461,-3.40306362073061));
#15724=CARTESIAN_POINT('Ctrl Pts',(82.6555493788764,1.61410380075984,-3.3546291125656));
#15725=CARTESIAN_POINT('Ctrl Pts',(82.6615170319686,1.71466794145509,-3.30624195670734));
#15726=CARTESIAN_POINT('Ctrl Pts',(82.6674846850609,1.81315202466722,-3.25328189334218));
#15727=CARTESIAN_POINT('Ctrl Pts',(82.6734523381531,1.90911829154975,-3.19595602463022));
#15728=CARTESIAN_POINT('Ctrl Pts',(82.679415920215,2.00501909189412,-3.13866926264078));
#15729=CARTESIAN_POINT('Ctrl Pts',(82.6853795022768,2.09840513820848,-3.07702283230171));
#15730=CARTESIAN_POINT('Ctrl Pts',(82.6913430843387,2.1888629907155,-3.01126989331345));
#15731=CARTESIAN_POINT('Ctrl Pts',(82.6973045161068,2.27928822675991,-2.94554066291673));
#15732=CARTESIAN_POINT('Ctrl Pts',(82.7032659478749,2.36678703349163,-2.87570811134752));
#15733=CARTESIAN_POINT('Ctrl Pts',(82.7092273796431,2.45097522684397,-2.80206852162776));
#15734=CARTESIAN_POINT('Ctrl Pts',(82.7151881043369,2.53515343479185,-2.72843766616226));
#15735=CARTESIAN_POINT('Ctrl Pts',(82.7211488290308,2.61602149853302,-2.65100094352853));
#15736=CARTESIAN_POINT('Ctrl Pts',(82.7271095537246,2.69322915550566,-2.57009421586725));
#15737=CARTESIAN_POINT('Ctrl Pts',(82.7330710136579,2.77044633583596,-2.48917750857785));
#15738=CARTESIAN_POINT('Ctrl Pts',(82.7390324735912,2.84400192580809,-2.40479024528745));
#15739=CARTESIAN_POINT('Ctrl Pts',(82.7449939335244,2.9135838106701,-2.31730380845954));
#15740=CARTESIAN_POINT('Ctrl Pts',(82.750961234612,2.98323387321499,-2.22973165072083));
#15741=CARTESIAN_POINT('Ctrl Pts',(82.7569285356995,3.04890219439032,-2.13905457835484));
#15742=CARTESIAN_POINT('Ctrl Pts',(82.7628958367871,3.11031805223396,-2.04567572612267));
#15743=CARTESIAN_POINT('Ctrl Pts',(82.7688660452264,3.17176383273428,-1.95225137842023));
#15744=CARTESIAN_POINT('Ctrl Pts',(82.7748362536657,3.22895280870762,-1.85612298376126));
#15745=CARTESIAN_POINT('Ctrl Pts',(82.780806462105,3.28165950963282,-1.75771966631101));
#15746=CARTESIAN_POINT('Ctrl Pts',(82.786786148287,3.33444988277065,-1.65916013298769));
#15747=CARTESIAN_POINT('Ctrl Pts',(82.792765834469,3.38274358151401,-1.55831883405778));
#15748=CARTESIAN_POINT('Ctrl Pts',(82.798745520651,3.42636251041828,-1.45564676680166));
#15749=CARTESIAN_POINT('Ctrl Pts',(82.8042533289766,3.46653931777226,-1.3610769098518));
#15750=CARTESIAN_POINT('Ctrl Pts',(82.8097611373021,3.50275051679149,-1.26495428300126));
#15751=CARTESIAN_POINT('Ctrl Pts',(82.8152689456277,3.53489464089742,-1.16764182875346));
#15752=CARTESIAN_POINT('Ctrl Pts',(82.8212402251074,3.56974362933703,-1.06214072435452));
#15753=CARTESIAN_POINT('Ctrl Pts',(82.827211504587,3.59992020435128,-0.954912241094764));
#15754=CARTESIAN_POINT('Ctrl Pts',(82.8331827840667,3.62525361863358,-0.846406381760034));
#15755=CARTESIAN_POINT('Ctrl Pts',(82.8391466256611,3.65055547736247,-0.738035678405555));
#15756=CARTESIAN_POINT('Ctrl Pts',(82.8451104672555,3.67102607907791,-0.628391165217952));
#15757=CARTESIAN_POINT('Ctrl Pts',(82.8510743088499,3.68654393762842,-0.51793953163973));
#15758=CARTESIAN_POINT('Ctrl Pts',(82.8570323314825,3.70204665529625,-0.407595666489731));
#15759=CARTESIAN_POINT('Ctrl Pts',(82.8629903541151,3.71260618482302,-0.296446657350823));
#15760=CARTESIAN_POINT('Ctrl Pts',(82.8689483767477,3.71815190178508,-0.184970261804432));
#15761=CARTESIAN_POINT('Ctrl Pts',(82.8749024030295,3.72369389895084,-0.0735686391838515));
#15762=CARTESIAN_POINT('Ctrl Pts',(82.8808564293114,3.7242287525567,0.0381595187089541));
#15763=CARTESIAN_POINT('Ctrl Pts',(82.8868104555931,3.71973764669685,0.149731099796243));
#15764=CARTESIAN_POINT('Ctrl Pts',(82.8927623812864,3.71524812530526,0.261263318277708));
#15765=CARTESIAN_POINT('Ctrl Pts',(82.8987143069796,3.70573618642912,0.372638654563123));
#15766=CARTESIAN_POINT('Ctrl Pts',(82.9046662326728,3.69123512453875,0.483374407547002));
#15767=CARTESIAN_POINT('Ctrl Pts',(82.9106175133116,3.67673563423614,0.594098159274989));
#15768=CARTESIAN_POINT('Ctrl Pts',(82.9165687939505,3.65724815033154,0.704182053105656));
#15769=CARTESIAN_POINT('Ctrl Pts',(82.9225200745893,3.63285771524098,0.813149668458436));
#15770=CARTESIAN_POINT('Ctrl Pts',(82.9284721648498,3.60846396203706,0.922132107937947));
#15771=CARTESIAN_POINT('Ctrl Pts',(82.9344242551102,3.57916602265238,1.02999756108211));
#15772=CARTESIAN_POINT('Ctrl Pts',(82.9403763453707,3.54509964802525,1.13628167637749));
#15773=CARTESIAN_POINT('Ctrl Pts',(82.9463344547801,3.5109988232179,1.24267327322813));
#15774=CARTESIAN_POINT('Ctrl Pts',(82.9522925641894,3.47212005779636,1.34747994085396));
#15775=CARTESIAN_POINT('Ctrl Pts',(82.9582506735988,3.42864847369204,1.45025418680631));
#15776=CARTESIAN_POINT('Ctrl Pts',(82.9642117746546,3.3851550619239,1.55308003708218));
#15777=CARTESIAN_POINT('Ctrl Pts',(82.9701728757104,3.33706441541386,1.65387105651601));
#15778=CARTESIAN_POINT('Ctrl Pts',(82.9761339767663,3.28460834836788,1.7522030591036));
#15779=CARTESIAN_POINT('Ctrl Pts',(82.9821047966509,3.23206675827321,1.85069537970814));
#15780=CARTESIAN_POINT('Ctrl Pts',(82.9880756165355,3.17514573726857,1.94672031337553));
#15781=CARTESIAN_POINT('Ctrl Pts',(82.9940464364201,3.1141215448209,2.03988101775136));
#15782=CARTESIAN_POINT('Ctrl Pts',(82.9996482265334,3.0568689857869,2.12728387411033));
#15783=CARTESIAN_POINT('Ctrl Pts',(83.0052500166468,2.99600535557949,2.21216566847866));
#15784=CARTESIAN_POINT('Ctrl Pts',(83.0108518067601,2.9317903228427,2.29422602752778));
#15785=CARTESIAN_POINT('Ctrl Pts',(83.0168114313028,2.86347332463906,2.38152828624852));
#15786=CARTESIAN_POINT('Ctrl Pts',(83.0227710558454,2.79114080332129,2.46592032327333));
#15787=CARTESIAN_POINT('Ctrl Pts',(83.0287306803881,2.71506975614864,2.54701075414827));
#15788=CARTESIAN_POINT('Ctrl Pts',(83.0346826412873,2.63909653080748,2.62799690862952));
#15789=CARTESIAN_POINT('Ctrl Pts',(83.0406346021865,2.5593946229042,2.70568959725362));
#15790=CARTESIAN_POINT('Ctrl Pts',(83.0465865630856,2.47628239154729,2.77972895797645));
#15791=CARTESIAN_POINT('Ctrl Pts',(83.0525324962084,2.39325433109783,2.85369333623188));
#15792=CARTESIAN_POINT('Ctrl Pts',(83.0584784293311,2.3068231269795,2.92401146895017));
#15793=CARTESIAN_POINT('Ctrl Pts',(83.0644243624538,2.21734471882464,2.99035950353807));
#15794=CARTESIAN_POINT('Ctrl Pts',(83.0703660317093,2.12793047621776,3.0566599595192));
#15795=CARTESIAN_POINT('Ctrl Pts',(83.0763077009647,2.03547371091488,3.11899573227344));
#15796=CARTESIAN_POINT('Ctrl Pts',(83.0822493702202,1.94036369803259,3.17708298315567));
#15797=CARTESIAN_POINT('Ctrl Pts',(83.0881887801875,1.84528985022724,3.23514814666944));
#15798=CARTESIAN_POINT('Ctrl Pts',(83.0941281901548,1.74756511666116,3.28896778215306));
#15799=CARTESIAN_POINT('Ctrl Pts',(83.1000676001221,1.64760748811742,3.33830153335486));
#15800=CARTESIAN_POINT('Ctrl Pts',(83.1060062208367,1.54766314234405,3.38762872889005));
#15801=CARTESIAN_POINT('Ctrl Pts',(83.1119448415514,1.44548686641152,3.43247104061365));
#15802=CARTESIAN_POINT('Ctrl Pts',(83.1178834622661,1.34152026984447,3.47263458027136));
#15803=CARTESIAN_POINT('Ctrl Pts',(83.1238227627977,1.23754177181821,3.51280271760509));
#15804=CARTESIAN_POINT('Ctrl Pts',(83.1297620633293,1.13177293579743,3.54829086786324));
#15805=CARTESIAN_POINT('Ctrl Pts',(83.1357013638609,1.0246735800673,3.57895398361198));
#15806=CARTESIAN_POINT('Ctrl Pts',(83.1416465568446,0.917467969768757,3.60964752060936));
#15807=CARTESIAN_POINT('Ctrl Pts',(83.1475917498282,0.808929605512165,3.63550634530618));
#15808=CARTESIAN_POINT('Ctrl Pts',(83.1535369428118,0.699531761879276,3.65643581601292));
#15809=CARTESIAN_POINT('Ctrl Pts',(83.1594850391635,0.590080493200947,3.67737550774309));
#15810=CARTESIAN_POINT('Ctrl Pts',(83.1654331355152,0.479769322688583,3.69338098883143));
#15811=CARTESIAN_POINT('Ctrl Pts',(83.1713812318669,0.369078114437835,3.70440938719562));
#15812=CARTESIAN_POINT('Ctrl Pts',(83.1773390334114,0.258206297222685,3.71545578001157));
#15813=CARTESIAN_POINT('Ctrl Pts',(83.183296834956,0.146953621173151,3.72150883900468));
#15814=CARTESIAN_POINT('Ctrl Pts',(83.1892546365005,0.0358019216816396,
3.72257784134918));
#15815=CARTESIAN_POINT('Ctrl Pts',(83.1949813136312,-0.0710378061530395,
3.72360537327234));
#15816=CARTESIAN_POINT('Ctrl Pts',(83.2007079907618,-0.177783918544049,
3.72002841209837));
#15817=CARTESIAN_POINT('Ctrl Pts',(83.2064346678925,-0.284014229770194,
3.711900251864));
#15818=CARTESIAN_POINT('Ctrl Pts',(83.2124015350731,-0.394700085317414,
3.70343117783813));
#15819=CARTESIAN_POINT('Ctrl Pts',(83.2183684022538,-0.505183970064088,
3.68999341159044));
#15820=CARTESIAN_POINT('Ctrl Pts',(83.2243352694345,-0.614985652551647,
3.67160185881525));
#15821=CARTESIAN_POINT('Ctrl Pts',(83.2302951610815,-0.724658971979239,
3.65323180658485));
#15822=CARTESIAN_POINT('Ctrl Pts',(83.2362550527286,-0.833651267434829,
3.62991954790342));
#15823=CARTESIAN_POINT('Ctrl Pts',(83.2422149443756,-0.94148563776353,3.6017318551476));
#15824=CARTESIAN_POINT('Ctrl Pts',(83.2481693307303,-1.04922039894372,3.5735702000277));
#15825=CARTESIAN_POINT('Ctrl Pts',(83.2541237170851,-1.15579896101161,3.54054217004465));
#15826=CARTESIAN_POINT('Ctrl Pts',(83.2600781034398,-1.26075359887706,3.50276575371785));
#15827=CARTESIAN_POINT('Ctrl Pts',(83.2660284500849,-1.36563703104061,3.46501496652278));
#15828=CARTESIAN_POINT('Ctrl Pts',(83.27197879673,-1.46889833964291,3.42252234102821));
#15829=CARTESIAN_POINT('Ctrl Pts',(83.277929143375,-1.570084708551,3.37545575744585));
#15830=CARTESIAN_POINT('Ctrl Pts',(83.2838778657098,-1.67124345586368,3.32840202197873));
#15831=CARTESIAN_POINT('Ctrl Pts',(83.2898265880445,-1.7703280097478,3.27677698055132));
#15832=CARTESIAN_POINT('Ctrl Pts',(83.2957753103792,-1.86690579847718,3.22079653224359));
#15833=CARTESIAN_POINT('Ctrl Pts',(83.3017228809011,-1.96346488747049,3.16482692307001));
#15834=CARTESIAN_POINT('Ctrl Pts',(83.307670451423,-2.05751781852964,3.10450379698923));
#15835=CARTESIAN_POINT('Ctrl Pts',(83.3136180219449,-2.14865776894596,3.04008837938113));
#15836=CARTESIAN_POINT('Ctrl Pts',(83.3195682478411,-2.23983841004109,2.97564420262782));
#15837=CARTESIAN_POINT('Ctrl Pts',(83.3255184737372,-2.32810313115278,2.907104324154));
#15838=CARTESIAN_POINT('Ctrl Pts',(83.3314686996334,-2.41307535751767,2.83477245673105));
#15839=CARTESIAN_POINT('Ctrl Pts',(83.3364941112922,-2.48484077020848,2.77368277439161));
#15840=CARTESIAN_POINT('Ctrl Pts',(83.3415195229509,-2.55425805754174,2.70988905418821));
#15841=CARTESIAN_POINT('Ctrl Pts',(83.3465449346096,-2.62112000711956,2.64359555733806));
#15842=CARTESIAN_POINT('',(82.4430005297901,2.16151778945158,-3.03095833168065));
#15843=CARTESIAN_POINT('Origin',(82.4430005297901,0.,0.));
#15844=CARTESIAN_POINT('Ctrl Pts',(82.4430005297901,2.16151778945147,-3.03095833168073));
#15845=CARTESIAN_POINT('Ctrl Pts',(82.4497525870341,2.26438712551953,-2.9575974089732));
#15846=CARTESIAN_POINT('Ctrl Pts',(82.4565046442782,2.36346172388708,-2.87903694463822));
#15847=CARTESIAN_POINT('Ctrl Pts',(82.4632567015222,2.45826699999897,-2.79567360741844));
#15848=CARTESIAN_POINT('Ctrl Pts',(82.4700154581067,2.55316634119397,-2.71222755772141));
#15849=CARTESIAN_POINT('Ctrl Pts',(82.4767742146913,2.64378773851266,-2.62396924669582));
#15850=CARTESIAN_POINT('Ctrl Pts',(82.4835329712758,2.72969125339154,-2.53133427734421));
#15851=CARTESIAN_POINT('Ctrl Pts',(82.4902898152388,2.81557045893036,-2.43872552222812));
#15852=CARTESIAN_POINT('Ctrl Pts',(82.4970466592018,2.89673431317573,-2.3417427375673));
#15853=CARTESIAN_POINT('Ctrl Pts',(82.5038035031648,2.97278138998534,-2.24085661519358));
#15854=CARTESIAN_POINT('Ctrl Pts',(82.510548629069,3.04869658212802,-2.14014545460938));
#15855=CARTESIAN_POINT('Ctrl Pts',(82.5172937549732,3.11951259794815,-2.03554464175841));
#15856=CARTESIAN_POINT('Ctrl Pts',(82.5240388808774,3.18487011231051,-1.9275554285704));
#15857=CARTESIAN_POINT('Ctrl Pts',(82.5296232407037,3.2389802775964,-1.83815003683076));
#15858=CARTESIAN_POINT('Ctrl Pts',(82.53520760053,3.28934967007504,-1.74642274789237));
#15859=CARTESIAN_POINT('Ctrl Pts',(82.5407919603563,3.33579618241313,-1.65267401259232));
#15860=CARTESIAN_POINT('Ctrl Pts',(82.5468159793767,3.38589944983491,-1.55154439663748));
#15861=CARTESIAN_POINT('Ctrl Pts',(82.5528399983971,3.43141471863513,-1.44810467648933));
#15862=CARTESIAN_POINT('Ctrl Pts',(82.5588640174175,3.47213824854727,-1.34280435859998));
#15863=CARTESIAN_POINT('Ctrl Pts',(82.5648874941942,3.51285811278705,-1.23751351917344));
#15864=CARTESIAN_POINT('Ctrl Pts',(82.5709109709708,3.54878695248395,-1.13036279259719));
#15865=CARTESIAN_POINT('Ctrl Pts',(82.5769344477475,3.57976955737609,-1.02182066850469));
#15866=CARTESIAN_POINT('Ctrl Pts',(82.5829609225814,3.61076758319991,-0.913224519881831));
#15867=CARTESIAN_POINT('Ctrl Pts',(82.5889873974153,3.63681434419998,-0.803235978819984));
#15868=CARTESIAN_POINT('Ctrl Pts',(82.5950138722492,3.65780483342544,-0.692337607724339));
#15869=CARTESIAN_POINT('Ctrl Pts',(82.6010420246523,3.67880116570166,-0.581408366228167));
#15870=CARTESIAN_POINT('Ctrl Pts',(82.6070701770554,3.69473835749882,-0.469569189038235));
#15871=CARTESIAN_POINT('Ctrl Pts',(82.6130983294586,3.70556295161657,-0.357310472987701));
#15872=CARTESIAN_POINT('Ctrl Pts',(82.6191321312306,3.71639769015704,-0.244946552080748));
#15873=CARTESIAN_POINT('Ctrl Pts',(82.6251659330027,3.72211023554301,-0.132162710340014));
#15874=CARTESIAN_POINT('Ctrl Pts',(82.6311997347748,3.72269917905029,-0.019452115522899));
#15875=CARTESIAN_POINT('Ctrl Pts',(82.6336609534907,3.7229394121301,0.0265231146751369));
#15876=CARTESIAN_POINT('Ctrl Pts',(82.6361221722066,3.72232774982774,0.0724861757607506));
#15877=CARTESIAN_POINT('Ctrl Pts',(82.6385833909225,3.72086658053853,0.118403768231767));
#15878=CARTESIAN_POINT('Ctrl Pts',(82.6446179854142,3.71728397973704,0.230987850586364));
#15879=CARTESIAN_POINT('Ctrl Pts',(82.650652579906,3.70858350729485,0.343527835818447));
#15880=CARTESIAN_POINT('Ctrl Pts',(82.6566871743978,3.69477453776741,0.455531203723344));
#15881=CARTESIAN_POINT('Ctrl Pts',(82.6627163739924,3.68097791338929,0.56743444118052));
#15882=CARTESIAN_POINT('Ctrl Pts',(82.668745573587,3.66208193039216,0.67880161720003));
#15883=CARTESIAN_POINT('Ctrl Pts',(82.6747747731817,3.63814792340125,0.789143364637372));
#15884=CARTESIAN_POINT('Ctrl Pts',(82.6808000674154,3.61422941945254,0.899413639179759));
#15885=CARTESIAN_POINT('Ctrl Pts',(82.6868253616491,3.58527947302877,1.00865941394278));
#15886=CARTESIAN_POINT('Ctrl Pts',(82.6928506558828,3.55141075192741,1.11640012253422));
#15887=CARTESIAN_POINT('Ctrl Pts',(82.69887449913,3.5175501869521,1.22411488545155));
#15888=CARTESIAN_POINT('Ctrl Pts',(82.7048983423771,3.47877331924376,1.33032491694052));
#15889=CARTESIAN_POINT('Ctrl Pts',(82.7109221856242,3.43524298274324,1.4345637706332));
#15890=CARTESIAN_POINT('Ctrl Pts',(82.716945436337,3.39171692809766,1.53879237088688));
#15891=CARTESIAN_POINT('Ctrl Pts',(82.7229686870497,3.34343848993966,1.64104980643127));
#15892=CARTESIAN_POINT('Ctrl Pts',(82.7289919377624,3.29061879767597,1.74088928162635));
#15893=CARTESIAN_POINT('Ctrl Pts',(82.7350159406708,3.2377925091827,1.84074122497626));
#15894=CARTESIAN_POINT('Ctrl Pts',(82.7410399435792,3.18042402656934,1.93817425007928));
#15895=CARTESIAN_POINT('Ctrl Pts',(82.7470639464876,3.11877033253438,2.0327663848567));
#15896=CARTESIAN_POINT('Ctrl Pts',(82.7530900465796,3.05709517451287,2.12739145073972));
#15897=CARTESIAN_POINT('Ctrl Pts',(82.7591161466717,2.99113205645184,2.21917331991592));
#15898=CARTESIAN_POINT('Ctrl Pts',(82.7651422467637,2.92118080661426,2.30771970948997));
#15899=CARTESIAN_POINT('Ctrl Pts',(82.7711758693073,2.8511422358097,2.3963766325624));
#15900=CARTESIAN_POINT('Ctrl Pts',(82.7772094918508,2.77710583986882,2.48178969136247));
#15901=CARTESIAN_POINT('Ctrl Pts',(82.7832431143944,2.69941145893569,2.56360007369845));
#15902=CARTESIAN_POINT('Ctrl Pts',(82.7892806497584,2.62166669298755,2.64546351028742));
#15903=CARTESIAN_POINT('Ctrl Pts',(82.7953181851224,2.54025950511836,2.72371933435787));
#15904=CARTESIAN_POINT('Ctrl Pts',(82.8013557204864,2.45556495511912,2.79804723221229));
#15905=CARTESIAN_POINT('Ctrl Pts',(82.807403681777,2.37072415021567,2.87250348330291));
#15906=CARTESIAN_POINT('Ctrl Pts',(82.8134516430675,2.28258495469221,2.9430180013515));
#15907=CARTESIAN_POINT('Ctrl Pts',(82.8194996043581,2.19155420785852,3.00931183437636));
#15908=CARTESIAN_POINT('Ctrl Pts',(82.8243884869237,2.11796930713768,3.0629005974176));
#15909=CARTESIAN_POINT('Ctrl Pts',(82.8292773694893,2.04249561614066,3.11373220542137));
#15910=CARTESIAN_POINT('Ctrl Pts',(82.8341662520549,1.9653598929364,3.16168120684819));
#15911=CARTESIAN_POINT('Ctrl Pts',(82.8400765136812,1.87210907360204,3.21964765201231));
#15912=CARTESIAN_POINT('Ctrl Pts',(82.8459867753075,1.77611037840658,3.27359751554604));
#15913=CARTESIAN_POINT('Ctrl Pts',(82.8518970369338,1.67774758116333,3.32325602630923));
#15914=CARTESIAN_POINT('Ctrl Pts',(82.8577989521669,1.57952369055903,3.3728444099815));
#15915=CARTESIAN_POINT('Ctrl Pts',(82.8637008674001,1.47894270954516,3.41815329597526));
#15916=CARTESIAN_POINT('Ctrl Pts',(82.8696027826332,1.37641727118754,3.4589511499986));
#15917=CARTESIAN_POINT('Ctrl Pts',(82.875498048588,1.27400734112691,3.49970303991084));
#15918=CARTESIAN_POINT('Ctrl Pts',(82.8813933145428,1.16965770180484,3.53595384502219));
#15919=CARTESIAN_POINT('Ctrl Pts',(82.8872885804976,1.06380471935477,3.56751833654412));
#15920=CARTESIAN_POINT('Ctrl Pts',(82.8932244360264,0.957222927129104,3.59930015316592));
#15921=CARTESIAN_POINT('Ctrl Pts',(82.8991602915551,0.849117397594608,3.62633067152118));
#15922=CARTESIAN_POINT('Ctrl Pts',(82.9050961470838,0.739953470235613,3.64847042257249));
#15923=CARTESIAN_POINT('Ctrl Pts',(82.9109836667738,0.631678467811638,3.67042988900744));
#15924=CARTESIAN_POINT('Ctrl Pts',(82.9168711864638,0.522362667208827,3.68757786662143));
#15925=CARTESIAN_POINT('Ctrl Pts',(82.9227587061538,0.412473493400228,3.69982880411273));
#15926=CARTESIAN_POINT('Ctrl Pts',(82.9286450490054,0.302606285004335,3.7120772928014));
#15927=CARTESIAN_POINT('Ctrl Pts',(82.9345313918569,0.192166354445299,3.71943063976913));
#15928=CARTESIAN_POINT('Ctrl Pts',(82.9404177347085,0.0816278908404526,
3.72185497432892));
#15929=CARTESIAN_POINT('Ctrl Pts',(82.9463044212326,-0.0289170265228388,
3.72427945043284));
#15930=CARTESIAN_POINT('Ctrl Pts',(82.9521911077568,-0.139560062392199,
3.72177433367711));
#15931=CARTESIAN_POINT('Ctrl Pts',(82.9580777942809,-0.249826264947155,
3.71435787180538));
#15932=CARTESIAN_POINT('Ctrl Pts',(82.9640504041897,-0.361701937499702,
3.70683315760796));
#15933=CARTESIAN_POINT('Ctrl Pts',(82.9700230140986,-0.473189236914967,
3.69425260232078));
#15934=CARTESIAN_POINT('Ctrl Pts',(82.9759956240075,-0.583798126309067,
3.67668972177665));
#15935=CARTESIAN_POINT('Ctrl Pts',(82.9818907079216,-0.692971284204131,
3.65935481188613));
#15936=CARTESIAN_POINT('Ctrl Pts',(82.9877857918357,-0.801288292914002,
3.63716630404435));
#15937=CARTESIAN_POINT('Ctrl Pts',(82.9936808757498,-0.908290114054953,
3.61024606241874));
#15938=CARTESIAN_POINT('Ctrl Pts',(82.999692248656,-1.01740269971021,3.58279478038529));
#15939=CARTESIAN_POINT('Ctrl Pts',(83.0057036215623,-1.12514721360662,3.55042324853487));
#15940=CARTESIAN_POINT('Ctrl Pts',(83.0117149944685,-1.23105640664389,3.51331292175363));
#15941=CARTESIAN_POINT('Ctrl Pts',(83.0177263673747,-1.33696559968117,3.47620259497239));
#15942=CARTESIAN_POINT('Ctrl Pts',(83.023737740281,-1.44103906794508,3.43435370796953));
#15943=CARTESIAN_POINT('Ctrl Pts',(83.0297491131872,-1.542835502784,3.38799736922112));
#15944=CARTESIAN_POINT('Ctrl Pts',(83.0357287047233,-1.64409375271539,3.34188611058699));
#15945=CARTESIAN_POINT('Ctrl Pts',(83.0417082962595,-1.74343945101141,3.29116017750618));
#15946=CARTESIAN_POINT('Ctrl Pts',(83.0476878877956,-1.84042560292446,3.23600079768225));
#15947=CARTESIAN_POINT('Ctrl Pts',(83.0536609650252,-1.93730609586108,3.18090150977348));
#15948=CARTESIAN_POINT('Ctrl Pts',(83.0596340422548,-2.03183179406103,3.1213785772606));
#15949=CARTESIAN_POINT('Ctrl Pts',(83.0656071194844,-2.12357676031699,3.05766075710527));
#15950=CARTESIAN_POINT('Ctrl Pts',(83.0715742291671,-2.21523006655029,2.99400659577591));
#15951=CARTESIAN_POINT('Ctrl Pts',(83.0775413388497,-2.30410782960365,2.9261661202019));
#15952=CARTESIAN_POINT('Ctrl Pts',(83.0835084485324,-2.3898105926219,2.85441288076763));
#15953=CARTESIAN_POINT('Ctrl Pts',(83.0890762444753,-2.46977820200121,2.78746130510422));
#15954=CARTESIAN_POINT('Ctrl Pts',(83.0946440404181,-2.54698154549054,2.71710370215753));
#15955=CARTESIAN_POINT('Ctrl Pts',(83.100211836361,-2.62112000711957,2.64359555733806));
#15956=CARTESIAN_POINT('Origin',(80.1322559480305,0.,0.));
#15957=CARTESIAN_POINT('',(84.5967274725783,-2.62112000711956,2.64359555733807));
#15958=CARTESIAN_POINT('',(84.3497092113127,-2.62112002533987,2.64359553927266));
#15959=CARTESIAN_POINT('',(80.1322559480305,-2.62112000711956,2.64359555733806));
#15960=CARTESIAN_POINT('',(83.5037451115797,-3.72274997864689,-0.000398728739238651));
#15961=CARTESIAN_POINT('Ctrl Pts',(83.5037451115797,-3.72274997864689,-0.00039872873923823));
#15962=CARTESIAN_POINT('Ctrl Pts',(83.5100196206599,-3.72273733869349,-0.118412259214994));
#15963=CARTESIAN_POINT('Ctrl Pts',(83.51629412974,-3.71710876285587,-0.236304017798562));
#15964=CARTESIAN_POINT('Ctrl Pts',(83.5225686388201,-3.70592449650868,-0.353540929281022));
#15965=CARTESIAN_POINT('Ctrl Pts',(83.5288611095432,-3.69470821366485,-0.471113447504741));
#15966=CARTESIAN_POINT('Ctrl Pts',(83.5351535802664,-3.67790446628232,-0.588027026941602));
#15967=CARTESIAN_POINT('Ctrl Pts',(83.5414460509894,-3.65562518860896,-0.703755669893829));
#15968=CARTESIAN_POINT('Ctrl Pts',(83.5477474655781,-3.63331424406364,-0.819648804898809));
#15969=CARTESIAN_POINT('Ctrl Pts',(83.5540488801668,-3.60551231776947,-0.934353309309916));
#15970=CARTESIAN_POINT('Ctrl Pts',(83.5603502947555,-3.57238150868199,-1.04735758885255));
#15971=CARTESIAN_POINT('Ctrl Pts',(83.5666688213221,-3.53916073032393,-1.16066874024292));
#15972=CARTESIAN_POINT('Ctrl Pts',(83.5729873478887,-3.5005822350553,-1.2722701059141));
#15973=CARTESIAN_POINT('Ctrl Pts',(83.5793058744553,-3.4568573355477,-1.38166744340672));
#15974=CARTESIAN_POINT('Ctrl Pts',(83.5854040463559,-3.41465731458977,-1.4872496171091));
#15975=CARTESIAN_POINT('Ctrl Pts',(83.5915022182565,-3.36766400046035,-1.59077869702065));
#15976=CARTESIAN_POINT('Ctrl Pts',(83.5976003901571,-3.31610731420533,-1.69183327877598));
#15977=CARTESIAN_POINT('Ctrl Pts',(83.6035656848774,-3.26567403135889,-1.79068591409443));
#15978=CARTESIAN_POINT('Ctrl Pts',(83.6095309795976,-3.21073524337409,-1.88744121534554));
#15979=CARTESIAN_POINT('Ctrl Pts',(83.6154962743178,-3.15148926053915,-1.98166167728158));
#15980=CARTESIAN_POINT('Ctrl Pts',(83.6214539899425,-3.09231855159846,-2.07576242914194));
#15981=CARTESIAN_POINT('Ctrl Pts',(83.6274117055672,-3.02885175060343,-2.16733439615148));
#15982=CARTESIAN_POINT('Ctrl Pts',(83.6333694211919,-2.96133374140531,-2.25596321656946));
#15983=CARTESIAN_POINT('Ctrl Pts',(83.6393211856149,-2.89388317639428,-2.34450350507104));
#15984=CARTESIAN_POINT('Ctrl Pts',(83.645272950038,-2.82238970387071,-2.43010616471014));
#15985=CARTESIAN_POINT('Ctrl Pts',(83.6512247144611,-2.74714192160807,-2.51238508693303));
#15986=CARTESIAN_POINT('Ctrl Pts',(83.6571723075251,-2.67194687757433,-2.59460634307591));
#15987=CARTESIAN_POINT('Ctrl Pts',(83.6631199005891,-2.59300303846704,-2.67350818876696));
#15988=CARTESIAN_POINT('Ctrl Pts',(83.6690674936532,-2.51063931632746,-2.74873748943233));
#15989=CARTESIAN_POINT('Ctrl Pts',(83.6750128818184,-2.42830612816521,-2.82393890100162));
#15990=CARTESIAN_POINT('Ctrl Pts',(83.6809582699837,-2.34255588496676,-2.89547019330391));
#15991=CARTESIAN_POINT('Ctrl Pts',(83.6869036581489,-2.25375393754337,-2.96301548283295));
#15992=CARTESIAN_POINT('Ctrl Pts',(83.6928483045751,-2.16496306893846,-3.03055234549722));
#15993=CARTESIAN_POINT('Ctrl Pts',(83.6987929510012,-2.07312158516433,-3.0941039419349));
#15994=CARTESIAN_POINT('Ctrl Pts',(83.7047375974274,-1.97862684690804,-3.15339552913915));
#15995=CARTESIAN_POINT('Ctrl Pts',(83.7106829643435,-1.88412065590747,-3.21269430247247));
#15996=CARTESIAN_POINT('Ctrl Pts',(83.7166283312597,-1.78696092457647,-3.26773181874748));
#15997=CARTESIAN_POINT('Ctrl Pts',(83.7225736981759,-1.68757217285197,-3.31827782500436));
#15998=CARTESIAN_POINT('Ctrl Pts',(83.7285249846558,-1.58808446372736,-3.36887415789559));
#15999=CARTESIAN_POINT('Ctrl Pts',(83.7344762711357,-1.48636367330883,-3.41496985803524));
#16000=CARTESIAN_POINT('Ctrl Pts',(83.7404275576156,-1.3828571226216,-3.45638159654207));
#16001=CARTESIAN_POINT('Ctrl Pts',(83.7463817713833,-1.27929965967314,-3.49781370443842));
#16002=CARTESIAN_POINT('Ctrl Pts',(83.7523359851509,-1.17395508017414,-3.53455712242865));
#16003=CARTESIAN_POINT('Ctrl Pts',(83.7582901989185,-1.0672870366516,-3.56647808683797));
#16004=CARTESIAN_POINT('Ctrl Pts',(83.7642540941447,-0.960445552555769,
-3.59845095423703));
#16005=CARTESIAN_POINT('Ctrl Pts',(83.770217989371,-0.852276709261824,-3.62558559676572));
#16006=CARTESIAN_POINT('Ctrl Pts',(83.7761818845972,-0.743256032909034,
-3.64779906684076));
#16007=CARTESIAN_POINT('Ctrl Pts',(83.781849006828,-0.63966040033416,-3.66890715900358));
#16008=CARTESIAN_POINT('Ctrl Pts',(83.7875161290588,-0.535295977888283,
-3.68557203647516));
#16009=CARTESIAN_POINT('Ctrl Pts',(83.7931832512895,-0.430573663541631,
-3.69776606652778));
#16010=CARTESIAN_POINT('Ctrl Pts',(83.7991495636772,-0.320322637374219,
-3.71060386843089));
#16011=CARTESIAN_POINT('Ctrl Pts',(83.805115876065,-0.209319446371947,-3.71852726417688));
#16012=CARTESIAN_POINT('Ctrl Pts',(83.8110821884527,-0.0980383235348542,
-3.72145886039581));
#16013=CARTESIAN_POINT('Ctrl Pts',(83.8170409367009,0.013101716186779,-3.72438673991313));
#16014=CARTESIAN_POINT('Ctrl Pts',(83.8229996849491,0.124518573731149,-3.72233539448482));
#16015=CARTESIAN_POINT('Ctrl Pts',(83.8289584331973,0.2357314749135,-3.71527902508481));
#16016=CARTESIAN_POINT('Ctrl Pts',(83.8349112437453,0.346833556029731,-3.70822968712912));
#16017=CARTESIAN_POINT('Ctrl Pts',(83.8408640542932,0.457731671199903,-3.69618527171105));
#16018=CARTESIAN_POINT('Ctrl Pts',(83.8468168648411,0.567944340902615,-3.67917202480894));
#16019=CARTESIAN_POINT('Ctrl Pts',(83.8527655202028,0.678080079856902,-3.66217065350897));
#16020=CARTESIAN_POINT('Ctrl Pts',(83.8587141755644,0.787530914333091,-3.64020741337706));
#16021=CARTESIAN_POINT('Ctrl Pts',(83.8646628309261,0.895820469822217,-3.61336038174267));
#16022=CARTESIAN_POINT('Ctrl Pts',(83.8706092908679,1.00407005980229,-3.58652325831485));
#16023=CARTESIAN_POINT('Ctrl Pts',(83.8765557508097,1.11115881871125,-3.5548060268469));
#16024=CARTESIAN_POINT('Ctrl Pts',(83.8825022107516,1.21662118406317,-3.5183377406083));
#16025=CARTESIAN_POINT('Ctrl Pts',(83.8884479371757,1.32207054024423,-3.48187395286702));
#16026=CARTESIAN_POINT('Ctrl Pts',(83.8943936635997,1.42589350793631,-3.44066041211545));
#16027=CARTESIAN_POINT('Ctrl Pts',(83.9003393900238,1.52764102649755,-3.39487561725927));
#16028=CARTESIAN_POINT('Ctrl Pts',(83.9062858439079,1.62940099387302,-3.34908522063104));
#16029=CARTESIAN_POINT('Ctrl Pts',(83.9122322977919,1.72908462725492,-3.29872262936565));
#16030=CARTESIAN_POINT('Ctrl Pts',(83.918178751676,1.82626484219466,-3.24401360796525));
#16031=CARTESIAN_POINT('Ctrl Pts',(83.9241311294265,1.92354186821385,-3.18925008535366));
#16032=CARTESIAN_POINT('Ctrl Pts',(83.930083507177,2.01831012997369,-3.130131688067));
#16033=CARTESIAN_POINT('Ctrl Pts',(83.9360358849275,2.11016895898102,-3.06692916890054));
#16034=CARTESIAN_POINT('Ctrl Pts',(83.9419911939282,2.20207302389456,-3.00369552563572));
#16035=CARTESIAN_POINT('Ctrl Pts',(83.9479465029288,2.29106446846605,-2.93637400447061));
#16036=CARTESIAN_POINT('Ctrl Pts',(83.9539018119295,2.3767748226723,-2.86527642729477));
#16037=CARTESIAN_POINT('Ctrl Pts',(83.9598667975774,2.46262444570119,-2.7940633252683));
#16038=CARTESIAN_POINT('Ctrl Pts',(83.9658317832255,2.54518201527315,-2.71906218676769));
#16039=CARTESIAN_POINT('Ctrl Pts',(83.9717967688734,2.62411477163207,-2.64062288632859));
#16040=CARTESIAN_POINT('Ctrl Pts',(83.9774532167229,2.69896474551428,-2.56624084444844));
#16041=CARTESIAN_POINT('Ctrl Pts',(83.9831096645724,2.77055530768488,-2.48876764338392));
#16042=CARTESIAN_POINT('Ctrl Pts',(83.9887661124219,2.83863709197814,-2.40852797836062));
#16043=CARTESIAN_POINT('Ctrl Pts',(83.9947321230154,2.91044481603531,-2.32389700424257));
#16044=CARTESIAN_POINT('Ctrl Pts',(84.0006981336089,2.97858019832519,-2.23591555189983));
#16045=CARTESIAN_POINT('Ctrl Pts',(84.0066641442025,3.04271589798734,-2.14493531991878));
#16046=CARTESIAN_POINT('Ctrl Pts',(84.0126225879999,3.10677025321431,-2.0540704797651));
#16047=CARTESIAN_POINT('Ctrl Pts',(84.0185810317973,3.1668347757237,-1.9602147615424));
#16048=CARTESIAN_POINT('Ctrl Pts',(84.0245394755947,3.22262143274553,-1.86375391715461));
#16049=CARTESIAN_POINT('Ctrl Pts',(84.0304919794575,3.27835247640454,-1.76738923396779));
#16050=CARTESIAN_POINT('Ctrl Pts',(84.0364444833203,3.32981392953477,-1.66842494932434));
#16051=CARTESIAN_POINT('Ctrl Pts',(84.0423969871831,3.37676067896021,-1.56727626139369));
#16052=CARTESIAN_POINT('Ctrl Pts',(84.0483453337523,3.42367464026426,-1.46619821680893));
#16053=CARTESIAN_POINT('Ctrl Pts',(84.0542936803215,3.46607999504213,-1.3629391807151));
#16054=CARTESIAN_POINT('Ctrl Pts',(84.0602420268907,3.50377759415442,-1.25793884318811));
#16055=CARTESIAN_POINT('Ctrl Pts',(84.0661881768666,3.54146127237411,-1.15297727997188));
#16056=CARTESIAN_POINT('Ctrl Pts',(84.0721343268425,3.57444051035109,-1.04627608558645));
#16057=CARTESIAN_POINT('Ctrl Pts',(84.0780804768184,3.60256457584799,-0.938294217900349));
#16058=CARTESIAN_POINT('Ctrl Pts',(84.084025892473,3.63068516815607,-0.830325685463184));
#16059=CARTESIAN_POINT('Ctrl Pts',(84.0899713081276,3.65395167536634,-0.721077197666321));
#16060=CARTESIAN_POINT('Ctrl Pts',(84.0959167237821,3.67226366375991,-0.61102139596633));
#16061=CARTESIAN_POINT('Ctrl Pts',(84.1018628664623,3.69057789140544,-0.500952136270207));
#16062=CARTESIAN_POINT('Ctrl Pts',(84.1078090091424,3.70393632765888,-0.390075777745001));
#16063=CARTESIAN_POINT('Ctrl Pts',(84.1137551518225,3.71229005859827,-0.278872880238347));
#16064=CARTESIAN_POINT('Ctrl Pts',(84.1197072196245,3.72065211373654,-0.167559172958134));
#16065=CARTESIAN_POINT('Ctrl Pts',(84.1256592874266,3.72399947021162,-0.0559186932835599));
#16066=CARTESIAN_POINT('Ctrl Pts',(84.1316113552286,3.72233530045396,0.0555650384174694));
#16067=CARTESIAN_POINT('Ctrl Pts',(84.1375663545071,3.72067031106946,0.167103677412746));
#16068=CARTESIAN_POINT('Ctrl Pts',(84.1435213537856,3.7139889021167,0.278484998212509));
#16069=CARTESIAN_POINT('Ctrl Pts',(84.1494763530642,3.70234627688846,0.38922950621725));
#16070=CARTESIAN_POINT('Ctrl Pts',(84.1554410326672,3.69068472564788,0.500154038218728));
#16071=CARTESIAN_POINT('Ctrl Pts',(84.1614057122701,3.67404590390891,0.610439275807124));
#16072=CARTESIAN_POINT('Ctrl Pts',(84.1673703918731,3.65253648259817,0.719614345180374));
#16073=CARTESIAN_POINT('Ctrl Pts',(84.1730299191002,3.63212748100068,0.823204029582159));
#16074=CARTESIAN_POINT('Ctrl Pts',(84.1786894463272,3.60733398724194,0.925794034213578));
#16075=CARTESIAN_POINT('Ctrl Pts',(84.1843489735542,3.57828820258272,1.02699615469453));
#16076=CARTESIAN_POINT('Ctrl Pts',(84.1903149038667,3.54766989822665,1.1336772914832));
#16077=CARTESIAN_POINT('Ctrl Pts',(84.1962808341792,3.51222729159586,1.23915996827174));
#16078=CARTESIAN_POINT('Ctrl Pts',(84.2022467644917,3.47207156306853,1.34297677695144));
#16079=CARTESIAN_POINT('Ctrl Pts',(84.2082051258581,3.4319667799146,1.44666187376142));
#16080=CARTESIAN_POINT('Ctrl Pts',(84.2141634872244,3.38716091515584,1.54868491978055));
#16081=CARTESIAN_POINT('Ctrl Pts',(84.2201218485908,3.33781528368355,1.64859233727095));
#16082=CARTESIAN_POINT('Ctrl Pts',(84.2260742679927,3.28851886204741,1.74840012228129));
#16083=CARTESIAN_POINT('Ctrl Pts',(84.2320266873946,3.23469186245655,1.84609610348638));
#16084=CARTESIAN_POINT('Ctrl Pts',(84.2379791067965,3.17654390277376,1.94124609368592));
#16085=CARTESIAN_POINT('Ctrl Pts',(84.2439273661645,3.11843658160552,2.03632958534823));
#16086=CARTESIAN_POINT('Ctrl Pts',(84.2498756255326,3.05601452415942,2.12887027078323));
#16087=CARTESIAN_POINT('Ctrl Pts',(84.2558238849006,2.98953321612768,2.21845863431557));
#16088=CARTESIAN_POINT('Ctrl Pts',(84.2617699460361,2.92307647685909,2.30801388966532));
#16089=CARTESIAN_POINT('Ctrl Pts',(84.2677160071716,2.85256371746134,2.39461865776034));
#16090=CARTESIAN_POINT('Ctrl Pts',(84.273662068307,2.77829330399252,2.47789303229384));
#16091=CARTESIAN_POINT('Ctrl Pts',(84.2796073935833,2.7040320819134,2.5611571011458));
#16092=CARTESIAN_POINT('Ctrl Pts',(84.2855527188597,2.62601440807823,2.64109128500481));
#16093=CARTESIAN_POINT('Ctrl Pts',(84.291498044136,2.54457792489982,2.71734994923593));
#16094=CARTESIAN_POINT('Ctrl Pts',(84.2974440950003,2.46313150293226,2.79361792033734));
#16095=CARTESIAN_POINT('Ctrl Pts',(84.3033901458646,2.37826574669442,2.86620919527541));
#16096=CARTESIAN_POINT('Ctrl Pts',(84.3093361967289,2.2903534541501,2.9348166241799));
#16097=CARTESIAN_POINT('Ctrl Pts',(84.3152881710003,2.20235358410068,3.0034923992426));
#16098=CARTESIAN_POINT('Ctrl Pts',(84.3212401452717,2.1113014445005,3.06817614342487));
#16099=CARTESIAN_POINT('Ctrl Pts',(84.3271921195431,2.01760117679494,3.12860241224348));
#16100=CARTESIAN_POINT('Ctrl Pts',(84.3331470242174,1.92385477657584,3.18905843141106));
#16101=CARTESIAN_POINT('Ctrl Pts',(84.3391019288917,1.82745801067643,3.24525258830528));
#16102=CARTESIAN_POINT('Ctrl Pts',(84.345056833566,1.72884051915109,3.2969649712791));
#16103=CARTESIAN_POINT('Ctrl Pts',(84.3510214177228,1.63006272845468,3.34876141086394));
#16104=CARTESIAN_POINT('Ctrl Pts',(84.3569860018796,1.52905737681446,3.39606134140062));
#16105=CARTESIAN_POINT('Ctrl Pts',(84.3629505860364,1.42627546643135,3.43869246318365));
#16106=CARTESIAN_POINT('Ctrl Pts',(84.3686110022531,1.32873498799592,3.47914958252942));
#16107=CARTESIAN_POINT('Ctrl Pts',(84.3742714184699,1.22959496450997,3.51540223207884));
#16108=CARTESIAN_POINT('Ctrl Pts',(84.3799318346867,1.12925196292743,3.54734514344524));
#16109=CARTESIAN_POINT('Ctrl Pts',(84.3858978809983,1.0234910132782,3.5810127892939));
#16110=CARTESIAN_POINT('Ctrl Pts',(84.39186392731,0.91605267053247,3.61000083033015));
#16111=CARTESIAN_POINT('Ctrl Pts',(84.3978299736217,0.807387589059532,3.63414265591386));
#16112=CARTESIAN_POINT('Ctrl Pts',(84.4037884527917,0.698860334888818,3.65825386078072));
#16113=CARTESIAN_POINT('Ctrl Pts',(84.4097469319616,0.589109839862022,3.67753098430548));
#16114=CARTESIAN_POINT('Ctrl Pts',(84.4157054111316,0.478603042662136,3.6918568079023));
#16115=CARTESIAN_POINT('Ctrl Pts',(84.4216579499752,0.368206415596873,3.70616834931961));
#16116=CARTESIAN_POINT('Ctrl Pts',(84.4276104888187,0.257055397390509,3.71553835602055));
#16117=CARTESIAN_POINT('Ctrl Pts',(84.4335630276622,0.145627568430018,3.71990055966731));
#16118=CARTESIAN_POINT('Ctrl Pts',(84.4395114084652,0.0342775754051283,
3.724259716174));
#16119=CARTESIAN_POINT('Ctrl Pts',(84.4454597892681,-0.077348428395596,
3.72361801180684));
#16120=CARTESIAN_POINT('Ctrl Pts',(84.4514081700711,-0.188767965640915,
3.71796102960316));
#16121=CARTESIAN_POINT('Ctrl Pts',(84.4573543538131,-0.300146349583368,
3.71230613683108));
#16122=CARTESIAN_POINT('Ctrl Pts',(84.4633005375551,-0.411318002711453,
3.70163966999279));
#16123=CARTESIAN_POINT('Ctrl Pts',(84.4692467212971,-0.52180131642087,3.68599931479666));
#16124=CARTESIAN_POINT('Ctrl Pts',(84.4751921702078,-0.632270976566676,
3.67036089244068));
#16125=CARTESIAN_POINT('Ctrl Pts',(84.4811376191185,-0.742052053729621,
3.6497498626038));
#16126=CARTESIAN_POINT('Ctrl Pts',(84.4870830680292,-0.850669686046545,
3.62425559911846));
#16127=CARTESIAN_POINT('Ctrl Pts',(84.4930292434128,-0.959300590324678,
3.59875822049546));
#16128=CARTESIAN_POINT('Ctrl Pts',(84.4989754187964,-1.06676736130999,3.56837651758695));
#16129=CARTESIAN_POINT('Ctrl Pts',(84.50492159418,-1.17260767456877,3.53325045871962));
#16130=CARTESIAN_POINT('Ctrl Pts',(84.510873693601,-1.2785534340902,3.4980894045701));
#16131=CARTESIAN_POINT('Ctrl Pts',(84.516825793022,-1.38286910249047,3.45817468400298));
#16132=CARTESIAN_POINT('Ctrl Pts',(84.522777892443,-1.48510968634047,3.41369547294976));
#16133=CARTESIAN_POINT('Ctrl Pts',(84.5287329227958,-1.58740061548134,3.36919435945102));
#16134=CARTESIAN_POINT('Ctrl Pts',(84.5346879531485,-1.68761404933881,3.32012446016647));
#16135=CARTESIAN_POINT('Ctrl Pts',(84.5406429835013,-1.78532875113122,3.26672141647926));
#16136=CARTESIAN_POINT('Ctrl Pts',(84.5466076929119,-1.88320227432364,3.2132315737126));
#16137=CARTESIAN_POINT('Ctrl Pts',(84.5525724023226,-1.97856859235349,3.15539472877556));
#16138=CARTESIAN_POINT('Ctrl Pts',(84.5585371117333,-2.07103424867934,3.09349069875718));
#16139=CARTESIAN_POINT('Ctrl Pts',(84.5641963064285,-2.1587637784421,3.03475741702073));
#16140=CARTESIAN_POINT('Ctrl Pts',(84.5698555011238,-2.24388219142092,2.97236346029204));
#16141=CARTESIAN_POINT('Ctrl Pts',(84.575514695819,-2.32608221373895,2.90658030981897));
#16142=CARTESIAN_POINT('Ctrl Pts',(84.581413414995,-2.41176133842471,2.83801289836744));
#16143=CARTESIAN_POINT('Ctrl Pts',(84.587312134171,-2.49455984951417,2.76553054908317));
#16144=CARTESIAN_POINT('Ctrl Pts',(84.5932108533469,-2.57409385340434,2.68940669969531));
#16145=CARTESIAN_POINT('Ctrl Pts',(84.5943830597574,-2.58989902507423,2.67427920140653));
#16146=CARTESIAN_POINT('Ctrl Pts',(84.5955552661679,-2.60557536834159,2.65900803735653));
#16147=CARTESIAN_POINT('Ctrl Pts',(84.5967274725783,-2.62112000711956,2.64359555733807));
#16148=CARTESIAN_POINT('Ctrl Pts',(83.3465449346096,-2.62112000711956,2.64359555733806));
#16149=CARTESIAN_POINT('Ctrl Pts',(83.3525016691969,-2.70037299466952,2.56501636971816));
#16150=CARTESIAN_POINT('Ctrl Pts',(83.3584584037842,-2.77603460091793,2.48292445303177));
#16151=CARTESIAN_POINT('Ctrl Pts',(83.3644151383715,-2.84779618052708,2.39769148905262));
#16152=CARTESIAN_POINT('Ctrl Pts',(83.3706822034804,-2.9232963535055,2.30801810729406));
#16153=CARTESIAN_POINT('Ctrl Pts',(83.3769492685892,-2.99447886170437,2.21486800490521));
#16154=CARTESIAN_POINT('Ctrl Pts',(83.3832163336981,-3.0610357268376,2.1187090035028));
#16155=CARTESIAN_POINT('Ctrl Pts',(83.389483398807,-3.12759259197083,2.02255000210039));
#16156=CARTESIAN_POINT('Ctrl Pts',(83.3957504639159,-3.18952359244235,1.92338258779279));
#16157=CARTESIAN_POINT('Ctrl Pts',(83.4020175290247,-3.24657727312924,1.82170348083895));
#16158=CARTESIAN_POINT('Ctrl Pts',(83.4082277166816,-3.30311315674049,1.72094717401999));
#16159=CARTESIAN_POINT('Ctrl Pts',(83.4144379043384,-3.35502911036208,1.61742461319456));
#16160=CARTESIAN_POINT('Ctrl Pts',(83.4206480919953,-3.40205797839426,1.51157833873867));
#16161=CARTESIAN_POINT('Ctrl Pts',(83.4268480740761,-3.44900956105002,1.40590600785203));
#16162=CARTESIAN_POINT('Ctrl Pts',(83.4330480561568,-3.49108990258534,1.29791790193999));
#16163=CARTESIAN_POINT('Ctrl Pts',(83.4392480382376,-3.52807725450457,1.18808183587979));
#16164=CARTESIAN_POINT('Ctrl Pts',(83.445435562709,-3.56499028782464,1.07846646316866));
#16165=CARTESIAN_POINT('Ctrl Pts',(83.4516230871803,-3.59683061192906,0.96701087846192));
#16166=CARTESIAN_POINT('Ctrl Pts',(83.4578106116517,-3.62342453387416,0.854202674907337));
#16167=CARTESIAN_POINT('Ctrl Pts',(83.463990675881,-3.64998639176911,0.741530483179206));
#16168=CARTESIAN_POINT('Ctrl Pts',(83.4701707401103,-3.67131435686101,0.627509275877126));
#16169=CARTESIAN_POINT('Ctrl Pts',(83.4763508043396,-3.68728427496461,0.512642407628058));
#16170=CARTESIAN_POINT('Ctrl Pts',(83.482522178374,-3.70323173671555,0.397937061240715));
#16171=CARTESIAN_POINT('Ctrl Pts',(83.4886935524083,-3.71383611662847,0.282388787199165));
#16172=CARTESIAN_POINT('Ctrl Pts',(83.4948649264427,-3.71902428479849,0.166511055425917));
#16173=CARTESIAN_POINT('Ctrl Pts',(83.497824988145,-3.72151275783868,0.110931012137859));
#16174=CARTESIAN_POINT('Ctrl Pts',(83.5007850498474,-3.72275594166151,0.0552753217717917));
#16175=CARTESIAN_POINT('Ctrl Pts',(83.5037451115497,-3.72274997864695,-0.000398728175137864));
#16176=CARTESIAN_POINT('',(83.2572559480305,-3.72274911375701,0.00256875873404117));
#16177=CARTESIAN_POINT('Ctrl Pts',(83.100211836361,-2.62112000711957,2.64359555733806));
#16178=CARTESIAN_POINT('Ctrl Pts',(83.1061733650853,-2.70050125117219,2.56488920363776));
#16179=CARTESIAN_POINT('Ctrl Pts',(83.1121348938096,-2.77636815978871,2.48257080322071));
#16180=CARTESIAN_POINT('Ctrl Pts',(83.1180964225339,-2.84838564888578,2.39699118849476));
#16181=CARTESIAN_POINT('Ctrl Pts',(83.124057147844,-2.92039343244001,2.31142310703146));
#16182=CARTESIAN_POINT('Ctrl Pts',(83.1300178731541,-2.98855256152826,2.22259500245706));
#16183=CARTESIAN_POINT('Ctrl Pts',(83.1359785984642,-3.05256744398181,2.13089172940399));
#16184=CARTESIAN_POINT('Ctrl Pts',(83.1419399627032,-3.11658918817695,2.03917862669667));
#16185=CARTESIAN_POINT('Ctrl Pts',(83.1479013269421,-3.17646556556848,1.94459008277441));
#16186=CARTESIAN_POINT('Ctrl Pts',(83.1538626911811,-3.23194404411675,1.84754032654183));
#16187=CARTESIAN_POINT('Ctrl Pts',(83.1598298427706,-3.2874763817128,1.75039635345986));
#16188=CARTESIAN_POINT('Ctrl Pts',(83.1657969943601,-3.3386020847474,1.65078675510819));
#16189=CARTESIAN_POINT('Ctrl Pts',(83.1717641459496,-3.3851143192338,1.54915093138736));
#16190=CARTESIAN_POINT('Ctrl Pts',(83.1777341182834,-3.43164854061269,1.44746706319059));
#16191=CARTESIAN_POINT('Ctrl Pts',(83.1837040906172,-3.47356479129552,1.34375544507299));
#16192=CARTESIAN_POINT('Ctrl Pts',(83.189674062951,-3.51070488846345,1.23847436332724));
#16193=CARTESIAN_POINT('Ctrl Pts',(83.1956536293093,-3.54790467150296,1.13302408996371));
#16194=CARTESIAN_POINT('Ctrl Pts',(83.2016331956676,-3.58031284013752,1.02599970947008));
#16195=CARTESIAN_POINT('Ctrl Pts',(83.2076127620259,-3.60782133468535,0.917874054263007));
#16196=CARTESIAN_POINT('Ctrl Pts',(83.2135191661238,-3.63499325237795,0.811071357422008));
#16197=CARTESIAN_POINT('Ctrl Pts',(83.2194255702217,-3.65738473422337,0.703194579387955));
#16198=CARTESIAN_POINT('Ctrl Pts',(83.2253319743196,-3.67494124204485,0.594705330409806));
#16199=CARTESIAN_POINT('Ctrl Pts',(83.2345685167955,-3.70239642925054,0.42504786374353));
#16200=CARTESIAN_POINT('Ctrl Pts',(83.2438050592713,-3.71810656497179,0.253443539326488));
#16201=CARTESIAN_POINT('Ctrl Pts',(83.2530416017472,-3.72186436816731,0.0811984449760008));
#16202=CARTESIAN_POINT('Ctrl Pts',(83.2544463838416,-3.72243589097006,0.0550017566555983));
#16203=CARTESIAN_POINT('Ctrl Pts',(83.2558511659361,-3.72273102045438,0.0287903051327956));
#16204=CARTESIAN_POINT('Ctrl Pts',(83.2572559480305,-3.72274911375701,0.00256875873404105));
#16205=CARTESIAN_POINT('Ctrl Pts',(83.2585049200401,-3.72274907161456,0.00262912398830983));
#16206=CARTESIAN_POINT('Ctrl Pts',(83.2638576126972,-3.72282728496551,-0.108118288811131));
#16207=CARTESIAN_POINT('Ctrl Pts',(83.2691451236267,-3.71796356302337,-0.218816680367323));
#16208=CARTESIAN_POINT('Ctrl Pts',(83.2833777464751,-3.69177043663755,-0.513918430758105));
#16209=CARTESIAN_POINT('Ctrl Pts',(83.2923742746305,-3.66158130974653,-0.697205937793369));
#16210=CARTESIAN_POINT('Ctrl Pts',(83.3051807990402,-3.6019411919301,-0.943105964834372));
#16211=CARTESIAN_POINT('Ctrl Pts',(83.3086466220414,-3.5842391240922,-1.00829480213931));
#16212=CARTESIAN_POINT('Ctrl Pts',(83.3145392556633,-3.55165987094859,-1.11653489041305));
#16213=CARTESIAN_POINT('Ctrl Pts',(83.316935558106,-3.53774802543589,-1.15986062570442));
#16214=CARTESIAN_POINT('Ctrl Pts',(83.3215329364804,-3.50983776513739,-1.24160270923904));
#16215=CARTESIAN_POINT('Ctrl Pts',(83.3237287763499,-3.49599373319366,-1.28006486725557));
#16216=CARTESIAN_POINT('Ctrl Pts',(83.3295758461878,-3.4578068614688,-1.38091393073346));
#16217=CARTESIAN_POINT('Ctrl Pts',(83.3332605728359,-3.43240997422359,-1.44288342070459));
#16218=CARTESIAN_POINT('Ctrl Pts',(83.3515733136363,-3.29981066759159,-1.74308846907473));
#16219=CARTESIAN_POINT('Ctrl Pts',(83.3669542903669,-3.16941840436925,-1.97024382688032));
#16220=CARTESIAN_POINT('Ctrl Pts',(83.3897565217143,-2.94335362567548,-2.28277272151319));
#16221=CARTESIAN_POINT('Ctrl Pts',(83.3971055115402,-2.8653311137376,-2.37997095737977));
#16222=CARTESIAN_POINT('Ctrl Pts',(83.4086512496694,-2.7323903958003,-2.52954903307825));
#16223=CARTESIAN_POINT('Ctrl Pts',(83.4129472351165,-2.68048979719727,-2.58448281512371));
#16224=CARTESIAN_POINT('Ctrl Pts',(83.4189166499203,-2.6042955312153,-2.66036362449628));
#16225=CARTESIAN_POINT('Ctrl Pts',(83.4206730949348,-2.58135022513618,-2.68263321825345));
#16226=CARTESIAN_POINT('Ctrl Pts',(83.4237525950993,-2.5401170454266,-2.72163315304266));
#16227=CARTESIAN_POINT('Ctrl Pts',(83.4250837025986,-2.52194505370165,-2.73848038752581));
#16228=CARTESIAN_POINT('Ctrl Pts',(83.428133800469,-2.47949951325509,-2.77705069903226));
#16229=CARTESIAN_POINT('Ctrl Pts',(83.4298435096785,-2.45510713390138,-2.79863851276391));
#16230=CARTESIAN_POINT('Ctrl Pts',(83.4353841900916,-2.37423569819015,-2.86834041006189));
#16231=CARTESIAN_POINT('Ctrl Pts',(83.4391332259844,-2.31659896398363,-2.91508873796779));
#16232=CARTESIAN_POINT('Ctrl Pts',(83.4562313316096,-2.04283030676886,-3.12388683190406));
#16233=CARTESIAN_POINT('Ctrl Pts',(83.4687957904166,-1.81086280537036,-3.26383482825989));
#16234=CARTESIAN_POINT('Ctrl Pts',(83.4865013276209,-1.48078382492111,-3.4168588080493));
#16235=CARTESIAN_POINT('Ctrl Pts',(83.4911173468721,-1.39433277550477,-3.45303918718552));
#16236=CARTESIAN_POINT('Ctrl Pts',(83.4996044202193,-1.23619370674814,-3.51231378902122));
#16237=CARTESIAN_POINT('Ctrl Pts',(83.503440559873,-1.16499473470343,-3.53656745324965));
#16238=CARTESIAN_POINT('Ctrl Pts',(83.5097692295129,-1.04847164302234,-3.57235995571267));
#16239=CARTESIAN_POINT('Ctrl Pts',(83.5122193145197,-1.00357769368316,-3.58523081486505));
#16240=CARTESIAN_POINT('Ctrl Pts',(83.5170448962557,-0.915669737136947,
-3.60865307376034));
#16241=CARTESIAN_POINT('Ctrl Pts',(83.5194172781105,-0.872686049542964,
-3.61928817672618));
#16242=CARTESIAN_POINT('Ctrl Pts',(83.5252766768713,-0.76715499209866,-3.64340965513409));
#16243=CARTESIAN_POINT('Ctrl Pts',(83.5287890688095,-0.704431593327425,
-3.65605472398968));
#16244=CARTESIAN_POINT('Ctrl Pts',(83.5479355589096,-0.365508791770839,
-3.7153364127369));
#16245=CARTESIAN_POINT('Ctrl Pts',(83.5644682736973,-0.0850695691510357,
-3.73229717196538));
#16246=CARTESIAN_POINT('Ctrl Pts',(83.5901494371418,0.349343444480504,-3.70956166195331));
#16247=CARTESIAN_POINT('Ctrl Pts',(83.599251969939,0.50347247068095,-3.69180312697101));
#16248=CARTESIAN_POINT('Ctrl Pts',(83.6105841792651,0.701018548347868,-3.65643640446163));
#16249=CARTESIAN_POINT('Ctrl Pts',(83.6131317785146,0.745833250036449,-3.64755909004184));
#16250=CARTESIAN_POINT('Ctrl Pts',(83.6171034157223,0.816556591822837,-3.63219152268993));
#16251=CARTESIAN_POINT('Ctrl Pts',(83.6185541069433,0.842577328332253,-3.62624371398824));
#16252=CARTESIAN_POINT('Ctrl Pts',(83.6214284907893,0.894570768669446,-3.61376918284361));
#16253=CARTESIAN_POINT('Ctrl Pts',(83.6228520689543,0.920541386241129,-3.60724107993627));
#16254=CARTESIAN_POINT('Ctrl Pts',(83.626660835685,0.990528164418255,-3.58884376802237));
#16255=CARTESIAN_POINT('Ctrl Pts',(83.6290188571499,1.03440154186965,-3.57644508353148));
#16256=CARTESIAN_POINT('Ctrl Pts',(83.6439924781601,1.31539049994864,-3.49143355508272));
#16257=CARTESIAN_POINT('Ctrl Pts',(83.6556675390205,1.54499682541416,-3.39608140268703));
#16258=CARTESIAN_POINT('Ctrl Pts',(83.6762584420214,1.92246193854061,-3.19305734416994));
#16259=CARTESIAN_POINT('Ctrl Pts',(83.6850280132631,2.07504963653927,-3.09606799524797));
#16260=CARTESIAN_POINT('Ctrl Pts',(83.6975610776047,2.27376479873965,-2.94844856096181));
#16261=CARTESIAN_POINT('Ctrl Pts',(83.7009996631463,2.32645023892897,-2.90705759712991));
#16262=CARTESIAN_POINT('Ctrl Pts',(83.7068637641646,2.41298631487513,-2.83521316950821));
#16263=CARTESIAN_POINT('Ctrl Pts',(83.7092596483056,2.44744763878988,-2.80551893421772));
#16264=CARTESIAN_POINT('Ctrl Pts',(83.7138682796151,2.5119881525956,-2.74781215427669));
#16265=CARTESIAN_POINT('Ctrl Pts',(83.7160760309642,2.54216457518938,-2.71991823518722));
#16266=CARTESIAN_POINT('Ctrl Pts',(83.721987389539,2.62097551097681,-2.64461104187058));
#16267=CARTESIAN_POINT('Ctrl Pts',(83.7257256587852,2.66878319044914,-2.5963581547807));
#16268=CARTESIAN_POINT('Ctrl Pts',(83.7391975189689,2.83389782740182,-2.42032487271339));
#16269=CARTESIAN_POINT('Ctrl Pts',(83.7492167701334,2.94355601864174,-2.28569826721965));
#16270=CARTESIAN_POINT('Ctrl Pts',(83.7683380940237,3.1311565748759,-2.0193895395188));
#16271=CARTESIAN_POINT('Ctrl Pts',(83.7773825708992,3.21116203266535,-1.88958030309448));
#16272=CARTESIAN_POINT('Ctrl Pts',(83.7909849898624,3.32075020708103,-1.68460674672849));
#16273=CARTESIAN_POINT('Ctrl Pts',(83.7956313562862,3.35622403414705,-1.61277499397278));
#16274=CARTESIAN_POINT('Ctrl Pts',(83.8034261896783,3.41282162792539,-1.48819853785444));
#16275=CARTESIAN_POINT('Ctrl Pts',(83.8066151922318,3.43510619660879,-1.43601268065878));
#16276=CARTESIAN_POINT('Ctrl Pts',(83.8113432052663,3.46696084763822,-1.35642551886147));
#16277=CARTESIAN_POINT('Ctrl Pts',(83.8129261062509,3.47741716679819,-1.3293899585882));
#16278=CARTESIAN_POINT('Ctrl Pts',(83.815852574161,3.49637952445641,-1.27860623382985));
#16279=CARTESIAN_POINT('Ctrl Pts',(83.8171999813375,3.50496162937362,-1.25488950590697));
#16280=CARTESIAN_POINT('Ctrl Pts',(83.8205702077459,3.52602790945583,-1.19477010012411));
#16281=CARTESIAN_POINT('Ctrl Pts',(83.8225757723952,3.53819017308572,-1.15825685061596));
#16282=CARTESIAN_POINT('Ctrl Pts',(83.8314316637413,3.59003589499568,-0.994162997081114));
#16283=CARTESIAN_POINT('Ctrl Pts',(83.8379996857618,3.62340319225326,-0.86468069151639));
#16284=CARTESIAN_POINT('Ctrl Pts',(83.8548324462676,3.69193750290241,-0.52375039050757));
#16285=CARTESIAN_POINT('Ctrl Pts',(83.8649279586079,3.71594660558186,-0.310578219390088));
#16286=CARTESIAN_POINT('Ctrl Pts',(83.8796097384085,3.72372783165573,-0.0105687999832971));
#16287=CARTESIAN_POINT('Ctrl Pts',(83.8838691542674,3.72297856222137,0.0754333607792057));
#16288=CARTESIAN_POINT('Ctrl Pts',(83.8917805181,3.71618339616644,0.232087674670751));
#16289=CARTESIAN_POINT('Ctrl Pts',(83.8954053909491,3.71109564712829,0.302740841039616));
#16290=CARTESIAN_POINT('Ctrl Pts',(83.9014872494626,3.69937842238453,0.419032843454376));
#16291=CARTESIAN_POINT('Ctrl Pts',(83.9039088694483,3.69391074271478,0.464771357455509));
#16292=CARTESIAN_POINT('Ctrl Pts',(83.9087830496748,3.68133580642662,0.555625010578794));
#16293=CARTESIAN_POINT('Ctrl Pts',(83.9112347362656,3.6742442268481,0.600734205186967));
#16294=CARTESIAN_POINT('Ctrl Pts',(83.9174315923414,3.65443332525176,0.713221696609458));
#16295=CARTESIAN_POINT('Ctrl Pts',(83.9212077158701,3.64067926602818,0.780398466693295));
#16296=CARTESIAN_POINT('Ctrl Pts',(83.9356978252883,3.58165226936026,1.0329823251376));
#16297=CARTESIAN_POINT('Ctrl Pts',(83.9467707403151,3.5240059185411,1.21517639209199));
#16298=CARTESIAN_POINT('Ctrl Pts',(83.9679619862629,3.38942279659358,1.54895902919156));
#16299=CARTESIAN_POINT('Ctrl Pts',(83.9780162803526,3.31557685485957,1.70129732655008));
#16300=CARTESIAN_POINT('Ctrl Pts',(83.9914350912164,3.20079623001511,1.90200653607067));
#16301=CARTESIAN_POINT('Ctrl Pts',(83.9950041241817,3.16861639365688,1.95514607327778));
#16302=CARTESIAN_POINT('Ctrl Pts',(84.0011963757302,3.10956695795086,2.0473657594154));
#16303=CARTESIAN_POINT('Ctrl Pts',(84.0038426353865,3.08325237539411,2.0867842275118));
#16304=CARTESIAN_POINT('Ctrl Pts',(84.0079344242075,3.04071361213057,2.14794390756076));
#16305=CARTESIAN_POINT('Ctrl Pts',(84.009408934715,3.02499298892332,2.17002760526528));
#16306=CARTESIAN_POINT('Ctrl Pts',(84.0122906618612,2.99345399735384,2.21332345825535));
#16307=CARTESIAN_POINT('Ctrl Pts',(84.0136984279709,2.97764804758882,2.23454239822952));
#16308=CARTESIAN_POINT('Ctrl Pts',(84.017418342554,2.93486379641107,2.29071859921863));
#16309=CARTESIAN_POINT('Ctrl Pts',(84.0197053783879,2.90748675249781,2.32536842457618));
#16310=CARTESIAN_POINT('Ctrl Pts',(84.03259065013,2.74762096130101,2.52046423837457));
#16311=CARTESIAN_POINT('Ctrl Pts',(84.0425190135211,2.60247016200988,2.67007972286238));
#16312=CARTESIAN_POINT('Ctrl Pts',(84.0624031484007,2.28953368249273,2.94274220337305));
#16313=CARTESIAN_POINT('Ctrl Pts',(84.072331372375,2.1224436072201,3.06543991445343));
#16314=CARTESIAN_POINT('Ctrl Pts',(84.0864978851887,1.88231055164521,3.21268770257991));
#16315=CARTESIAN_POINT('Ctrl Pts',(84.0903134071336,1.81742641055444,3.24983316467351));
#16316=CARTESIAN_POINT('Ctrl Pts',(84.0966248541689,1.71020517253938,3.3070005657496));
#16317=CARTESIAN_POINT('Ctrl Pts',(84.0990793757297,1.66853007633547,3.32822198808082));
#16318=CARTESIAN_POINT('Ctrl Pts',(84.1039265587214,1.58636333652785,3.36813103886614));
#16319=CARTESIAN_POINT('Ctrl Pts',(84.1063163702875,1.54591376819017,3.38688732037933));
#16320=CARTESIAN_POINT('Ctrl Pts',(84.1122457380088,1.44576455455904,3.43115818723231));
#16321=CARTESIAN_POINT('Ctrl Pts',(84.1158116609776,1.38571725484166,3.45584557431743));
#16322=CARTESIAN_POINT('Ctrl Pts',(84.1346499696334,1.06956370073763,3.57626171697957));
#16323=CARTESIAN_POINT('Ctrl Pts',(84.1507648386761,0.804157548623636,3.64512084960632));
#16324=CARTESIAN_POINT('Ctrl Pts',(84.1762430953166,0.376943384656355,3.7070007311358));
#16325=CARTESIAN_POINT('Ctrl Pts',(84.1855479519405,0.218934516246659,3.71967940236616));
#16326=CARTESIAN_POINT('Ctrl Pts',(84.1970974593835,0.0144622026793799,
3.72300775562695));
#16327=CARTESIAN_POINT('Ctrl Pts',(84.1996708459668,-0.0316776945410093,
3.72290112718942));
#16328=CARTESIAN_POINT('Ctrl Pts',(84.2036770923633,-0.104657644209761,
3.72137550988149));
#16329=CARTESIAN_POINT('Ctrl Pts',(84.2051370643525,-0.131503616993609,
3.72052359140501));
#16330=CARTESIAN_POINT('Ctrl Pts',(84.2080174526266,-0.185030306576398,
3.71824489174586));
#16331=CARTESIAN_POINT('Ctrl Pts',(84.209437928948,-0.211709548058561,3.71682128132288));
#16332=CARTESIAN_POINT('Ctrl Pts',(84.2132328593006,-0.283654820992114,
3.71220507110036));
#16333=CARTESIAN_POINT('Ctrl Pts',(84.2155804119649,-0.328882759828231,
3.7084717908243));
#16334=CARTESIAN_POINT('Ctrl Pts',(84.2306036367792,-0.621877745031476,
3.678884215306));
#16335=CARTESIAN_POINT('Ctrl Pts',(84.2423267203417,-0.86660830598496,3.62904051580633));
#16336=CARTESIAN_POINT('Ctrl Pts',(84.2617401583419,-1.25251078999618,3.50914410478832));
#16337=CARTESIAN_POINT('Ctrl Pts',(84.2692526983368,-1.3974573896755,3.45398091650242));
#16338=CARTESIAN_POINT('Ctrl Pts',(84.2809982225684,-1.61085106516936,3.35713160301902));
#16339=CARTESIAN_POINT('Ctrl Pts',(84.2850400742585,-1.68209134678154,3.32200863327877));
#16340=CARTESIAN_POINT('Ctrl Pts',(84.2916274983343,-1.79418963292394,3.26221109529338));
#16341=CARTESIAN_POINT('Ctrl Pts',(84.2941241706537,-1.83579234461218,3.2389819182649));
#16342=CARTESIAN_POINT('Ctrl Pts',(84.299016557877,-1.91552886629479,3.19243069134184));
#16343=CARTESIAN_POINT('Ctrl Pts',(84.3014085125211,-1.95371112459508,3.16920765592025));
#16344=CARTESIAN_POINT('Ctrl Pts',(84.3072071267281,-2.04430897257305,3.11184516564172));
#16345=CARTESIAN_POINT('Ctrl Pts',(84.3106364169776,-2.0962989975848,3.07706181085706));
#16346=CARTESIAN_POINT('Ctrl Pts',(84.3255913422868,-2.3161779157726,2.9217947892804));
#16347=CARTESIAN_POINT('Ctrl Pts',(84.3375608740159,-2.47462004730783,2.78884999307511));
#16348=CARTESIAN_POINT('Ctrl Pts',(84.3497092113127,-2.62112002533992,2.64359553927261));
#16349=CARTESIAN_POINT('Origin',(80.1322559480305,0.,0.));
#16350=CARTESIAN_POINT('',(85.8498933978769,-2.62112000707361,2.64359555738363));
#16351=CARTESIAN_POINT('',(85.6021262427416,-2.62112000930789,2.64359555516834));
#16352=CARTESIAN_POINT('',(80.1322559480305,-2.62112000711956,2.64359555733806));
#16353=CARTESIAN_POINT('',(84.7537451115017,-3.72274958225736,-0.00176360502600202));
#16354=CARTESIAN_POINT('Ctrl Pts',(85.8498933978769,-2.62112000707361,2.64359555738363));
#16355=CARTESIAN_POINT('Ctrl Pts',(85.849690671865,-2.6184134442255,2.64627910934065));
#16356=CARTESIAN_POINT('Ctrl Pts',(85.8494877682365,-2.6157027508985,2.64895851394654));
#16357=CARTESIAN_POINT('Ctrl Pts',(85.8467827579202,-2.57954191884002,2.6845923255638));
#16358=CARTESIAN_POINT('Ctrl Pts',(85.8442541779368,-2.54547641486122,2.7169140613065));
#16359=CARTESIAN_POINT('Ctrl Pts',(85.8375783888193,-2.45491206316508,2.79964394224953));
#16360=CARTESIAN_POINT('Ctrl Pts',(85.833389512113,-2.39747278233872,2.84898623874646));
#16361=CARTESIAN_POINT('Ctrl Pts',(85.8193038106923,-2.20236979897572,3.00650596879077));
#16362=CARTESIAN_POINT('Ctrl Pts',(85.8091355210378,-2.05859394793133,3.10671713627308));
#16363=CARTESIAN_POINT('Ctrl Pts',(85.7844201176763,-1.69807556203329,3.32195157666296));
#16364=CARTESIAN_POINT('Ctrl Pts',(85.7697852079376,-1.4759574290867,3.42642423730708));
#16365=CARTESIAN_POINT('Ctrl Pts',(85.7537493346471,-1.20683816778594,3.52194047344496));
#16366=CARTESIAN_POINT('Ctrl Pts',(85.7514911153441,-1.16827171348717,3.53492072508049));
#16367=CARTESIAN_POINT('Ctrl Pts',(85.7479931769934,-1.1073266952543,3.55432646112222));
#16368=CARTESIAN_POINT('Ctrl Pts',(85.7467314252218,-1.0850882112766,3.5611785482578));
#16369=CARTESIAN_POINT('Ctrl Pts',(85.7440235336394,-1.03676569334935,3.57557290535865));
#16370=CARTESIAN_POINT('Ctrl Pts',(85.7425816923323,-1.01066044131974,3.5830392497816));
#16371=CARTESIAN_POINT('Ctrl Pts',(85.7386547552395,-0.938620784840327,
3.60279326329947));
#16372=CARTESIAN_POINT('Ctrl Pts',(85.7361999030544,-0.892527813711963,
3.6144878986108));
#16373=CARTESIAN_POINT('Ctrl Pts',(85.7306046011122,-0.785460212401721,
3.63947975819947));
#16374=CARTESIAN_POINT('Ctrl Pts',(85.7274902187997,-0.724349407330987,
3.65213351651395));
#16375=CARTESIAN_POINT('Ctrl Pts',(85.7160022790089,-0.494949250037407,
3.69364865955921));
#16376=CARTESIAN_POINT('Ctrl Pts',(85.7078909325865,-0.325052530382849,
3.71246019291951));
#16377=CARTESIAN_POINT('Ctrl Pts',(85.6906654259996,0.0336435509885337,
3.72735554171201));
#16378=CARTESIAN_POINT('Ctrl Pts',(85.6815524370027,0.222057317023121,3.72088623031167));
#16379=CARTESIAN_POINT('Ctrl Pts',(85.6685746735745,0.477207648111928,3.69267210153699));
#16380=CARTESIAN_POINT('Ctrl Pts',(85.6650649689563,0.545029842721874,3.68327247522413));
#16381=CARTESIAN_POINT('Ctrl Pts',(85.6591208615526,0.6575800274808,3.66449724096061));
#16382=CARTESIAN_POINT('Ctrl Pts',(85.656718348156,0.702464850401875,3.65615842317771));
#16383=CARTESIAN_POINT('Ctrl Pts',(85.6518382467234,0.792342665615207,3.6377445746562));
#16384=CARTESIAN_POINT('Ctrl Pts',(85.6493605835827,0.83732439850672,3.62765490176853));
#16385=CARTESIAN_POINT('Ctrl Pts',(85.6430018368033,0.951063617474324,3.59991438627524));
#16386=CARTESIAN_POINT('Ctrl Pts',(85.63908630388,1.01952279049039,3.58112802790292));
#16387=CARTESIAN_POINT('Ctrl Pts',(85.6302875271805,1.16987179069909,3.53520912508429));
#16388=CARTESIAN_POINT('Ctrl Pts',(85.6253796023952,1.25143887867322,3.50716450216352));
#16389=CARTESIAN_POINT('Ctrl Pts',(85.6079786913726,1.53320161432178,3.39920670606868));
#16390=CARTESIAN_POINT('Ctrl Pts',(85.5951510989502,1.72736505329527,3.30477133006903));
#16391=CARTESIAN_POINT('Ctrl Pts',(85.5747142866102,2.02577702016933,3.12611610337083));
#16392=CARTESIAN_POINT('Ctrl Pts',(85.5670243972746,2.13560545026952,3.05214170424462));
#16393=CARTESIAN_POINT('Ctrl Pts',(85.5574720328277,2.27182319314675,2.94943237272094));
#16394=CARTESIAN_POINT('Ctrl Pts',(85.5553535574472,2.30202223251655,2.9259230696851));
#16395=CARTESIAN_POINT('Ctrl Pts',(85.5518912440141,2.35146525431007,2.88619327484354));
#16396=CARTESIAN_POINT('Ctrl Pts',(85.5505308828231,2.37091645121678,2.87023618807598));
#16397=CARTESIAN_POINT('Ctrl Pts',(85.5476361342394,2.4123897687681,2.83550356354633));
#16398=CARTESIAN_POINT('Ctrl Pts',(85.5461059159884,2.43435717266661,2.81666648997742));
#16399=CARTESIAN_POINT('Ctrl Pts',(85.5416194178792,2.49878774444922,2.76010029706633));
#16400=CARTESIAN_POINT('Ctrl Pts',(85.5387092671786,2.54061097516456,2.72165213478155));
#16401=CARTESIAN_POINT('Ctrl Pts',(85.5317968229488,2.63937172582106,2.62659990025905));
#16402=CARTESIAN_POINT('Ctrl Pts',(85.5278415292646,2.69539094125685,2.56908134265731));
#16403=CARTESIAN_POINT('Ctrl Pts',(85.5165010950126,2.85244590106617,2.39702580300335));
#16404=CARTESIAN_POINT('Ctrl Pts',(85.50924685486,2.94834958500859,2.27802919945283));
#16405=CARTESIAN_POINT('Ctrl Pts',(85.4935449089584,3.13734262298577,2.01152504874999));
#16406=CARTESIAN_POINT('Ctrl Pts',(85.4850867484135,3.22792573528098,1.86269716150979));
#16407=CARTESIAN_POINT('Ctrl Pts',(85.4728497410405,3.33893488953635,1.64772475897147));
#16408=CARTESIAN_POINT('Ctrl Pts',(85.4693655046101,3.36844673677804,1.58652101842006));
#16409=CARTESIAN_POINT('Ctrl Pts',(85.4636886265646,3.41306288591806,1.48712861096727));
#16410=CARTESIAN_POINT('Ctrl Pts',(85.4615317343766,3.42923932167846,1.44943688014956));
#16411=CARTESIAN_POINT('Ctrl Pts',(85.4569480635662,3.46197230741317,1.36955071887326));
#16412=CARTESIAN_POINT('Ctrl Pts',(85.4545171095525,3.4783875643555,1.32730597020498));
#16413=CARTESIAN_POINT('Ctrl Pts',(85.4484547514622,3.51699110628418,1.22232104980251));
#16414=CARTESIAN_POINT('Ctrl Pts',(85.444795266573,3.538275535791,1.15926729498409));
#16415=CARTESIAN_POINT('Ctrl Pts',(85.4311615839286,3.61023463082996,0.925603878823073));
#16416=CARTESIAN_POINT('Ctrl Pts',(85.4208784736446,3.65034344467164,0.752009042050682));
#16417=CARTESIAN_POINT('Ctrl Pts',(85.3955882918672,3.71698579221673,0.326652004638766));
#16418=CARTESIAN_POINT('Ctrl Pts',(85.3804520176507,3.73058373419855,0.0737393952907888));
#16419=CARTESIAN_POINT('Ctrl Pts',(85.3636757419601,3.71631345849157,-0.223359226114893));
#16420=CARTESIAN_POINT('Ctrl Pts',(85.36117938238,3.71335598082205,-0.268072326452417));
#16421=CARTESIAN_POINT('Ctrl Pts',(85.3572634888432,3.70735760461216,-0.339226442226781));
#16422=CARTESIAN_POINT('Ctrl Pts',(85.3558187653444,3.70483928268253,-0.365706135442116));
#16423=CARTESIAN_POINT('Ctrl Pts',(85.3529395161141,3.69919392747321,-0.418999304245632));
#16424=CARTESIAN_POINT('Ctrl Pts',(85.3515054731768,3.69605864120948,-0.445810204152075));
#16425=CARTESIAN_POINT('Ctrl Pts',(85.3476264503708,3.68669599884262,-0.518966908123563));
#16426=CARTESIAN_POINT('Ctrl Pts',(85.3452104894457,3.67988647037834,-0.565234446341687));
#16427=CARTESIAN_POINT('Ctrl Pts',(85.3344763028182,3.64527779241602,-0.773114466746253));
#16428=CARTESIAN_POINT('Ctrl Pts',(85.3265494915856,3.60768891066312,-0.932922966576545));
#16429=CARTESIAN_POINT('Ctrl Pts',(85.306004472804,3.48241018388323,-1.34215037544668));
#16430=CARTESIAN_POINT('Ctrl Pts',(85.2934810245839,3.37851977141229,-1.58560494221275));
#16431=CARTESIAN_POINT('Ctrl Pts',(85.2767595163137,3.21750684931743,-1.8737364836297));
#16432=CARTESIAN_POINT('Ctrl Pts',(85.2733641118959,3.18372448134068,-1.93057931628217));
#16433=CARTESIAN_POINT('Ctrl Pts',(85.2675795871691,3.12454326829097,-2.02437737777324));
#16434=CARTESIAN_POINT('Ctrl Pts',(85.2652194988286,3.09995760553115,-2.06182856209323));
#16435=CARTESIAN_POINT('Ctrl Pts',(85.2603592027751,3.04848611462761,-2.13723240205437));
#16436=CARTESIAN_POINT('Ctrl Pts',(85.257857514359,3.02155299329874,-2.17514302465089));
#16437=CARTESIAN_POINT('Ctrl Pts',(85.2513488598448,2.95040283633244,-2.27142055647856));
#16438=CARTESIAN_POINT('Ctrl Pts',(85.247304087132,2.90516269536378,-2.32900342355141));
#16439=CARTESIAN_POINT('Ctrl Pts',(85.2381486347237,2.80054002858953,-2.45437522820134));
#16440=CARTESIAN_POINT('Ctrl Pts',(85.233009787767,2.74033565318834,-2.52141648531876));
#16441=CARTESIAN_POINT('Ctrl Pts',(85.2138900374879,2.51055586160951,-2.75933095029729));
#16442=CARTESIAN_POINT('Ctrl Pts',(85.1994926721621,2.32695572552251,-2.91582994796519));
#16443=CARTESIAN_POINT('Ctrl Pts',(85.1794133401151,2.04470101149989,-3.11267855988058));
#16444=CARTESIAN_POINT('Ctrl Pts',(85.1734583055322,1.95741008072819,-3.16829903621415));
#16445=CARTESIAN_POINT('Ctrl Pts',(85.1656614014065,1.83662806856286,-3.238359571677));
#16446=CARTESIAN_POINT('Ctrl Pts',(85.1636642298542,1.80508217280523,-3.25604882050573));
#16447=CARTESIAN_POINT('Ctrl Pts',(85.1603248978248,1.75119397463262,-3.28524250485353));
#16448=CARTESIAN_POINT('Ctrl Pts',(85.1589692673526,1.72898460721741,-3.29698513832612));
#16449=CARTESIAN_POINT('Ctrl Pts',(85.1560187909301,1.6798857445708,-3.32231226848747));
#16450=CARTESIAN_POINT('Ctrl Pts',(85.1544295912095,1.65294767942693,-3.3357966079129));
#16451=CARTESIAN_POINT('Ctrl Pts',(85.1495438452933,1.56873275593393,-3.37668122870755));
#16452=CARTESIAN_POINT('Ctrl Pts',(85.1463066382227,1.51091439842671,-3.40294535709103));
#16453=CARTESIAN_POINT('Ctrl Pts',(85.1383752689073,1.3652789044957,-3.46465643146747));
#16454=CARTESIAN_POINT('Ctrl Pts',(85.1337487411319,1.27672671808013,-3.49825687718033));
#16455=CARTESIAN_POINT('Ctrl Pts',(85.1141347012584,0.892244002792272,-3.62759872028588));
#16456=CARTESIAN_POINT('Ctrl Pts',(85.0995838599321,0.586259359639179,-3.68942663553642));
#16457=CARTESIAN_POINT('Ctrl Pts',(85.0805513678091,0.212363743369056,-3.71723823530693));
#16458=CARTESIAN_POINT('Ctrl Pts',(85.0772610466554,0.148470781483462,-3.72033792503272));
#16459=CARTESIAN_POINT('Ctrl Pts',(85.0716002164644,0.0400926945410302,
-3.72279948451585));
#16460=CARTESIAN_POINT('Ctrl Pts',(85.0692557557627,-0.00435970776291281,
-3.72301278485109));
#16461=CARTESIAN_POINT('Ctrl Pts',(85.0643789373947,-0.0958629766291269,
-3.72181310301018));
#16462=CARTESIAN_POINT('Ctrl Pts',(85.0618440808799,-0.142904408503924,
-3.72030382385572));
#16463=CARTESIAN_POINT('Ctrl Pts',(85.0551293303995,-0.266093901446509,
-3.71401154633122));
#16464=CARTESIAN_POINT('Ctrl Pts',(85.0509068507374,-0.342142874098028,
-3.70777896439628));
#16465=CARTESIAN_POINT('Ctrl Pts',(85.0362181452921,-0.601868186238297,
-3.67843478434));
#16466=CARTESIAN_POINT('Ctrl Pts',(85.0254414107457,-0.783969729701323,
-3.64396859276095));
#16467=CARTESIAN_POINT('Ctrl Pts',(85.0009552627431,-1.18532731820022,-3.53651868552044));
#16468=CARTESIAN_POINT('Ctrl Pts',(84.9872180388399,-1.40191405716723,-3.45638720978235));
#16469=CARTESIAN_POINT('Ctrl Pts',(84.9718707338294,-1.64789446364138,-3.33842850674785));
#16470=CARTESIAN_POINT('Ctrl Pts',(84.9695164666197,-1.68576682161008,-3.31946555624318));
#16471=CARTESIAN_POINT('Ctrl Pts',(84.9659081034696,-1.74418278175617,-3.2889585801291));
#16472=CARTESIAN_POINT('Ctrl Pts',(84.9646297084749,-1.76495336420293,-3.27785933186331));
#16473=CARTESIAN_POINT('Ctrl Pts',(84.961927736748,-1.80905081171537,-3.25375412549343));
#16474=CARTESIAN_POINT('Ctrl Pts',(84.960507774711,-1.83234598235991,-3.24069267713044));
#16475=CARTESIAN_POINT('Ctrl Pts',(84.9567150874877,-1.89480801702728,-3.20478174982224));
#16476=CARTESIAN_POINT('Ctrl Pts',(84.9543692210441,-1.9337023210387,-3.18146493993844));
#16477=CARTESIAN_POINT('Ctrl Pts',(84.9443354643363,-2.10051263966192,-3.07727394809547));
#16478=CARTESIAN_POINT('Ctrl Pts',(84.9369827810126,-2.22386541700076,-2.98934740188423));
#16479=CARTESIAN_POINT('Ctrl Pts',(84.9159627626948,-2.56360247213679,-2.71448092137758));
#16480=CARTESIAN_POINT('Ctrl Pts',(84.9024776027734,-2.76424147811763,-2.50986546867904));
#16481=CARTESIAN_POINT('Ctrl Pts',(84.8847550471818,-2.97832064635667,-2.23438445737353));
#16482=CARTESIAN_POINT('Ctrl Pts',(84.8814995092742,-3.01584937030715,-2.18346508142242));
#16483=CARTESIAN_POINT('Ctrl Pts',(84.8758793316965,-3.07745041164041,-2.09526432294667));
#16484=CARTESIAN_POINT('Ctrl Pts',(84.8735397712441,-3.10218702154537,-2.05846279565114));
#16485=CARTESIAN_POINT('Ctrl Pts',(84.8686558052075,-3.15192662118896,-1.98152995368773));
#16486=CARTESIAN_POINT('Ctrl Pts',(84.8661085388942,-3.17683413205588,-1.94134669859161));
#16487=CARTESIAN_POINT('Ctrl Pts',(84.8593165320083,-3.24050823784929,-1.83411320327146));
#16488=CARTESIAN_POINT('Ctrl Pts',(84.8550273615134,-3.2779579375688,-1.76631125667132));
#16489=CARTESIAN_POINT('Ctrl Pts',(84.8412594319495,-3.38956998045064,-1.548447751507));
#16490=CARTESIAN_POINT('Ctrl Pts',(84.831543517956,-3.45573829440158,-1.39453892485221));
#16491=CARTESIAN_POINT('Ctrl Pts',(84.8202647296711,-3.51942678638267,-1.21371224090924));
#16492=CARTESIAN_POINT('Ctrl Pts',(84.818827801575,-3.52730213564476,-1.19063090082885));
#16493=CARTESIAN_POINT('Ctrl Pts',(84.8045260992239,-3.60334936767769,-0.960370371252661));
#16494=CARTESIAN_POINT('Ctrl Pts',(84.791550227207,-3.65341923644053,-0.747646651339363));
#16495=CARTESIAN_POINT('Ctrl Pts',(84.7767654333701,-3.69088600924998,-0.488036032550343));
#16496=CARTESIAN_POINT('Ctrl Pts',(84.7743057493962,-3.69641713113331,-0.444206515957367));
#16497=CARTESIAN_POINT('Ctrl Pts',(84.7704330357799,-3.70401337983993,-0.373969471396635));
#16498=CARTESIAN_POINT('Ctrl Pts',(84.7689957101955,-3.70657900291763,-0.34762118329231));
#16499=CARTESIAN_POINT('Ctrl Pts',(84.7663402017868,-3.71084565512058,-0.298361757564472));
#16500=CARTESIAN_POINT('Ctrl Pts',(84.7651181604813,-3.71261605647989,-0.275458319804983));
#16501=CARTESIAN_POINT('Ctrl Pts',(84.7620086973118,-3.71661573803118,-0.216633771789246));
#16502=CARTESIAN_POINT('Ctrl Pts',(84.7601367848935,-3.71853638012616,-0.18069339852061));
#16503=CARTESIAN_POINT('Ctrl Pts',(84.755838637514,-3.72178703021132,-0.0971430511158404));
#16504=CARTESIAN_POINT('Ctrl Pts',(84.7534291834744,-3.7227252296709,-0.0495238594225499));
#16505=CARTESIAN_POINT('Ctrl Pts',(84.7510485996216,-3.72274951596391,-0.0018983915450042));
#16506=CARTESIAN_POINT('Ctrl Pts',(84.5967274725783,-2.62112000711956,2.64359555733807));
#16507=CARTESIAN_POINT('Ctrl Pts',(84.6026171986451,-2.69922371257001,2.56615588075135));
#16508=CARTESIAN_POINT('Ctrl Pts',(84.6085069247118,-2.77399981426397,2.48514542701443));
#16509=CARTESIAN_POINT('Ctrl Pts',(84.6143966507786,-2.8451029650521,2.40088664471102));
#16510=CARTESIAN_POINT('Ctrl Pts',(84.6202805304275,-2.91613553552328,2.31671150162044));
#16511=CARTESIAN_POINT('Ctrl Pts',(84.6261644100763,-2.98350213256905,2.22929476853713));
#16512=CARTESIAN_POINT('Ctrl Pts',(84.6320482897252,-3.04689454055936,2.13899537662183));
#16513=CARTESIAN_POINT('Ctrl Pts',(84.6379289762132,-3.11025254571151,2.04874498987079));
#16514=CARTESIAN_POINT('Ctrl Pts',(84.6438096627011,-3.16964040204038,1.95561540157729));
#16515=CARTESIAN_POINT('Ctrl Pts',(84.6496903491891,-3.22479085590767,1.8599977145562));
#16516=CARTESIAN_POINT('Ctrl Pts',(84.6555693742753,-3.27992572876026,1.76440704128536));
#16517=CARTESIAN_POINT('Ctrl Pts',(84.6614483993615,-3.3308253651958,1.66633003653838));
#16518=CARTESIAN_POINT('Ctrl Pts',(84.6673274244476,-3.37726694254101,1.56618503418967));
#16519=CARTESIAN_POINT('Ctrl Pts',(84.6732063181649,-3.42370748213289,1.46604226961615));
#16520=CARTESIAN_POINT('Ctrl Pts',(84.6790852118822,-3.46568998202649,1.36383198771931));
#16521=CARTESIAN_POINT('Ctrl Pts',(84.6849641055995,-3.50303890758951,1.259994434279));
#16522=CARTESIAN_POINT('Ctrl Pts',(84.6908477122249,-3.54041777450897,1.15607363782295));
#16523=CARTESIAN_POINT('Ctrl Pts',(84.6967313188503,-3.57315550128109,1.05052336672847));
#16524=CARTESIAN_POINT('Ctrl Pts',(84.7026149254756,-3.60112584615127,0.943800933820955));
#16525=CARTESIAN_POINT('Ctrl Pts',(84.7085008428755,-3.62910717631744,0.837036585895238));
#16526=CARTESIAN_POINT('Ctrl Pts',(84.7143867602754,-3.65231730426597,0.729099577227213));
#16527=CARTESIAN_POINT('Ctrl Pts',(84.7202726776752,-3.67068113579185,0.620457542336191));
#16528=CARTESIAN_POINT('Ctrl Pts',(84.7261672436868,-3.68907195064722,0.511655871705734));
#16529=CARTESIAN_POINT('Ctrl Pts',(84.7320618096985,-3.70260218924548,0.402147529924563));
#16530=CARTESIAN_POINT('Ctrl Pts',(84.73795637571,-3.71124864543577,0.292405633070136));
#16531=CARTESIAN_POINT('Ctrl Pts',(84.7432192876406,-3.7189685585475,0.194423536152382));
#16532=CARTESIAN_POINT('Ctrl Pts',(84.7484821995711,-3.72279601755899,0.0962555076601766));
#16533=CARTESIAN_POINT('Ctrl Pts',(84.7537451115017,-3.72274958225736,-0.00176360502600202));
#16534=CARTESIAN_POINT('Ctrl Pts',(84.3497092113127,-2.62112002533992,2.64359553927261));
#16535=CARTESIAN_POINT('Ctrl Pts',(84.3546425218072,-2.68061210737739,2.58460925137001));
#16536=CARTESIAN_POINT('Ctrl Pts',(84.3596011602631,-2.73813507340312,2.52359289680976));
#16537=CARTESIAN_POINT('Ctrl Pts',(84.3709873311534,-2.86576174273039,2.37869753085833));
#16538=CARTESIAN_POINT('Ctrl Pts',(84.3773963270634,-2.93430300190607,2.29361290023421));
#16539=CARTESIAN_POINT('Ctrl Pts',(84.3876729138189,-3.04025380739108,2.14955135947495));
#16540=CARTESIAN_POINT('Ctrl Pts',(84.3916171678889,-3.079921981068,2.09231832310341));
#16541=CARTESIAN_POINT('Ctrl Pts',(84.3971995718364,-3.13497507960041,2.00792634534748));
#16542=CARTESIAN_POINT('Ctrl Pts',(84.3989069315164,-3.1516591772335,1.9816360710892));
#16543=CARTESIAN_POINT('Ctrl Pts',(84.401947187844,-3.18113105962466,1.93388126126274));
#16544=CARTESIAN_POINT('Ctrl Pts',(84.403286765783,-3.19403518993944,1.91249334613323));
#16545=CARTESIAN_POINT('Ctrl Pts',(84.4064525911418,-3.22432020005884,1.86113589718298));
#16546=CARTESIAN_POINT('Ctrl Pts',(84.4082669282372,-3.2414995419462,1.83105119208179));
#16547=CARTESIAN_POINT('Ctrl Pts',(84.4146894730729,-3.3015222850743,1.72244550386871));
#16548=CARTESIAN_POINT('Ctrl Pts',(84.4191753486541,-3.34195496938704,1.64262196725123));
#16549=CARTESIAN_POINT('Ctrl Pts',(84.4361098694402,-3.48615963720086,1.3305100808022));
#16550=CARTESIAN_POINT('Ctrl Pts',(84.4479914823629,-3.56890153561116,1.08927441714604));
#16551=CARTESIAN_POINT('Ctrl Pts',(84.4668897857842,-3.65653965255822,0.711592481441709));
#16552=CARTESIAN_POINT('Ctrl Pts',(84.473507464344,-3.67967662088619,0.58019128387289));
#16553=CARTESIAN_POINT('Ctrl Pts',(84.4831974327259,-3.70244347491494,0.392311637265982));
#16554=CARTESIAN_POINT('Ctrl Pts',(84.4860959566969,-3.70791962231769,0.336641886761319));
#16555=CARTESIAN_POINT('Ctrl Pts',(84.4913155253879,-3.71542002257566,0.237512876096766));
#16556=CARTESIAN_POINT('Ctrl Pts',(84.4936210795109,-3.71794066887489,0.194101216628514));
#16557=CARTESIAN_POINT('Ctrl Pts',(84.498661511634,-3.72174915842175,0.100069848188601));
#16558=CARTESIAN_POINT('Ctrl Pts',(84.5014041514759,-3.72276581131591,0.0494484318281852));
#16559=CARTESIAN_POINT('Ctrl Pts',(84.5094561643464,-3.72271936821563,-0.0975257749299699));
#16560=CARTESIAN_POINT('Ctrl Pts',(84.5148444201971,-3.71894850872693,-0.193831203364285));
#16561=CARTESIAN_POINT('Ctrl Pts',(84.5280396087446,-3.70089586081381,-0.424969055916771));
#16562=CARTESIAN_POINT('Ctrl Pts',(84.5359321790091,-3.6829774649357,-0.55937598081174));
#16563=CARTESIAN_POINT('Ctrl Pts',(84.5578033575243,-3.61382963707513,-0.924614276726773));
#16564=CARTESIAN_POINT('Ctrl Pts',(84.5719207963187,-3.54788959126416,-1.1520258440117));
#16565=CARTESIAN_POINT('Ctrl Pts',(84.5879553685414,-3.44339907249679,-1.4156663398813));
#16566=CARTESIAN_POINT('Ctrl Pts',(84.5905984927436,-3.42511900395839,-1.45933840121242));
#16567=CARTESIAN_POINT('Ctrl Pts',(84.5946871583552,-3.39506901312689,-1.52745170224194));
#16568=CARTESIAN_POINT('Ctrl Pts',(84.5961615701025,-3.38385700256842,-1.55213214073889));
#16569=CARTESIAN_POINT('Ctrl Pts',(84.5990449603415,-3.36115602275812,-1.60068721937661));
#16570=CARTESIAN_POINT('Ctrl Pts',(84.6004544532229,-3.34967987386434,-1.62456584571078));
#16571=CARTESIAN_POINT('Ctrl Pts',(84.6041824903521,-3.3183437910243,-1.68802332653556));
#16572=CARTESIAN_POINT('Ctrl Pts',(84.6064757621696,-3.29803040588654,-1.7273748962317));
#16573=CARTESIAN_POINT('Ctrl Pts',(84.6116274072054,-3.25017685600444,-1.81615482901501));
#16574=CARTESIAN_POINT('Ctrl Pts',(84.6144653321263,-3.22220205097662,-1.86533707402179));
#16575=CARTESIAN_POINT('Ctrl Pts',(84.624236301421,-3.1207866644609,-2.03453981501924));
#16576=CARTESIAN_POINT('Ctrl Pts',(84.6309798232979,-3.04167118982644,-2.15102335977938));
#16577=CARTESIAN_POINT('Ctrl Pts',(84.648701250769,-2.81686819763753,-2.4447147784816));
#16578=CARTESIAN_POINT('Ctrl Pts',(84.6596661181123,-2.66108963499289,-2.61342103503158));
#16579=CARTESIAN_POINT('Ctrl Pts',(84.6747278479668,-2.43958292500034,-2.81283707854977));
#16580=CARTESIAN_POINT('Ctrl Pts',(84.6782598319896,-2.38709498621008,-2.85751536462328));
#16581=CARTESIAN_POINT('Ctrl Pts',(84.6842305044487,-2.29776786785886,-2.92937220770402));
#16582=CARTESIAN_POINT('Ctrl Pts',(84.6866366374356,-2.26161251891279,-2.95737506564155));
#16583=CARTESIAN_POINT('Ctrl Pts',(84.6915151082924,-2.18806669136302,-3.01219989859036));
#16584=CARTESIAN_POINT('Ctrl Pts',(84.693987330951,-2.15067652219217,-3.03900877225089));
#16585=CARTESIAN_POINT('Ctrl Pts',(84.7003124425367,-2.05477241656622,-3.10511594194083));
#16586=CARTESIAN_POINT('Ctrl Pts',(84.7041990459056,-1.9956233393541,-3.14345690006567));
#16587=CARTESIAN_POINT('Ctrl Pts',(84.712918677061,-1.86248836521959,-3.22448363374186));
#16588=CARTESIAN_POINT('Ctrl Pts',(84.7177756466539,-1.78805082798849,-3.26634818049653));
#16589=CARTESIAN_POINT('Ctrl Pts',(84.7348299721388,-1.52531747284678,-3.40243888500404));
#16590=CARTESIAN_POINT('Ctrl Pts',(84.7473468256508,-1.33052279992698,-3.4832288539473));
#16591=CARTESIAN_POINT('Ctrl Pts',(84.76788386942,-0.997850851148307,-3.58920405298518));
#16592=CARTESIAN_POINT('Ctrl Pts',(84.7759570145586,-0.863481240740499,
-3.62387885383581));
#16593=CARTESIAN_POINT('Ctrl Pts',(84.7858809971974,-0.68971368566898,-3.65850319749194));
#16594=CARTESIAN_POINT('Ctrl Pts',(84.7880135066625,-0.6518297348069,-3.66544251646989));
#16595=CARTESIAN_POINT('Ctrl Pts',(84.7914917940829,-0.588994228358466,
-3.67594723925156));
#16596=CARTESIAN_POINT('Ctrl Pts',(84.7928544193103,-0.564102494804995,
-3.67984929239526));
#16597=CARTESIAN_POINT('Ctrl Pts',(84.7957460590942,-0.510644344919281,
-3.68767421882953));
#16598=CARTESIAN_POINT('Ctrl Pts',(84.7972710677173,-0.482068855933844,
-3.6915184562593));
#16599=CARTESIAN_POINT('Ctrl Pts',(84.8017233148346,-0.397639780640664,
-3.70187951412336));
#16600=CARTESIAN_POINT('Ctrl Pts',(84.8046054858955,-0.341678089832645,
-3.7074635570398));
#16601=CARTESIAN_POINT('Ctrl Pts',(84.8114337865579,-0.206743936676068,
-3.71784628455022));
#16602=CARTESIAN_POINT('Ctrl Pts',(84.8153344486984,-0.127702141772687,
-3.72139991209022));
#16603=CARTESIAN_POINT('Ctrl Pts',(84.8345807201097,0.267364908873462,-3.7265583250506));
#16604=CARTESIAN_POINT('Ctrl Pts',(84.849260887943,0.582562327217847,-3.69044016638166));
#16605=CARTESIAN_POINT('Ctrl Pts',(84.8689025965965,0.961687145052707,-3.59716061791241));
#16606=CARTESIAN_POINT('Ctrl Pts',(84.8727024635736,1.03340423358019,-3.57721699737138));
#16607=CARTESIAN_POINT('Ctrl Pts',(84.8789959196215,1.14909197302861,-3.54127635666802));
#16608=CARTESIAN_POINT('Ctrl Pts',(84.8814486566974,1.19344497172963,-3.52657616399787));
#16609=CARTESIAN_POINT('Ctrl Pts',(84.8863255408438,1.28011183520681,-3.49602943283517));
#16610=CARTESIAN_POINT('Ctrl Pts',(84.8887475227697,1.32243718193637,-3.48023961326192));
#16611=CARTESIAN_POINT('Ctrl Pts',(84.8947511138191,1.42554981714395,-3.43962002105868));
#16612=CARTESIAN_POINT('Ctrl Pts',(84.8983595747667,1.48598597784304,-3.41394538787247));
#16613=CARTESIAN_POINT('Ctrl Pts',(84.9145404220927,1.75016928798928,-3.29337016027291));
#16614=CARTESIAN_POINT('Ctrl Pts',(84.9276492091179,1.94573484863204,-3.18174053458709));
#16615=CARTESIAN_POINT('Ctrl Pts',(84.9532420129863,2.30141313122155,-2.93360502451104));
#16616=CARTESIAN_POINT('Ctrl Pts',(84.9656507130217,2.46244362557708,-2.79980746806889));
#16617=CARTESIAN_POINT('Ctrl Pts',(84.9799184722144,2.64285480987267,-2.62223831936189));
#16618=CARTESIAN_POINT('Ctrl Pts',(84.9823759499848,2.67375720602408,-2.59072153768956));
#16619=CARTESIAN_POINT('Ctrl Pts',(84.9862461200811,2.72228230590524,-2.53943832032324));
#16620=CARTESIAN_POINT('Ctrl Pts',(84.9876830526767,2.74026671316064,-2.52002110810626));
#16621=CARTESIAN_POINT('Ctrl Pts',(84.9905624032274,2.77627622563386,-2.48030135313373));
#16622=CARTESIAN_POINT('Ctrl Pts',(84.9920040440085,2.79428925589946,-2.45999026957238));
#16623=CARTESIAN_POINT('Ctrl Pts',(84.9959297417642,2.84322275496985,-2.4035828888023));
#16624=CARTESIAN_POINT('Ctrl Pts',(84.9983835871451,2.87367749904876,-2.36708773820864));
#16625=CARTESIAN_POINT('Ctrl Pts',(85.0039760887491,2.94245505296496,-2.28138429292121));
#16626=CARTESIAN_POINT('Ctrl Pts',(85.0070887152721,2.98025732090569,-2.23177574181176));
#16627=CARTESIAN_POINT('Ctrl Pts',(85.0185648194923,3.11670618534649,-2.0430579984548));
#16628=CARTESIAN_POINT('Ctrl Pts',(85.0266666177967,3.20700741484958,-1.89817057062981));
#16629=CARTESIAN_POINT('Ctrl Pts',(85.0438943628245,3.37556394950495,-1.58113230508593));
#16630=CARTESIAN_POINT('Ctrl Pts',(85.0530195233058,3.4512890778597,-1.40819302504942));
#16631=CARTESIAN_POINT('Ctrl Pts',(85.0660109939238,3.53621385168474,-1.16565301833298));
#16632=CARTESIAN_POINT('Ctrl Pts',(85.0695210442296,3.55705261892887,-1.10042323551924));
#16633=CARTESIAN_POINT('Ctrl Pts',(85.0754655470594,3.58876800525969,-0.99080563590118));
#16634=CARTESIAN_POINT('Ctrl Pts',(85.0778680993223,3.60064770608313,-0.946724595775906));
#16635=CARTESIAN_POINT('Ctrl Pts',(85.082748123297,3.62288739772546,-0.857717437968567));
#16636=CARTESIAN_POINT('Ctrl Pts',(85.0852256668082,3.63322942484477,-0.81279517157289));
#16637=CARTESIAN_POINT('Ctrl Pts',(85.0915837520213,3.65736948030658,-0.698249743210625));
#16638=CARTESIAN_POINT('Ctrl Pts',(85.095498729564,3.67001506327405,-0.628404912958072));
#16639=CARTESIAN_POINT('Ctrl Pts',(85.1042959845805,3.69358477160547,-0.473003445243937));
#16640=CARTESIAN_POINT('Ctrl Pts',(85.1092029291424,3.70354750565902,-0.387343705000337));
#16641=CARTESIAN_POINT('Ctrl Pts',(85.126596933153,3.72796870382054,-0.0867143048216947));
#16642=CARTESIAN_POINT('Ctrl Pts',(85.1394183000811,3.72674060072934,0.129091739340578));
#16643=CARTESIAN_POINT('Ctrl Pts',(85.1598575977116,3.69463973859095,0.475444047252364));
#16644=CARTESIAN_POINT('Ctrl Pts',(85.1675555825175,3.67538615230655,0.606590205940345));
#16645=CARTESIAN_POINT('Ctrl Pts',(85.1771158314097,3.64161019859385,0.773955767594703));
#16646=CARTESIAN_POINT('Ctrl Pts',(85.179234631196,3.63346062847825,0.811354704571847));
#16647=CARTESIAN_POINT('Ctrl Pts',(85.1826972983423,3.6190005250616,0.873118370521107));
#16648=CARTESIAN_POINT('Ctrl Pts',(85.1840576968601,3.61301723882062,0.897556156096714));
#16649=CARTESIAN_POINT('Ctrl Pts',(85.1869523224538,3.59962106044714,0.94996468101585));
#16650=CARTESIAN_POINT('Ctrl Pts',(85.1884823846651,3.59212910964458,0.977912694539554));
#16651=CARTESIAN_POINT('Ctrl Pts',(85.192967893653,3.568970590119,1.06044373238354));
#16652=CARTESIAN_POINT('Ctrl Pts',(85.1958772412779,3.55237967468349,1.11476062781221));
#16653=CARTESIAN_POINT('Ctrl Pts',(85.2027872708971,3.50936458033948,1.24485541880959));
#16654=CARTESIAN_POINT('Ctrl Pts',(85.2067409966739,3.48172017835727,1.32020093105392));
#16655=CARTESIAN_POINT('Ctrl Pts',(85.2180823766607,3.39444499365084,1.53620909772717));
#16656=CARTESIAN_POINT('Ctrl Pts',(85.2253388973998,3.32856692658448,1.67416827599768));
#16657=CARTESIAN_POINT('Ctrl Pts',(85.2410436683723,3.16989163459986,1.95983227580369));
#16658=CARTESIAN_POINT('Ctrl Pts',(85.2495023220511,3.07482457616018,2.10584967689417));
#16659=CARTESIAN_POINT('Ctrl Pts',(85.2617398911134,2.92893577849752,2.29887327896219));
#16660=CARTESIAN_POINT('Ctrl Pts',(85.2652241509502,2.88649753061265,2.3519384421253));
#16661=CARTESIAN_POINT('Ctrl Pts',(85.2709010511713,2.8161492148612,2.43512902468597));
#16662=CARTESIAN_POINT('Ctrl Pts',(85.2730579411314,2.7891506599999,2.46600652658258));
#16663=CARTESIAN_POINT('Ctrl Pts',(85.2776415935549,2.73125754398276,2.53005012436876));
#16664=CARTESIAN_POINT('Ctrl Pts',(85.280072531138,2.70025654879109,2.56311055782589));
#16665=CARTESIAN_POINT('Ctrl Pts',(85.2861348167576,2.62226764885239,2.64329480692903));
#16666=CARTESIAN_POINT('Ctrl Pts',(85.2897942444364,2.57460635569363,2.68973909696347));
#16667=CARTESIAN_POINT('Ctrl Pts',(85.3034275194096,2.39499752822537,2.85561224541495));
#16668=CARTESIAN_POINT('Ctrl Pts',(85.3137102570149,2.25579212138062,2.96680376765666));
#16669=CARTESIAN_POINT('Ctrl Pts',(85.3390006099171,1.90101237685729,3.21073849834573));
#16670=CARTESIAN_POINT('Ctrl Pts',(85.3541374800096,1.67880840364266,3.33231146350343));
#16671=CARTESIAN_POINT('Ctrl Pts',(85.3709141654963,1.40471472741503,3.44784736342914));
#16672=CARTESIAN_POINT('Ctrl Pts',(85.3734104222247,1.36311660588644,3.46450405866438));
#16673=CARTESIAN_POINT('Ctrl Pts',(85.3773261940875,1.29636051776932,3.48984589578087));
#16674=CARTESIAN_POINT('Ctrl Pts',(85.3787708962779,1.27139350176222,3.49901895286059));
#16675=CARTESIAN_POINT('Ctrl Pts',(85.3816501553886,1.22089448978339,3.51696073440474));
#16676=CARTESIAN_POINT('Ctrl Pts',(85.383084228597,1.1953612431606,3.52572088348676));
#16677=CARTESIAN_POINT('Ctrl Pts',(85.386963405192,1.12534039699767,3.54889606166907));
#16678=CARTESIAN_POINT('Ctrl Pts',(85.3893794862127,1.08067174557414,3.56275219719353));
#16679=CARTESIAN_POINT('Ctrl Pts',(85.4001148621791,0.878228383851434,3.62139173424208));
#16680=CARTESIAN_POINT('Ctrl Pts',(85.4080426475064,0.717848812927682,3.65656459621806));
#16681=CARTESIAN_POINT('Ctrl Pts',(85.428586926304,0.294683416065642,3.72044230909833));
#16682=CARTESIAN_POINT('Ctrl Pts',(85.4411087798052,0.0302761415880997,
3.73197041859556));
#16683=CARTESIAN_POINT('Ctrl Pts',(85.4578286262312,-0.29911254598409,3.71130314038781));
#16684=CARTESIAN_POINT('Ctrl Pts',(85.4612242458891,-0.364977212526694,
3.70540554909866));
#16685=CARTESIAN_POINT('Ctrl Pts',(85.4670090376998,-0.475145527758885,
3.69257514701699));
#16686=CARTESIAN_POINT('Ctrl Pts',(85.4693691721422,-0.519544989957933,
3.68659019485562));
#16687=CARTESIAN_POINT('Ctrl Pts',(85.474229480708,-0.60978872310713,3.67276293703801));
#16688=CARTESIAN_POINT('Ctrl Pts',(85.4767311338216,-0.655615537576436,
3.66485987221069));
#16689=CARTESIAN_POINT('Ctrl Pts',(85.4832395072245,-0.773182520215193,
3.64230921161286));
#16690=CARTESIAN_POINT('Ctrl Pts',(85.487284027,-0.844657878632875,3.62640037271484));
#16691=CARTESIAN_POINT('Ctrl Pts',(85.4964387681904,-1.00292135129857,3.58624170739158));
#16692=CARTESIAN_POINT('Ctrl Pts',(85.5015771493159,-1.08939050622804,3.56092790127404));
#16693=CARTESIAN_POINT('Ctrl Pts',(85.520693131495,-1.40318706911168,3.45656436676044));
#16694=CARTESIAN_POINT('Ctrl Pts',(85.5350869986141,-1.62361723200026,3.35866453585474));
#16695=CARTESIAN_POINT('Ctrl Pts',(85.5551668799099,-1.92313195969921,3.18922337607143));
#16696=CARTESIAN_POINT('Ctrl Pts',(85.5611254427033,-2.0110678368837,3.13451613488043));
#16697=CARTESIAN_POINT('Ctrl Pts',(85.5689260043489,-2.12650198376631,3.0558411414526));
#16698=CARTESIAN_POINT('Ctrl Pts',(85.5709234868712,-2.15609221874516,3.03503580003459));
#16699=CARTESIAN_POINT('Ctrl Pts',(85.5742631658348,-2.20571358658557,2.99905422758009));
#16700=CARTESIAN_POINT('Ctrl Pts',(85.5756188393707,-2.22590215299836,2.98410093884328));
#16701=CARTESIAN_POINT('Ctrl Pts',(85.5785691957999,-2.26995988419176,2.95077224761442));
#16702=CARTESIAN_POINT('Ctrl Pts',(85.5801582371514,-2.2937597757726,2.93230983019852));
#16703=CARTESIAN_POINT('Ctrl Pts',(85.5850429041051,-2.36700938840469,2.87404990181377));
#16704=CARTESIAN_POINT('Ctrl Pts',(85.5882792277949,-2.41566911748086,2.83327369662885));
#16705=CARTESIAN_POINT('Ctrl Pts',(85.5950764191946,-2.51730318488695,2.74358279703725));
#16706=CARTESIAN_POINT('Ctrl Pts',(85.598620270255,-2.56994374939982,2.69433672039096));
#16707=CARTESIAN_POINT('Ctrl Pts',(85.6021262427416,-2.62112000930789,2.64359555516834));
#16708=CARTESIAN_POINT('Origin',(80.1322559480305,0.,0.));
#16709=CARTESIAN_POINT('',(87.0941439883772,-2.62111999291044,2.64359557142638));
#16710=CARTESIAN_POINT('',(86.8469367975669,-2.62112000772923,2.64359555673358));
#16711=CARTESIAN_POINT('',(80.1322559480305,-2.62112000711956,2.64359555733806));
#16712=CARTESIAN_POINT('Ctrl Pts',(87.0941439883772,-2.62111999291044,2.64359557142638));
#16713=CARTESIAN_POINT('Ctrl Pts',(87.091234710344,-2.57927384666699,2.68508594602471));
#16714=CARTESIAN_POINT('Ctrl Pts',(87.0883621998307,-2.53643946225557,2.72558579927331));
#16715=CARTESIAN_POINT('Ctrl Pts',(87.0751689172554,-2.33394346756449,2.9081323252061));
#16716=CARTESIAN_POINT('Ctrl Pts',(87.0650941661905,-2.16321393192004,3.03727380232705));
#16717=CARTESIAN_POINT('Ctrl Pts',(87.0504372145944,-1.90961892014635,3.19681187581807));
#16718=CARTESIAN_POINT('Ctrl Pts',(87.0461806764361,-1.83533027562482,3.24003275801531));
#16719=CARTESIAN_POINT('Ctrl Pts',(87.0382735907821,-1.69722498701445,3.31410732065542));
#16720=CARTESIAN_POINT('Ctrl Pts',(87.0346500589835,-1.63389525245935,3.34578324019333));
#16721=CARTESIAN_POINT('Ctrl Pts',(87.028569442854,-1.52793389649372,3.39505633437968));
#16722=CARTESIAN_POINT('Ctrl Pts',(87.0261476761901,-1.48580888212723,3.4137019825099));
#16723=CARTESIAN_POINT('Ctrl Pts',(87.0212723765704,-1.40124353522606,3.44927104204571));
#16724=CARTESIAN_POINT('Ctrl Pts',(87.0188197000595,-1.35881609967048,3.46620436865924));
#16725=CARTESIAN_POINT('Ctrl Pts',(87.0126182982754,-1.2518944315951,3.50661338693058));
#16726=CARTESIAN_POINT('Ctrl Pts',(87.0088385463976,-1.18704435583023,3.52909364801014));
#16727=CARTESIAN_POINT('Ctrl Pts',(86.9941201512639,-0.93581211070486,3.60847497750482));
#16728=CARTESIAN_POINT('Ctrl Pts',(86.9828048860468,-0.745708861740775,
3.6524976899244));
#16729=CARTESIAN_POINT('Ctrl Pts',(86.9615749957209,-0.389271763427499,
3.7060443984394));
#16730=CARTESIAN_POINT('Ctrl Pts',(86.9517339586807,-0.224028354117965,
3.71969226663774));
#16731=CARTESIAN_POINT('Ctrl Pts',(86.9385603172174,0.00304872113064497,
3.7232563760466));
#16732=CARTESIAN_POINT('Ctrl Pts',(86.9350293986215,0.0645381599798527,
3.72269832176204));
#16733=CARTESIAN_POINT('Ctrl Pts',(86.9288949343423,0.173003292476461,3.71902546379455));
#16734=CARTESIAN_POINT('Ctrl Pts',(86.9262689318477,0.219986391202562,3.71654233430373));
#16735=CARTESIAN_POINT('Ctrl Pts',(86.9222002944552,0.293891133961937,3.71122987822687));
#16736=CARTESIAN_POINT('Ctrl Pts',(86.920729233345,0.320849354963846,3.70899649341275));
#16737=CARTESIAN_POINT('Ctrl Pts',(86.9178463775644,0.374212645525434,3.70398936378226));
#16738=CARTESIAN_POINT('Ctrl Pts',(86.9164341798328,0.400616964721536,3.70122661066823));
#16739=CARTESIAN_POINT('Ctrl Pts',(86.9126895916483,0.471247353124605,3.69307166354918));
#16740=CARTESIAN_POINT('Ctrl Pts',(86.9103828737011,0.515411187451082,3.68716747884026));
#16741=CARTESIAN_POINT('Ctrl Pts',(86.8951303223451,0.810717408010992,3.64227864855071));
#16742=CARTESIAN_POINT('Ctrl Pts',(86.8831861308858,1.05742771334007,3.57845339306033));
#16743=CARTESIAN_POINT('Ctrl Pts',(86.8624562488596,1.46178423452129,3.42832760359663));
#16744=CARTESIAN_POINT('Ctrl Pts',(86.8538445630491,1.6232189039216,3.35490637898227));
#16745=CARTESIAN_POINT('Ctrl Pts',(86.8415102271794,1.83715658282693,3.23853911018966));
#16746=CARTESIAN_POINT('Ctrl Pts',(86.8380996896994,1.89464596396203,3.20524505688366));
#16747=CARTESIAN_POINT('Ctrl Pts',(86.8322737385911,1.98979115161382,3.14668886916404));
#16748=CARTESIAN_POINT('Ctrl Pts',(86.8298873161157,2.02793267179682,3.12224414641387));
#16749=CARTESIAN_POINT('Ctrl Pts',(86.8252910676337,2.09975512704548,3.07434216112538));
#16750=CARTESIAN_POINT('Ctrl Pts',(86.8230860974373,2.13351292703815,3.05101191854651));
#16751=CARTESIAN_POINT('Ctrl Pts',(86.8171692110018,2.22221803790045,2.98751509031372));
#16752=CARTESIAN_POINT('Ctrl Pts',(86.8134222422132,2.27645938652393,2.9463929252939));
#16753=CARTESIAN_POINT('Ctrl Pts',(86.7959460958633,2.52059790445449,2.75053614468384));
#16754=CARTESIAN_POINT('Ctrl Pts',(86.7815736230602,2.69603966561627,2.57879913774977));
#16755=CARTESIAN_POINT('Ctrl Pts',(86.7557831455884,2.976543323531,2.24407201686349));
#16756=CARTESIAN_POINT('Ctrl Pts',(86.7444550819635,3.08821906628995,2.08772183895059));
#16757=CARTESIAN_POINT('Ctrl Pts',(86.7314503638769,3.20798010367828,1.88926584402681));
#16758=CARTESIAN_POINT('Ctrl Pts',(86.7292360530217,3.22805921721248,1.85474950311365));
#16759=CARTESIAN_POINT('Ctrl Pts',(86.7256500133549,3.26013254986333,1.79751568543212));
#16760=CARTESIAN_POINT('Ctrl Pts',(86.724259810935,3.27245364637974,1.77498567652399));
#16761=CARTESIAN_POINT('Ctrl Pts',(86.7213639468827,3.2979008403936,1.72728779473046));
#16762=CARTESIAN_POINT('Ctrl Pts',(86.7198612343079,3.31097391549297,1.70209427154438));
#16763=CARTESIAN_POINT('Ctrl Pts',(86.715552969407,3.34800737589311,1.62868437483962));
#16764=CARTESIAN_POINT('Ctrl Pts',(86.7127881618465,3.3712123098086,1.58009312673608));
#16765=CARTESIAN_POINT('Ctrl Pts',(86.7046950683262,3.43703218331002,1.43420918774034));
#16766=CARTESIAN_POINT('Ctrl Pts',(86.6994914317596,3.47654841031451,1.33557472888027));
#16767=CARTESIAN_POINT('Ctrl Pts',(86.6840090581203,3.5827159194742,1.03377424405145));
#16768=CARTESIAN_POINT('Ctrl Pts',(86.673932548184,3.63614415233331,0.826437651324505));
#16769=CARTESIAN_POINT('Ctrl Pts',(86.6592734084947,3.6856997688977,0.53091331183854));
#16770=CARTESIAN_POINT('Ctrl Pts',(86.6550165598259,3.69697175782733,0.44570220647882));
#16771=CARTESIAN_POINT('Ctrl Pts',(86.6471089674876,3.71213530202019,0.289710271656887));
#16772=CARTESIAN_POINT('Ctrl Pts',(86.6434852456678,3.71697343771286,0.219062096731713));
#16773=CARTESIAN_POINT('Ctrl Pts',(86.6374044008693,3.72162944582098,0.102292904319072));
#16774=CARTESIAN_POINT('Ctrl Pts',(86.6349826013614,3.72261022495269,0.0562355517218713));
#16775=CARTESIAN_POINT('Ctrl Pts',(86.6301073051167,3.72286092596252,-0.0355054231258351));
#16776=CARTESIAN_POINT('Ctrl Pts',(86.6276546663145,3.72214501490199,-0.0811809627238327));
#16777=CARTESIAN_POINT('Ctrl Pts',(86.6214535046793,3.71825097383426,-0.195413189595637));
#16778=CARTESIAN_POINT('Ctrl Pts',(86.6176739603969,3.71401733190922,-0.263914841127556));
#16779=CARTESIAN_POINT('Ctrl Pts',(86.6029653253518,3.69051757253894,-0.526165055799792));
#16780=CARTESIAN_POINT('Ctrl Pts',(86.5916603801591,3.65795985707613,-0.718390179630367));
#16781=CARTESIAN_POINT('Ctrl Pts',(86.5704332110095,3.57013733808099,-1.06792337880992));
#16782=CARTESIAN_POINT('Ctrl Pts',(86.5605842079323,3.5190553710567,-1.22580256063017));
#16783=CARTESIAN_POINT('Ctrl Pts',(86.5474013957484,3.43482667150271,-1.43687716921547));
#16784=CARTESIAN_POINT('Ctrl Pts',(86.5438690545387,3.41061861836088,-1.49342945457998));
#16785=CARTESIAN_POINT('Ctrl Pts',(86.5377324247055,3.36543564296836,-1.5921446892173));
#16786=CARTESIAN_POINT('Ctrl Pts',(86.5351056586267,3.34504142930956,-1.63455804739113));
#16787=CARTESIAN_POINT('Ctrl Pts',(86.531036123131,3.31166474033107,-1.7007280788922));
#16788=CARTESIAN_POINT('Ctrl Pts',(86.5295649079841,3.29921853093252,-1.72474824972293));
#16789=CARTESIAN_POINT('Ctrl Pts',(86.5266820181287,3.27404275807684,-1.77206551926204));
#16790=CARTESIAN_POINT('Ctrl Pts',(86.525269935454,3.26132372346861,-1.79536620823842));
#16791=CARTESIAN_POINT('Ctrl Pts',(86.521526061774,3.22659910322151,-1.85739321627774));
#16792=CARTESIAN_POINT('Ctrl Pts',(86.5192199257933,3.20414532689804,-1.89586507586917));
#16793=CARTESIAN_POINT('Ctrl Pts',(86.503964144065,3.04894413769073,-2.15114671041387));
#16794=CARTESIAN_POINT('Ctrl Pts',(86.4920168411387,2.89496739083631,-2.35429011359411));
#16795=CARTESIAN_POINT('Ctrl Pts',(86.4712852251985,2.60063532172118,-2.6696303005918));
#16796=CARTESIAN_POINT('Ctrl Pts',(86.4626752456974,2.47072070710897,-2.7902978916309));
#16797=CARTESIAN_POINT('Ctrl Pts',(86.4503430188948,2.28095743290653,-2.94287484692372));
#16798=CARTESIAN_POINT('Ctrl Pts',(86.4469327394015,2.22809189548189,-2.98309989879739));
#16799=CARTESIAN_POINT('Ctrl Pts',(86.4411070955824,2.13740957935147,-3.04834379191097));
#16800=CARTESIAN_POINT('Ctrl Pts',(86.4387207150123,2.10015989208887,-3.07412553030201));
#16801=CARTESIAN_POINT('Ctrl Pts',(86.4341244595709,2.02828856245078,-3.12195401847443));
#16802=CARTESIAN_POINT('Ctrl Pts',(86.4319194386632,1.99375449651386,-3.14412057869629));
#16803=CARTESIAN_POINT('Ctrl Pts',(86.426002195275,1.90098311538947,-3.20152516143294));
#16804=CARTESIAN_POINT('Ctrl Pts',(86.4222549122829,1.84213575449728,-3.23574337857887));
#16805=CARTESIAN_POINT('Ctrl Pts',(86.4085932330683,1.62732783423568,-3.35288909819996));
#16806=CARTESIAN_POINT('Ctrl Pts',(86.3983796386424,1.46646432188542,-3.42630007277247));
#16807=CARTESIAN_POINT('Ctrl Pts',(86.3774232449251,1.13228802828112,-3.55094642527077));
#16808=CARTESIAN_POINT('Ctrl Pts',(86.3667023622961,0.959218475685186,-3.60155484728061));
#16809=CARTESIAN_POINT('Ctrl Pts',(86.3508705634862,0.692808651888334,-3.65888318765684));
#16810=CARTESIAN_POINT('Ctrl Pts',(86.345577330563,0.60175253614416,-3.67495662261087));
#16811=CARTESIAN_POINT('Ctrl Pts',(86.3385235647833,0.476277003299358,-3.69231630235341));
#16812=CARTESIAN_POINT('Ctrl Pts',(86.3366376564716,0.442302673423051,-3.6965400002081));
#16813=CARTESIAN_POINT('Ctrl Pts',(86.3334193235122,0.383478668138524,-3.70303037436475));
#16814=CARTESIAN_POINT('Ctrl Pts',(86.3320759896681,0.358656856810983,-3.70551685988385));
#16815=CARTESIAN_POINT('Ctrl Pts',(86.3290711156063,0.302512163386443,-3.71057157847395));
#16816=CARTESIAN_POINT('Ctrl Pts',(86.3274170929586,0.27117901036536,-3.71299301401829));
#16817=CARTESIAN_POINT('Ctrl Pts',(86.322058361885,0.168444805649324,-3.71962488191335));
#16818=CARTESIAN_POINT('Ctrl Pts',(86.3184307732184,0.0969495923947637,
-3.72217474645538));
#16819=CARTESIAN_POINT('Ctrl Pts',(86.301140067071,-0.249946241598828,-3.72454364688135));
#16820=CARTESIAN_POINT('Ctrl Pts',(86.2883343425865,-0.524685446967067,
-3.69586571150935));
#16821=CARTESIAN_POINT('Ctrl Pts',(86.2703371553668,-0.885919711062651,
-3.61703073702839));
#16822=CARTESIAN_POINT('Ctrl Pts',(86.2656890673109,-0.977275751649216,
-3.5934239723411));
#16823=CARTESIAN_POINT('Ctrl Pts',(86.2571471206628,-1.14008979882564,-3.54468379837117));
#16824=CARTESIAN_POINT('Ctrl Pts',(86.2532885893692,-1.21186497192525,-3.52079114814455));
#16825=CARTESIAN_POINT('Ctrl Pts',(86.2469241736505,-1.32692718729817,-3.47855363718965));
#16826=CARTESIAN_POINT('Ctrl Pts',(86.244461049937,-1.37068320718194,-3.46154567407277));
#16827=CARTESIAN_POINT('Ctrl Pts',(86.239609245014,-1.4552856064792,-3.42680509958048));
#16828=CARTESIAN_POINT('Ctrl Pts',(86.2372236896611,-1.49615860917684,-3.40915804466471));
#16829=CARTESIAN_POINT('Ctrl Pts',(86.2313283567601,-1.59534948342596,-3.36420469838027));
#16830=CARTESIAN_POINT('Ctrl Pts',(86.2277929668989,-1.65329272174107,-3.3361108661339));
#16831=CARTESIAN_POINT('Ctrl Pts',(86.2087679124266,-1.95690823409506,-3.17904981015634));
#16832=CARTESIAN_POINT('Ctrl Pts',(86.1924049772516,-2.18828718485437,-3.02443480990461));
#16833=CARTESIAN_POINT('Ctrl Pts',(86.1692538297488,-2.48817075252099,-2.7714772367783));
#16834=CARTESIAN_POINT('Ctrl Pts',(86.1624958015562,-2.57255569733065,-2.69333232559858));
#16835=CARTESIAN_POINT('Ctrl Pts',(86.152967932467,-2.68870537949301,-2.57532405589478));
#16836=CARTESIAN_POINT('Ctrl Pts',(86.1500838301582,-2.72348020859216,-2.53852054599982));
#16837=CARTESIAN_POINT('Ctrl Pts',(86.1449484390948,-2.78491047515975,-2.47079066460091));
#16838=CARTESIAN_POINT('Ctrl Pts',(86.1426832719786,-2.81182843066204,-2.44011352379744));
#16839=CARTESIAN_POINT('Ctrl Pts',(86.1390382580498,-2.85495351897188,-2.38930434658693));
#16840=CARTESIAN_POINT('Ctrl Pts',(86.1376387504644,-2.87146476911752,-2.36943560180076));
#16841=CARTESIAN_POINT('Ctrl Pts',(86.1347492572674,-2.90548701794336,-2.32761701889195));
#16842=CARTESIAN_POINT('Ctrl Pts',(86.1332617095365,-2.92295885611954,-2.30563818066895));
#16843=CARTESIAN_POINT('Ctrl Pts',(86.1290499348558,-2.97222482089685,-2.24220345840253));
#16844=CARTESIAN_POINT('Ctrl Pts',(86.1263636662157,-3.00339819035779,-2.20027192596006));
#16845=CARTESIAN_POINT('Ctrl Pts',(86.1108641311429,-3.18077738182521,-1.95088014821582));
#16846=CARTESIAN_POINT('Ctrl Pts',(86.0989638794391,-3.30635261652344,-1.72954705126819));
#16847=CARTESIAN_POINT('Ctrl Pts',(86.0809297235219,-3.45697624840952,-1.3866330424685));
#16848=CARTESIAN_POINT('Ctrl Pts',(86.0750632668744,-3.5001117929979,-1.27383329321157));
#16849=CARTESIAN_POINT('Ctrl Pts',(86.0646014739261,-3.56554401578721,-1.07413475770021));
#16850=CARTESIAN_POINT('Ctrl Pts',(86.0600743652014,-3.59032260376837,-0.988155706948785));
#16851=CARTESIAN_POINT('Ctrl Pts',(86.0528974291893,-3.62395109652917,-0.853399459939284));
#16852=CARTESIAN_POINT('Ctrl Pts',(86.050314465975,-3.63496525114363,-0.805195325660149));
#16853=CARTESIAN_POINT('Ctrl Pts',(86.0453711446694,-3.65398003992337,-0.713611886942932));
#16854=CARTESIAN_POINT('Ctrl Pts',(86.0430173192182,-3.66217617058866,-0.670281680117861));
#16855=CARTESIAN_POINT('Ctrl Pts',(86.0375558301385,-3.67922967059822,-0.570444723274658));
#16856=CARTESIAN_POINT('Ctrl Pts',(86.0344325619859,-3.68755820915327,-0.513860017721723));
#16857=CARTESIAN_POINT('Ctrl Pts',(86.023593687396,-3.71162884604093,-0.319308837833603));
#16858=CARTESIAN_POINT('Ctrl Pts',(86.0156928360809,-3.72095373050056,-0.180676435058985));
#16859=CARTESIAN_POINT('Ctrl Pts',(86.0067692681638,-3.722682803568,-0.0269054678282001));
#16860=CARTESIAN_POINT('Ctrl Pts',(86.0058999202337,-3.72276084300876,-0.0119524458300203));
#16861=CARTESIAN_POINT('Ctrl Pts',(85.9967740637689,-3.72263454584351,0.144742773224368));
#16862=CARTESIAN_POINT('Ctrl Pts',(85.9883845617901,-3.7144251989962,0.28635919450188));
#16863=CARTESIAN_POINT('Ctrl Pts',(85.9709413541588,-3.68050254699941,0.580048373103257));
#16864=CARTESIAN_POINT('Ctrl Pts',(85.9619087842773,-3.65337723218817,0.731707651111109));
#16865=CARTESIAN_POINT('Ctrl Pts',(85.9506415789239,-3.60612838185203,0.925630172085175));
#16866=CARTESIAN_POINT('Ctrl Pts',(85.9480952434709,-3.59450172037099,0.969799396397021));
#16867=CARTESIAN_POINT('Ctrl Pts',(85.9441204514966,-3.5747746464447,1.03950492607714));
#16868=CARTESIAN_POINT('Ctrl Pts',(85.9426655759653,-3.567206653127,1.06518592101018));
#16869=CARTESIAN_POINT('Ctrl Pts',(85.939785552781,-3.5515070010549,1.11641582106765));
#16870=CARTESIAN_POINT('Ctrl Pts',(85.9383605269914,-3.54337506691927,1.14196299637133));
#16871=CARTESIAN_POINT('Ctrl Pts',(85.9345367812972,-3.52058880253859,1.21096014234923));
#16872=CARTESIAN_POINT('Ctrl Pts',(85.932165692308,-3.50540619694783,1.25423192944197));
#16873=CARTESIAN_POINT('Ctrl Pts',(85.9218857338454,-3.4351509638238,1.44321427556931));
#16874=CARTESIAN_POINT('Ctrl Pts',(85.9143313362934,-3.37176042436534,1.5856760974596));
#16875=CARTESIAN_POINT('Ctrl Pts',(85.8934922586439,-3.17099912689698,1.96997476260508));
#16876=CARTESIAN_POINT('Ctrl Pts',(85.8803546562412,-3.01522915536588,2.20100433970703));
#16877=CARTESIAN_POINT('Ctrl Pts',(85.8629942517555,-2.79352059610721,2.46155427520549));
#16878=CARTESIAN_POINT('Ctrl Pts',(85.8596855616872,-2.75056527281446,2.50946146266941));
#16879=CARTESIAN_POINT('Ctrl Pts',(85.8542022108891,-2.67844635242311,2.58581689865048));
#16880=CARTESIAN_POINT('Ctrl Pts',(85.8520579517535,-2.6500186227414,2.61494263447641));
#16881=CARTESIAN_POINT('Ctrl Pts',(85.8498933978769,-2.62112000707361,2.64359555738363));
#16882=CARTESIAN_POINT('',(85.760341149807,-3.72274987726766,-0.000955930746860748));
#16883=CARTESIAN_POINT('Ctrl Pts',(85.6021262427416,-2.62112000930789,2.64359555516834));
#16884=CARTESIAN_POINT('Ctrl Pts',(85.6032237479712,-2.63714016151762,2.62771160445319));
#16885=CARTESIAN_POINT('Ctrl Pts',(85.6043175234224,-2.65301682263349,2.611681144791));
#16886=CARTESIAN_POINT('Ctrl Pts',(85.6204504607634,-2.88564119772402,2.37249240765257));
#16887=CARTESIAN_POINT('Ctrl Pts',(85.6350064317477,-3.07371361545918,2.12318795058449));
#16888=CARTESIAN_POINT('Ctrl Pts',(85.6540442114052,-3.26042230954893,1.79794384197059));
#16889=CARTESIAN_POINT('Ctrl Pts',(85.6573334774966,-3.2908193617108,1.74168395999376));
#16890=CARTESIAN_POINT('Ctrl Pts',(85.6629930620253,-3.3398653990825,1.64503563015123));
#16891=CARTESIAN_POINT('Ctrl Pts',(85.6653373612563,-3.35926718323422,1.6050441979263));
#16892=CARTESIAN_POINT('Ctrl Pts',(85.670214350167,-3.39773133500175,1.52200683470502));
#16893=CARTESIAN_POINT('Ctrl Pts',(85.67274954924,-3.41670246926471,1.47892764998727));
#16894=CARTESIAN_POINT('Ctrl Pts',(85.6794664790305,-3.46428138622222,1.3650813849668));
#16895=CARTESIAN_POINT('Ctrl Pts',(85.683690847758,-3.49153746178149,1.29377653654447));
#16896=CARTESIAN_POINT('Ctrl Pts',(85.696816072913,-3.56818137717465,1.07315993754611));
#16897=CARTESIAN_POINT('Ctrl Pts',(85.7059206556922,-3.61031497043406,0.921525182771377));
#16898=CARTESIAN_POINT('Ctrl Pts',(85.7220082984104,-3.6668019232921,0.653492386157504));
#16899=CARTESIAN_POINT('Ctrl Pts',(85.7289222746521,-3.68548553613412,0.538223500814585));
#16900=CARTESIAN_POINT('Ctrl Pts',(85.744125487982,-3.7147635344508,0.281772912376273));
#16901=CARTESIAN_POINT('Ctrl Pts',(85.7523850009167,-3.72278619233908,0.140468464394411));
#16902=CARTESIAN_POINT('Ctrl Pts',(85.760341149807,-3.72274987726766,-0.000955930746860748));
#16903=CARTESIAN_POINT('Ctrl Pts',(85.7603413601859,-3.72274987630553,-0.000959670334727729));
#16904=CARTESIAN_POINT('Ctrl Pts',(85.7620234535716,-3.72274216851247,-0.0308597147720175));
#16905=CARTESIAN_POINT('Ctrl Pts',(85.7636914883015,-3.72237423781889,-0.0607595695636158));
#16906=CARTESIAN_POINT('Ctrl Pts',(85.76688002092,-3.7209684279052,-0.118473539850565));
#16907=CARTESIAN_POINT('Ctrl Pts',(85.7684026300494,-3.71997880335005,-0.146286764873807));
#16908=CARTESIAN_POINT('Ctrl Pts',(85.7712404249104,-3.7175267093758,-0.198665983594152));
#16909=CARTESIAN_POINT('Ctrl Pts',(85.7725586100737,-3.71613249638555,-0.223231507567389));
#16910=CARTESIAN_POINT('Ctrl Pts',(85.7757422062399,-3.71213868356963,-0.283102350288278));
#16911=CARTESIAN_POINT('Ctrl Pts',(85.7775942166989,-3.70927894502006,-0.318387237437441));
#16912=CARTESIAN_POINT('Ctrl Pts',(85.7844257586302,-3.69672585713205,-0.449940163380343));
#16913=CARTESIAN_POINT('Ctrl Pts',(85.7892606494674,-3.68378367955504,-0.545864913335448));
#16914=CARTESIAN_POINT('Ctrl Pts',(85.7990812631252,-3.64931792670788,-0.742985128920719));
#16915=CARTESIAN_POINT('Ctrl Pts',(85.8040509119715,-3.62728600636354,-0.844005746828899));
#16916=CARTESIAN_POINT('Ctrl Pts',(85.8202961752315,-3.54137552192721,-1.17173517848588));
#16917=CARTESIAN_POINT('Ctrl Pts',(85.8315127254487,-3.46020168281947,-1.39330549026171));
#16918=CARTESIAN_POINT('Ctrl Pts',(85.8470625877511,-3.32698661590936,-1.67195036076543));
#16919=CARTESIAN_POINT('Ctrl Pts',(85.8508135674605,-3.29336800030353,-1.73723466447043));
#16920=CARTESIAN_POINT('Ctrl Pts',(85.857047842864,-3.23532216759319,-1.84220624266304));
#16921=CARTESIAN_POINT('Ctrl Pts',(85.8594918470563,-3.21204081089915,-1.88250549660204));
#16922=CARTESIAN_POINT('Ctrl Pts',(85.8643393894678,-3.16489124281644,-1.96069771704336));
#16923=CARTESIAN_POINT('Ctrl Pts',(85.8667405411498,-3.1410826432328,-1.99861744991541));
#16924=CARTESIAN_POINT('Ctrl Pts',(85.8727399514875,-3.08052086891813,-2.09131763751415));
#16925=CARTESIAN_POINT('Ctrl Pts',(85.8763659832838,-3.04298558571128,-2.14556665408895));
#16926=CARTESIAN_POINT('Ctrl Pts',(85.8948271741709,-2.84734745166465,-2.41285163066821));
#16927=CARTESIAN_POINT('Ctrl Pts',(85.9104440100743,-2.66825050866978,-2.60952949688887));
#16928=CARTESIAN_POINT('Ctrl Pts',(85.935734866639,-2.34770975351193,-2.89374428403784));
#16929=CARTESIAN_POINT('Ctrl Pts',(85.9453366356581,-2.21861468461013,-2.99386917826029));
#16930=CARTESIAN_POINT('Ctrl Pts',(85.9571958935502,-2.04467801529147,-3.11132412937402));
#16931=CARTESIAN_POINT('Ctrl Pts',(85.9598005404815,-2.00550769109523,-3.13671568879983));
#16932=CARTESIAN_POINT('Ctrl Pts',(85.9638440435153,-1.94296154583124,-3.17560948967413));
#16933=CARTESIAN_POINT('Ctrl Pts',(85.9653107824337,-1.9198996996016,-3.18960505884037));
#16934=CARTESIAN_POINT('Ctrl Pts',(85.9681927067859,-1.87378667581422,-3.21690835070137));
#16935=CARTESIAN_POINT('Ctrl Pts',(85.9696081575552,-1.85074096599047,-3.23022194134742));
#16936=CARTESIAN_POINT('Ctrl Pts',(85.9733729641343,-1.78845064798734,-3.26532179316026));
#16937=CARTESIAN_POINT('Ctrl Pts',(85.9756961504816,-1.74895045960043,-3.28664795176947));
#16938=CARTESIAN_POINT('Ctrl Pts',(85.9908566233137,-1.48508951218564,-3.4230019596901));
#16939=CARTESIAN_POINT('Ctrl Pts',(86.0027120691318,-1.2499058347712,-3.5157067042161));
#16940=CARTESIAN_POINT('Ctrl Pts',(86.0233928514973,-0.835575438296182,
-3.6321397446596));
#16941=CARTESIAN_POINT('Ctrl Pts',(86.0320534234354,-0.660783337843969,
-3.66796726675853));
#16942=CARTESIAN_POINT('Ctrl Pts',(86.0444481643793,-0.418097803460161,
-3.69979650167523));
#16943=CARTESIAN_POINT('Ctrl Pts',(86.0478660498463,-0.351869546893273,
-3.70668140932236));
#16944=CARTESIAN_POINT('Ctrl Pts',(86.0537007272735,-0.240302472715328,
-3.71526266943368));
#16945=CARTESIAN_POINT('Ctrl Pts',(86.0560883160667,-0.1950519291564,-3.71791292133806));
#16946=CARTESIAN_POINT('Ctrl Pts',(86.0606842997619,-0.10878972891976,-3.72138604485015));
#16947=CARTESIAN_POINT('Ctrl Pts',(86.0628877860286,-0.0677906345396503,
-3.72235860038369));
#16948=CARTESIAN_POINT('Ctrl Pts',(86.0687943725394,0.0411142919451229,
-3.72314218317815));
#16949=CARTESIAN_POINT('Ctrl Pts',(86.0725322973588,0.109010882290738,-3.7217729538625));
#16950=CARTESIAN_POINT('Ctrl Pts',(86.0859941946651,0.349868263769225,-3.71031938976274));
#16951=CARTESIAN_POINT('Ctrl Pts',(86.0960040874057,0.522104565570314,-3.69002354922952));
#16952=CARTESIAN_POINT('Ctrl Pts',(86.1169158849143,0.871997688471396,-3.62380193433515));
#16953=CARTESIAN_POINT('Ctrl Pts',(86.1278082882364,1.04895678266236,-3.57659203051134));
#16954=CARTESIAN_POINT('Ctrl Pts',(86.1421829947364,1.28261672762166,-3.49541365849707));
#16955=CARTESIAN_POINT('Ctrl Pts',(86.145892044404,1.34294717522115,-3.47268137084953));
#16956=CARTESIAN_POINT('Ctrl Pts',(86.1522966317303,1.44774544907876,-3.4300539012389));
#16957=CARTESIAN_POINT('Ctrl Pts',(86.1550172664346,1.49246975370475,-3.41083144091072));
#16958=CARTESIAN_POINT('Ctrl Pts',(86.1591970822581,1.56174016449165,-3.37943555025224));
#16959=CARTESIAN_POINT('Ctrl Pts',(86.1606871428466,1.58654952875076,-3.36785950782387));
#16960=CARTESIAN_POINT('Ctrl Pts',(86.163575463146,1.63492219692241,-3.34463565947165));
#16961=CARTESIAN_POINT('Ctrl Pts',(86.1649747153636,1.65849393953887,-3.33301007837422));
#16962=CARTESIAN_POINT('Ctrl Pts',(86.1686375129399,1.72048199199379,-3.30161712757996));
#16963=CARTESIAN_POINT('Ctrl Pts',(86.170877374298,1.75868186846619,-3.28142839792383));
#16964=CARTESIAN_POINT('Ctrl Pts',(86.1844793401716,1.99161226348869,-3.15308772075165));
#16965=CARTESIAN_POINT('Ctrl Pts',(86.1950623158639,2.1766796335749,-3.02829427964438));
#16966=CARTESIAN_POINT('Ctrl Pts',(86.2149102775699,2.49793099866395,-2.76691691646907));
#16967=CARTESIAN_POINT('Ctrl Pts',(86.2241218163708,2.63683101099577,-2.6348821878027));
#16968=CARTESIAN_POINT('Ctrl Pts',(86.2375616561667,2.81595671069249,-2.43619702705285));
#16969=CARTESIAN_POINT('Ctrl Pts',(86.2414458247611,2.86520441335654,-2.37808133623507));
#16970=CARTESIAN_POINT('Ctrl Pts',(86.2478413105384,2.94192893452935,-2.28169551067491));
#16971=CARTESIAN_POINT('Ctrl Pts',(86.2503090240149,2.97052353873976,-2.24434175306066));
#16972=CARTESIAN_POINT('Ctrl Pts',(86.2551622335661,3.02475509317736,-2.17064533606917));
#16973=CARTESIAN_POINT('Ctrl Pts',(86.2575444336255,3.0504637852163,-2.13436524874363));
#16974=CARTESIAN_POINT('Ctrl Pts',(86.2634170036499,3.11160101309343,-2.04472688812219));
#16975=CARTESIAN_POINT('Ctrl Pts',(86.266932517595,3.1463133572091,-1.99089941704815));
#16976=CARTESIAN_POINT('Ctrl Pts',(86.2860730502175,3.32523753254829,-1.69707180038417));
#16977=CARTESIAN_POINT('Ctrl Pts',(86.3025911836158,3.443396601791,-1.44230204935577));
#16978=CARTESIAN_POINT('Ctrl Pts',(86.3282244210372,3.58071922993454,-1.03014355809153));
#16979=CARTESIAN_POINT('Ctrl Pts',(86.3372947884107,3.62039237270546,-0.880631157919389));
#16980=CARTESIAN_POINT('Ctrl Pts',(86.3485998406114,3.65961157650132,-0.684251546319924));
#16981=CARTESIAN_POINT('Ctrl Pts',(86.3511486792379,3.66773784123743,-0.639262515341313));
#16982=CARTESIAN_POINT('Ctrl Pts',(86.3551264232466,3.67930772910303,-0.567696545590053));
#16983=CARTESIAN_POINT('Ctrl Pts',(86.3565818095862,3.68329644110635,-0.541213587991543));
#16984=CARTESIAN_POINT('Ctrl Pts',(86.3592843674836,3.69024773637019,-0.491417663395994));
#16985=CARTESIAN_POINT('Ctrl Pts',(86.3605351246982,3.69327601590024,-0.468115375054028));
#16986=CARTESIAN_POINT('Ctrl Pts',(86.3639931650483,3.70110737538778,-0.40303823657074));
#16987=CARTESIAN_POINT('Ctrl Pts',(86.3661758424477,3.70542375302013,-0.361207304695409));
#16988=CARTESIAN_POINT('Ctrl Pts',(86.3802643899425,3.72901730998095,-0.0871505492183481));
#16989=CARTESIAN_POINT('Ctrl Pts',(86.3913041578462,3.72716444645251,0.146396748049796));
#16990=CARTESIAN_POINT('Ctrl Pts',(86.4113663761407,3.68464715923591,0.562681725536755));
#16991=CARTESIAN_POINT('Ctrl Pts',(86.4203093137164,3.6520619638395,0.745434379651789));
#16992=CARTESIAN_POINT('Ctrl Pts',(86.4334050378777,3.58734939395829,0.997711559086204));
#16993=CARTESIAN_POINT('Ctrl Pts',(86.4372365227098,3.56650049101604,1.06984921147692));
#16994=CARTESIAN_POINT('Ctrl Pts',(86.4435681799452,3.52912561627286,1.18588953662559));
#16995=CARTESIAN_POINT('Ctrl Pts',(86.4460264742298,3.51392567600013,1.23019823383819));
#16996=CARTESIAN_POINT('Ctrl Pts',(86.450876953624,3.48263637006645,1.31609218449873));
#16997=CARTESIAN_POINT('Ctrl Pts',(86.4532661948277,3.46662792376517,1.35769854230954));
#16998=CARTESIAN_POINT('Ctrl Pts',(86.4591863604072,3.42553886425975,1.45902202667711));
#16999=CARTESIAN_POINT('Ctrl Pts',(86.4627434096578,3.39964022229376,1.51838975231757));
#17000=CARTESIAN_POINT('Ctrl Pts',(86.481639946389,3.25585836254753,1.8258387388197));
#17001=CARTESIAN_POINT('Ctrl Pts',(86.4978310497067,3.11234808391068,2.06095867065574));
#17002=CARTESIAN_POINT('Ctrl Pts',(86.5233365058518,2.84788282936661,2.40276217430003));
#17003=CARTESIAN_POINT('Ctrl Pts',(86.5325948236028,2.74362166504506,2.52116029461058));
#17004=CARTESIAN_POINT('Ctrl Pts',(86.5440963871367,2.59959336221692,2.66516477096101));
#17005=CARTESIAN_POINT('Ctrl Pts',(86.5466653289905,2.56641970265719,2.69712424419947));
#17006=CARTESIAN_POINT('Ctrl Pts',(86.5506667729415,2.51298107348377,2.74672798542203));
#17007=CARTESIAN_POINT('Ctrl Pts',(86.5521262577413,2.49310441463993,2.76478190218471));
#17008=CARTESIAN_POINT('Ctrl Pts',(86.554830556129,2.45550528287414,2.79819786430433));
#17009=CARTESIAN_POINT('Ctrl Pts',(86.5560790601752,2.43782975636516,2.81361042350881));
#17010=CARTESIAN_POINT('Ctrl Pts',(86.5595208583163,2.38826573539713,2.85601110524603));
#17011=CARTESIAN_POINT('Ctrl Pts',(86.5616899420457,2.35606601929198,2.88263175694308));
#17012=CARTESIAN_POINT('Ctrl Pts',(86.5758910133389,2.13950242357816,3.05561900446099));
#17013=CARTESIAN_POINT('Ctrl Pts',(86.5870359720157,1.9420426417751,3.18477167842611));
#17014=CARTESIAN_POINT('Ctrl Pts',(86.605137737773,1.60796292594034,3.36058149117198));
#17015=CARTESIAN_POINT('Ctrl Pts',(86.6119821133482,1.47855502271591,3.41949194176839));
#17016=CARTESIAN_POINT('Ctrl Pts',(86.6239254862094,1.2535966770716,3.50673741837284));
#17017=CARTESIAN_POINT('Ctrl Pts',(86.6289220125222,1.15969929668677,3.53889919546114));
#17018=CARTESIAN_POINT('Ctrl Pts',(86.6366686039045,1.01566139621753,3.5818865699422));
#17019=CARTESIAN_POINT('Ctrl Pts',(86.6393321115707,0.966394888843101,3.59549163024325));
#17020=CARTESIAN_POINT('Ctrl Pts',(86.6443405364,0.874362294776768,3.61887846000264));
#17021=CARTESIAN_POINT('Ctrl Pts',(86.6466766216492,0.831672942870827,3.62892692526664));
#17022=CARTESIAN_POINT('Ctrl Pts',(86.6520221336373,0.734590381361373,3.64997579623659));
#17023=CARTESIAN_POINT('Ctrl Pts',(86.6550451322229,0.680109597594471,3.66051865597117));
#17024=CARTESIAN_POINT('Ctrl Pts',(86.6647392334136,0.506811020099884,3.69005226359779));
#17025=CARTESIAN_POINT('Ctrl Pts',(86.6715426127137,0.387306129039432,3.70450171178061));
#17026=CARTESIAN_POINT('Ctrl Pts',(86.691204920197,0.0470238711182816,3.72899959982192));
#17027=CARTESIAN_POINT('Ctrl Pts',(86.7043586670008,-0.174238238734954,
3.72522208861027));
#17028=CARTESIAN_POINT('Ctrl Pts',(86.7249932877825,-0.52362397347469,3.68805096152193));
#17029=CARTESIAN_POINT('Ctrl Pts',(86.7325713348379,-0.652601836679468,
3.6674266045557));
#17030=CARTESIAN_POINT('Ctrl Pts',(86.7419781716467,-0.817009135104777,
3.63218637583907));
#17031=CARTESIAN_POINT('Ctrl Pts',(86.7440585210913,-0.85366008750314,3.62374757216707));
#17032=CARTESIAN_POINT('Ctrl Pts',(86.7474911170056,-0.914753134087983,
3.60870265019284));
#17033=CARTESIAN_POINT('Ctrl Pts',(86.7488587425677,-0.939266452442896,
3.60240014129813));
#17034=CARTESIAN_POINT('Ctrl Pts',(86.7517819567075,-0.992070882991982,
3.58824813995246));
#17035=CARTESIAN_POINT('Ctrl Pts',(86.7533330500894,-1.02033642176015,3.58031326083735));
#17036=CARTESIAN_POINT('Ctrl Pts',(86.7579579721765,-1.10522389961378,3.55539614999773));
#17037=CARTESIAN_POINT('Ctrl Pts',(86.7609812735936,-1.16154009995532,3.53739833012533));
#17038=CARTESIAN_POINT('Ctrl Pts',(86.7763149980169,-1.44946985022717,3.43776190115447));
#17039=CARTESIAN_POINT('Ctrl Pts',(86.7878380537975,-1.67303480865425,3.33468781785303));
#17040=CARTESIAN_POINT('Ctrl Pts',(86.8081604031828,-2.03683335923394,3.12109691305108));
#17041=CARTESIAN_POINT('Ctrl Pts',(86.8167775148827,-2.18229433312326,3.02117856833808));
#17042=CARTESIAN_POINT('Ctrl Pts',(86.8288131620099,-2.36695051414137,2.87402130040385));
#17043=CARTESIAN_POINT('Ctrl Pts',(86.8319043403277,-2.41287001940151,2.835579470552));
#17044=CARTESIAN_POINT('Ctrl Pts',(86.8373580951998,-2.49111325561623,2.76680046078543));
#17045=CARTESIAN_POINT('Ctrl Pts',(86.8397005235802,-2.52385988236031,2.73696202284962));
#17046=CARTESIAN_POINT('Ctrl Pts',(86.8436793063366,-2.57800553040469,2.68582682802946));
#17047=CARTESIAN_POINT('Ctrl Pts',(86.8453025273368,-2.59969198180257,2.66484140401889));
#17048=CARTESIAN_POINT('Ctrl Pts',(86.8469367975669,-2.62112000772923,2.64359555673358));
#17049=CARTESIAN_POINT('Origin',(80.1322559480305,0.,0.));
#17050=CARTESIAN_POINT('',(88.3477258555205,-2.62111983094262,2.64359573201716));
#17051=CARTESIAN_POINT('',(88.1029424526342,-2.62112000712061,2.64359555733703));
#17052=CARTESIAN_POINT('',(80.1322559480305,-2.62112000711956,2.64359555733806));
#17053=CARTESIAN_POINT('',(87.2551002656951,-3.72274852255099,-0.00283400709896036));
#17054=CARTESIAN_POINT('Ctrl Pts',(88.3477258555205,-2.62111983094262,2.64359573201716));
#17055=CARTESIAN_POINT('Ctrl Pts',(88.3386778175898,-2.51136572793979,2.75241670355373));
#17056=CARTESIAN_POINT('Ctrl Pts',(88.3294954746967,-2.39490245454868,2.85433544673622));
#17057=CARTESIAN_POINT('Ctrl Pts',(88.3127086086782,-2.16856793729687,3.028755955785));
#17058=CARTESIAN_POINT('Ctrl Pts',(88.3050930888711,-2.06057942350332,3.10323493620186));
#17059=CARTESIAN_POINT('Ctrl Pts',(88.2956136740075,-1.91632525836319,3.19186856815039));
#17060=CARTESIAN_POINT('Ctrl Pts',(88.2934985649453,-1.88346346357205,3.21136934331982));
#17061=CARTESIAN_POINT('Ctrl Pts',(88.2900265925673,-1.82826926324478,3.24298381229709));
#17062=CARTESIAN_POINT('Ctrl Pts',(88.2886535466726,-1.8061031379439,3.25538079131257));
#17063=CARTESIAN_POINT('Ctrl Pts',(88.2857395313557,-1.75829408664224,3.28148054746855));
#17064=CARTESIAN_POINT('Ctrl Pts',(88.2842026200638,-1.73261475687405,3.29511136209604));
#17065=CARTESIAN_POINT('Ctrl Pts',(88.2796716999771,-1.65563960978507,3.33482175159534));
#17066=CARTESIAN_POINT('Ctrl Pts',(88.2767252181063,-1.60389428165307,3.36001524042488));
#17067=CARTESIAN_POINT('Ctrl Pts',(88.2697028087483,-1.47722902258046,3.41809197960814));
#17068=CARTESIAN_POINT('Ctrl Pts',(88.2656759268388,-1.40176797156805,3.4497255103927));
#17069=CARTESIAN_POINT('Ctrl Pts',(88.2511212284633,-1.12213498214866,3.55625617283491));
#17070=CARTESIAN_POINT('Ctrl Pts',(88.2408891904004,-0.912555742871995,
3.61571432820128));
#17071=CARTESIAN_POINT('Ctrl Pts',(88.2238293571705,-0.568595911857687,
3.68146547383455));
#17072=CARTESIAN_POINT('Ctrl Pts',(88.2172465474274,-0.436979283891042,
3.69939649323452));
#17073=CARTESIAN_POINT('Ctrl Pts',(88.2075808615456,-0.248623401737625,
3.71486459231851));
#17074=CARTESIAN_POINT('Ctrl Pts',(88.2046686769021,-0.192458939123812,
3.71819736783688));
#17075=CARTESIAN_POINT('Ctrl Pts',(88.199410567924,-0.0922777503102582,
3.72186617905728));
#17076=CARTESIAN_POINT('Ctrl Pts',(88.1970800235928,-0.0482894160077024,
3.72269673117071));
#17077=CARTESIAN_POINT('Ctrl Pts',(88.1920512038369,0.045675523318885,3.72280521298625));
#17078=CARTESIAN_POINT('Ctrl Pts',(88.1893465157492,0.0956432750413966,
3.72185665290953));
#17079=CARTESIAN_POINT('Ctrl Pts',(88.1815489591566,0.238010934682628,3.71628521545284));
#17080=CARTESIAN_POINT('Ctrl Pts',(88.176384868378,0.330273709073209,3.70922394906707));
#17081=CARTESIAN_POINT('Ctrl Pts',(88.1639138913763,0.548452594274935,3.68432105785041));
#17082=CARTESIAN_POINT('Ctrl Pts',(88.1565342835466,0.673903304284392,3.66345089389269));
#17083=CARTESIAN_POINT('Ctrl Pts',(88.1340041738482,1.04870188561478,3.58119434181881));
#17084=CARTESIAN_POINT('Ctrl Pts',(88.1186174207522,1.29301327702992,3.50040750138304));
#17085=CARTESIAN_POINT('Ctrl Pts',(88.1016638876949,1.56732914839386,3.37702458832808));
#17086=CARTESIAN_POINT('Ctrl Pts',(88.0992061516287,1.6072594166623,3.35820386966895));
#17087=CARTESIAN_POINT('Ctrl Pts',(88.0953357535915,1.67058093034058,3.32696968179059));
#17088=CARTESIAN_POINT('Ctrl Pts',(88.0938988420199,1.69419011058612,3.31500948513039));
#17089=CARTESIAN_POINT('Ctrl Pts',(88.0910195852989,1.74175334161597,3.29027349926186));
#17090=CARTESIAN_POINT('Ctrl Pts',(88.0895780154058,1.76569904482905,3.27748552623805));
#17091=CARTESIAN_POINT('Ctrl Pts',(88.0856528786868,1.83117049553585,3.24159529216389));
#17092=CARTESIAN_POINT('Ctrl Pts',(88.0831995069761,1.87239824285088,3.21795752505246));
#17093=CARTESIAN_POINT('Ctrl Pts',(88.0776083441257,1.96664147456081,3.1614988693436));
#17094=CARTESIAN_POINT('Ctrl Pts',(88.0744965632663,2.01930816704048,3.12812227162595));
#17095=CARTESIAN_POINT('Ctrl Pts',(88.0630262870208,2.21271865012908,2.99863036463961));
#17096=CARTESIAN_POINT('Ctrl Pts',(88.0549291977798,2.34765205649643,2.89420841495331));
#17097=CARTESIAN_POINT('Ctrl Pts',(88.0377001601113,2.61589411043876,2.65547737525317));
#17098=CARTESIAN_POINT('Ctrl Pts',(88.028568807245,2.74708094977458,2.5195239403281));
#17099=CARTESIAN_POINT('Ctrl Pts',(88.0155702728691,2.91106095697644,2.32148233649355));
#17100=CARTESIAN_POINT('Ctrl Pts',(88.0120599387767,2.95326512942192,2.26754944294188));
#17101=CARTESIAN_POINT('Ctrl Pts',(88.0061150077484,3.02108938131016,2.17576901294856));
#17102=CARTESIAN_POINT('Ctrl Pts',(88.0037123161503,3.04754367464437,2.13855772859567));
#17103=CARTESIAN_POINT('Ctrl Pts',(87.9988320383362,3.09932029104117,2.06281512274474));
#17104=CARTESIAN_POINT('Ctrl Pts',(87.996354380982,3.12462444610435,2.02428118411595));
#17105=CARTESIAN_POINT('Ctrl Pts',(87.9899960297971,3.18705429220077,1.92525051834178));
#17106=CARTESIAN_POINT('Ctrl Pts',(87.9860808997728,3.22317623772767,1.86414555231813));
#17107=CARTESIAN_POINT('Ctrl Pts',(87.9772832650764,3.29926413536385,1.72660291012258));
#17108=CARTESIAN_POINT('Ctrl Pts',(87.9723760921402,3.33836426558408,1.64973453094291));
#17109=CARTESIAN_POINT('Ctrl Pts',(87.9549803074499,3.46570829470571,1.37628047658505));
#17110=CARTESIAN_POINT('Ctrl Pts',(87.942157336948,3.53952885300576,1.1734596664509));
#17111=CARTESIAN_POINT('Ctrl Pts',(87.9216902084876,3.62985705751071,0.837058930014744));
#17112=CARTESIAN_POINT('Ctrl Pts',(87.9139664269932,3.65742642669966,0.706942086733032));
#17113=CARTESIAN_POINT('Ctrl Pts',(87.9043972570307,3.68385937722709,0.538046536616738));
#17114=CARTESIAN_POINT('Ctrl Pts',(87.902292364192,3.68916405300237,0.500382653140881));
#17115=CARTESIAN_POINT('Ctrl Pts',(87.8988318747619,3.69704389965128,0.437467375902617));
#17116=CARTESIAN_POINT('Ctrl Pts',(87.8974603358787,3.69993965255739,0.412259630929676));
#17117=CARTESIAN_POINT('Ctrl Pts',(87.894543387535,3.70560890170458,0.358022895718634));
#17118=CARTESIAN_POINT('Ctrl Pts',(87.8930021655089,3.70829945672817,0.328987799342598));
#17119=CARTESIAN_POINT('Ctrl Pts',(87.8884430686021,3.71532233034682,0.242100830870248));
#17120=CARTESIAN_POINT('Ctrl Pts',(87.8854736056124,3.7186440205103,0.184174220970671));
#17121=CARTESIAN_POINT('Ctrl Pts',(87.8783813440398,3.7234163658059,0.04346646875734));
#17122=CARTESIAN_POINT('Ctrl Pts',(87.8743089036718,3.72346249377927,-0.0393323360391734));
#17123=CARTESIAN_POINT('Ctrl Pts',(87.8594338464656,3.71342955085848,-0.345148125767257));
#17124=CARTESIAN_POINT('Ctrl Pts',(87.8489373271024,3.68606373355316,-0.567118576897356));
#17125=CARTESIAN_POINT('Ctrl Pts',(87.8318671626106,3.61230146911092,-0.908921748915311));
#17126=CARTESIAN_POINT('Ctrl Pts',(87.8255830158037,3.57934451740969,-1.0310916031993));
#17127=CARTESIAN_POINT('Ctrl Pts',(87.8162560037859,3.52297290911332,-1.20442749242116));
#17128=CARTESIAN_POINT('Ctrl Pts',(87.8133650614059,3.50451740311575,-1.25711616704649));
#17129=CARTESIAN_POINT('Ctrl Pts',(87.8081300932156,3.46942550441721,-1.35051328465182));
#17130=CARTESIAN_POINT('Ctrl Pts',(87.8058008998807,3.45323918607512,-1.3913800231793));
#17131=CARTESIAN_POINT('Ctrl Pts',(87.8007578667453,3.41700555888998,-1.47833199256914));
#17132=CARTESIAN_POINT('Ctrl Pts',(87.7980372373347,3.39674115727954,-1.52431678084574));
#17133=CARTESIAN_POINT('Ctrl Pts',(87.7901339249019,3.3358707390591,-1.65520057680586));
#17134=CARTESIAN_POINT('Ctrl Pts',(87.7848768879323,3.29297034447667,-1.73898440702014));
#17135=CARTESIAN_POINT('Ctrl Pts',(87.7721085617985,3.18309057773597,-1.93490093686167));
#17136=CARTESIAN_POINT('Ctrl Pts',(87.7645194008865,3.11329660446284,-2.04530865349794));
#17137=CARTESIAN_POINT('Ctrl Pts',(87.742275316538,2.89451261941406,-2.35417958411365));
#17138=CARTESIAN_POINT('Ctrl Pts',(87.727427835427,2.73130802937129,-2.54171772147356));
#17139=CARTESIAN_POINT('Ctrl Pts',(87.710858425892,2.51748346668256,-2.74284882152555));
#17140=CARTESIAN_POINT('Ctrl Pts',(87.7083187301591,2.48373106724228,-2.7734496590092));
#17141=CARTESIAN_POINT('Ctrl Pts',(87.7043517833256,2.42928162071707,-2.82102353998803));
#17142=CARTESIAN_POINT('Ctrl Pts',(87.7028982765776,2.40894942727238,-2.83840549476555));
#17143=CARTESIAN_POINT('Ctrl Pts',(87.7000184430961,2.36784956789811,-2.87278191386471));
#17144=CARTESIAN_POINT('Ctrl Pts',(87.6985922848782,2.34708198230921,-2.88977399725392));
#17145=CARTESIAN_POINT('Ctrl Pts',(87.6947615729383,2.2902434042844,-2.93526244844375));
#17146=CARTESIAN_POINT('Ctrl Pts',(87.6923848240721,2.25382450216796,-2.96331840399038));
#17147=CARTESIAN_POINT('Ctrl Pts',(87.682048678778,2.09094646545296,-3.08405403837996));
#17148=CARTESIAN_POINT('Ctrl Pts',(87.6744482297694,1.95921706191711,-3.16937257260822));
#17149=CARTESIAN_POINT('Ctrl Pts',(87.6536483815622,1.581797621996,-3.38126875073741));
#17150=CARTESIAN_POINT('Ctrl Pts',(87.6405887357926,1.32684080338732,-3.48920426914433));
#17151=CARTESIAN_POINT('Ctrl Pts',(87.6233094273196,1.00041065447841,-3.5863931607547));
#17152=CARTESIAN_POINT('Ctrl Pts',(87.6199891560409,0.938054963181408,-3.60320546775309));
#17153=CARTESIAN_POINT('Ctrl Pts',(87.6142932199103,0.831997314829299,-3.62886104627075));
#17154=CARTESIAN_POINT('Ctrl Pts',(87.6119444459019,0.788515631628333,-3.63855670555856));
#17155=CARTESIAN_POINT('Ctrl Pts',(87.607073142924,0.69892880567694,-3.65685176832089));
#17156=CARTESIAN_POINT('Ctrl Pts',(87.6045484166771,0.652814335803341,-3.66536485286278));
#17157=CARTESIAN_POINT('Ctrl Pts',(87.597896535097,0.532206848534663,-3.6852817362447));
#17158=CARTESIAN_POINT('Ctrl Pts',(87.5937282719487,0.457509300951298,-3.69529833019803));
#17159=CARTESIAN_POINT('Ctrl Pts',(87.5842276491347,0.289230056115743,-3.71268332713183));
#17160=CARTESIAN_POINT('Ctrl Pts',(87.5788635215976,0.195571555858999,-3.71879301261899));
#17161=CARTESIAN_POINT('Ctrl Pts',(87.557741181702,-0.168912399694604,-3.72876240828649));
#17162=CARTESIAN_POINT('Ctrl Pts',(87.5414564413288,-0.439592765959358,
-3.70660867077501));
#17163=CARTESIAN_POINT('Ctrl Pts',(87.5216158054898,-0.777480969252871,
-3.6413967255353));
#17164=CARTESIAN_POINT('Ctrl Pts',(87.5174458439575,-0.849073018769935,
-3.62537212307217));
#17165=CARTESIAN_POINT('Ctrl Pts',(87.5115620788491,-0.951670457834807,
-3.59920118576324));
#17166=CARTESIAN_POINT('Ctrl Pts',(87.5097731145124,-0.983086560379654,
-3.59074738684396));
#17167=CARTESIAN_POINT('Ctrl Pts',(87.5066537677753,-1.03834604736253,-3.57509790453704));
#17168=CARTESIAN_POINT('Ctrl Pts',(87.5053147691838,-1.06223405641105,-3.56807320961385));
#17169=CARTESIAN_POINT('Ctrl Pts',(87.5022648064355,-1.11703208582513,-3.55135973168301));
#17170=CARTESIAN_POINT('Ctrl Pts',(87.5005627019815,-1.14788877774059,-3.54150647594772));
#17171=CARTESIAN_POINT('Ctrl Pts',(87.4948237603667,-1.25265933217468,-3.50653755900257));
#17172=CARTESIAN_POINT('Ctrl Pts',(87.4908800666779,-1.32591359060185,-3.47949933928717));
#17173=CARTESIAN_POINT('Ctrl Pts',(87.480464866776,-1.52042650957529,-3.4006682641765));
#17174=CARTESIAN_POINT('Ctrl Pts',(87.4741274708399,-1.63987558698074,-3.34470515313688));
#17175=CARTESIAN_POINT('Ctrl Pts',(87.4561239794847,-1.97099806715439,-3.16755869329075));
#17176=CARTESIAN_POINT('Ctrl Pts',(87.4445062287557,-2.17406275107045,-3.03178217094962));
#17177=CARTESIAN_POINT('Ctrl Pts',(87.4287368014681,-2.41507099362414,-2.83389210615855));
#17178=CARTESIAN_POINT('Ctrl Pts',(87.4252420769192,-2.46654333218421,-2.78920699130686));
#17179=CARTESIAN_POINT('Ctrl Pts',(87.4195528302774,-2.54700536977767,-2.71538509276096));
#17180=CARTESIAN_POINT('Ctrl Pts',(87.4173943726057,-2.5767904971737,-2.6871366014865));
#17181=CARTESIAN_POINT('Ctrl Pts',(87.4128111605039,-2.63843961168021,-2.62670034812941));
#17182=CARTESIAN_POINT('Ctrl Pts',(87.4103823029705,-2.67019538195899,-2.59441220387761));
#17183=CARTESIAN_POINT('Ctrl Pts',(87.4043335722367,-2.7469975207394,-2.5134185033366));
#17184=CARTESIAN_POINT('Ctrl Pts',(87.4006859037732,-2.79134481003505,-2.4640741360887));
#17185=CARTESIAN_POINT('Ctrl Pts',(87.3871474939668,-2.94877758204568,-2.27919501561617));
#17186=CARTESIAN_POINT('Ctrl Pts',(87.3769533275565,-3.0534937830724,-2.13686296876134));
#17187=CARTESIAN_POINT('Ctrl Pts',(87.3515944429072,-3.28406238274875,-1.77172740916098));
#17188=CARTESIAN_POINT('Ctrl Pts',(87.3362863661774,-3.39783466331522,-1.54233940597438));
#17189=CARTESIAN_POINT('Ctrl Pts',(87.3193882640276,-3.50275494364628,-1.26156341839448));
#17190=CARTESIAN_POINT('Ctrl Pts',(87.3169182809703,-3.51753611034684,-1.21974362212606));
#17191=CARTESIAN_POINT('Ctrl Pts',(87.3130334363718,-3.5399522561828,-1.15252253360953));
#17192=CARTESIAN_POINT('Ctrl Pts',(87.3115940290524,-3.54806898962337,-1.12728732701567));
#17193=CARTESIAN_POINT('Ctrl Pts',(87.3087148198242,-3.56393618913984,-1.07608575332492));
#17194=CARTESIAN_POINT('Ctrl Pts',(87.3072756988858,-3.57167403712233,-1.05011731227512));
#17195=CARTESIAN_POINT('Ctrl Pts',(87.303365493146,-3.59213163717905,-0.978617651118007));
#17196=CARTESIAN_POINT('Ctrl Pts',(87.3009242219604,-3.60426909844324,-0.932923821940991));
#17197=CARTESIAN_POINT('Ctrl Pts',(87.2953666510638,-3.63028112174045,-0.826896364906126));
#17198=CARTESIAN_POINT('Ctrl Pts',(87.2922759131574,-3.64352793565999,-0.766422482730354));
#17199=CARTESIAN_POINT('Ctrl Pts',(87.2775961180349,-3.69997106573645,-0.474045101324363));
#17200=CARTESIAN_POINT('Ctrl Pts',(87.2665385515448,-3.72256915154514,-0.238720185061259));
#17201=CARTESIAN_POINT('Ctrl Pts',(87.2551011079057,-3.72274891890995,-0.00283712086446175));
#17202=CARTESIAN_POINT('Ctrl Pts',(87.2551009553192,-3.72274892130689,-0.00283397395788376));
#17203=CARTESIAN_POINT('Ctrl Pts',(87.2481690907567,-3.72285775161648,0.140127084840354));
#17204=CARTESIAN_POINT('Ctrl Pts',(87.2411206974449,-3.71473158564361,0.282969156473876));
#17205=CARTESIAN_POINT('Ctrl Pts',(87.2314476587175,-3.69306159874725,0.471551346865502));
#17206=CARTESIAN_POINT('Ctrl Pts',(87.2290352459888,-3.68683178562366,0.518011379072727));
#17207=CARTESIAN_POINT('Ctrl Pts',(87.2241973229379,-3.67273551875958,0.609924749068469));
#17208=CARTESIAN_POINT('Ctrl Pts',(87.2217730790791,-3.66489822330142,0.655374058299254));
#17209=CARTESIAN_POINT('Ctrl Pts',(87.2168980386484,-3.64763040186785,0.745481248027248));
#17210=CARTESIAN_POINT('Ctrl Pts',(87.2144482110008,-3.63821892122694,0.790134591914953));
#17211=CARTESIAN_POINT('Ctrl Pts',(87.2082648874663,-3.61266472449791,0.901217850442107));
#17212=CARTESIAN_POINT('Ctrl Pts',(87.2045007518601,-3.5955090541113,0.967395391167315));
#17213=CARTESIAN_POINT('Ctrl Pts',(87.18242114745,-3.48580302326893,1.34720690893251));
#17214=CARTESIAN_POINT('Ctrl Pts',(87.1628606429618,-3.35407526029626,1.64800092110445));
#17215=CARTESIAN_POINT('Ctrl Pts',(87.1390495266081,-3.14347056822796,1.99595423378076));
#17216=CARTESIAN_POINT('Ctrl Pts',(87.1344169459925,-3.09994577583506,2.06290519015491));
#17217=CARTESIAN_POINT('Ctrl Pts',(87.1266436286505,-3.021947026892,2.1748346923464));
#17218=CARTESIAN_POINT('Ctrl Pts',(87.1234623852895,-2.98853786527519,2.2205206253762));
#17219=CARTESIAN_POINT('Ctrl Pts',(87.1187467974954,-2.93651370615651,2.28835964007137));
#17220=CARTESIAN_POINT('Ctrl Pts',(87.1171685721622,-2.91866197932996,2.31108523107678));
#17221=CARTESIAN_POINT('Ctrl Pts',(87.1142492723602,-2.8847677687392,2.35321399776764));
#17222=CARTESIAN_POINT('Ctrl Pts',(87.1129043839747,-2.86879029564076,2.3726658958337));
#17223=CARTESIAN_POINT('Ctrl Pts',(87.1095430509435,-2.8279713376069,2.4213460950567));
#17224=CARTESIAN_POINT('Ctrl Pts',(87.1075437435319,-2.80287255399562,2.45035598743111));
#17225=CARTESIAN_POINT('Ctrl Pts',(87.1016745714368,-2.7269375600657,2.53543008319701));
#17226=CARTESIAN_POINT('Ctrl Pts',(87.0978789969963,-2.67484318990745,2.59032912354232));
#17227=CARTESIAN_POINT('Ctrl Pts',(87.0941439883772,-2.62111999291044,2.64359557142638));
#17228=CARTESIAN_POINT('Ctrl Pts',(86.8469367975669,-2.62112000772923,2.64359555673358));
#17229=CARTESIAN_POINT('Ctrl Pts',(86.8479364796116,-2.63422751735572,2.6305994856644));
#17230=CARTESIAN_POINT('Ctrl Pts',(86.8489402927088,-2.64723833041324,2.61750597024224));
#17231=CARTESIAN_POINT('Ctrl Pts',(86.8545857674141,-2.71956531200265,2.54362833282821));
#17232=CARTESIAN_POINT('Ctrl Pts',(86.8593090595828,-2.77688156213494,2.48092882258983));
#17233=CARTESIAN_POINT('Ctrl Pts',(86.8810117078852,-3.02607124839538,2.18887180157179));
#17234=CARTESIAN_POINT('Ctrl Pts',(86.898909857695,-3.19201871212538,1.93887702829356));
#17235=CARTESIAN_POINT('Ctrl Pts',(86.9209505092802,-3.36122010782939,1.60222574810387));
#17236=CARTESIAN_POINT('Ctrl Pts',(86.925463694497,-3.39399089429002,1.5315857253983));
#17237=CARTESIAN_POINT('Ctrl Pts',(86.9330629058012,-3.44633387571132,1.40880914677604));
#17238=CARTESIAN_POINT('Ctrl Pts',(86.9361872946315,-3.4669959917596,1.35716609388758));
#17239=CARTESIAN_POINT('Ctrl Pts',(86.9408372646071,-3.49656103651619,1.27818350914106));
#17240=CARTESIAN_POINT('Ctrl Pts',(86.9424050266554,-3.50631672641429,1.25117356252425));
#17241=CARTESIAN_POINT('Ctrl Pts',(86.9453171800885,-3.52405761641445,1.20021766626114));
#17242=CARTESIAN_POINT('Ctrl Pts',(86.9466651110412,-3.5321133678115,1.17629915499785));
#17243=CARTESIAN_POINT('Ctrl Pts',(86.9500513466499,-3.5519303731355,1.11542029135123));
#17244=CARTESIAN_POINT('Ctrl Pts',(86.9520719292542,-3.56335870890518,1.07835371793144));
#17245=CARTESIAN_POINT('Ctrl Pts',(86.96161878224,-3.61526387232496,0.900160204006547));
#17246=CARTESIAN_POINT('Ctrl Pts',(86.968800275248,-3.64795117390932,0.756888770379204));
#17247=CARTESIAN_POINT('Ctrl Pts',(86.9857386298002,-3.70566792992219,0.410608304780262));
#17248=CARTESIAN_POINT('Ctrl Pts',(86.9953903594235,-3.72261047931251,0.20674836417901));
#17249=CARTESIAN_POINT('Ctrl Pts',(87.0111802735306,-3.72282939123067,-0.11566265239382));
#17250=CARTESIAN_POINT('Ctrl Pts',(87.0170716576226,-3.71728119422797,-0.233781980183838));
#17251=CARTESIAN_POINT('Ctrl Pts',(87.0259674608812,-3.70088901968681,-0.406650390857667));
#17252=CARTESIAN_POINT('Ctrl Pts',(87.0288432021793,-3.69441970680641,-0.461743105891317));
#17253=CARTESIAN_POINT('Ctrl Pts',(87.034059677121,-3.68063605131306,-0.560097198287279));
#17254=CARTESIAN_POINT('Ctrl Pts',(87.0363859344194,-3.67378319037585,-0.603413181308806));
#17255=CARTESIAN_POINT('Ctrl Pts',(87.041475400076,-3.65728775048501,-0.696941379411489));
#17256=CARTESIAN_POINT('Ctrl Pts',(87.0442465761122,-3.64737280347217,-0.74709588359248));
#17257=CARTESIAN_POINT('Ctrl Pts',(87.052493830743,-3.61516685725108,-0.894034908728921));
#17258=CARTESIAN_POINT('Ctrl Pts',(87.0580549112132,-3.59003352505528,-0.990144780847397));
#17259=CARTESIAN_POINT('Ctrl Pts',(87.0718264483764,-3.51961544840658,-1.2212371022127));
#17260=CARTESIAN_POINT('Ctrl Pts',(87.0801337058674,-3.47037460852577,-1.35484618256512));
#17261=CARTESIAN_POINT('Ctrl Pts',(87.1023570125416,-3.31986942264083,-1.70074657191134));
#17262=CARTESIAN_POINT('Ctrl Pts',(87.1163753574549,-3.20593745829391,-1.90684223360547));
#17263=CARTESIAN_POINT('Ctrl Pts',(87.1319390803758,-3.04972998165191,-2.13536042330805));
#17264=CARTESIAN_POINT('Ctrl Pts',(87.1342631556041,-3.0255445483069,-2.1694924689364));
#17265=CARTESIAN_POINT('Ctrl Pts',(87.1378367368629,-2.9869042542877,-2.22212080645775));
#17266=CARTESIAN_POINT('Ctrl Pts',(87.1391098227967,-2.97284164384179,-2.24089949017644));
#17267=CARTESIAN_POINT('Ctrl Pts',(87.1418131221603,-2.94231347999386,-2.28087245316507));
#17268=CARTESIAN_POINT('Ctrl Pts',(87.1432395204213,-2.92579425549943,-2.30202428804485));
#17269=CARTESIAN_POINT('Ctrl Pts',(87.1470716623311,-2.88034952011591,-2.35893392876347));
#17270=CARTESIAN_POINT('Ctrl Pts',(87.1494495660655,-2.85098707137756,-2.39433826255021));
#17271=CARTESIAN_POINT('Ctrl Pts',(87.1597971322618,-2.71853978565936,-2.5481468719549));
#17272=CARTESIAN_POINT('Ctrl Pts',(87.1674069396115,-2.60867457506647,-2.66051416042603));
#17273=CARTESIAN_POINT('Ctrl Pts',(87.1881988675785,-2.2872360604958,-2.95015530535578));
#17274=CARTESIAN_POINT('Ctrl Pts',(87.2012426963686,-2.06259001495656,-3.1113627893878));
#17275=CARTESIAN_POINT('Ctrl Pts',(87.2185055481398,-1.76585917063264,-3.2779238780769));
#17276=CARTESIAN_POINT('Ctrl Pts',(87.2218281542193,-1.70869613796958,-3.30808108175837));
#17277=CARTESIAN_POINT('Ctrl Pts',(87.2275268431535,-1.61084408063918,-3.35649133298813));
#17278=CARTESIAN_POINT('Ctrl Pts',(87.2298759696225,-1.57055866677803,-3.3755292874633));
#17279=CARTESIAN_POINT('Ctrl Pts',(87.2347469053028,-1.48720569969636,-3.41310479744019));
#17280=CARTESIAN_POINT('Ctrl Pts',(87.2372708889242,-1.44411034448974,-3.43156089781793));
#17281=CARTESIAN_POINT('Ctrl Pts',(87.2439181074332,-1.33092802690625,-3.47752292530341));
#17282=CARTESIAN_POINT('Ctrl Pts',(87.2480823406078,-1.26033736765293,-3.50372426654168));
#17283=CARTESIAN_POINT('Ctrl Pts',(87.2575716186588,-1.10020638506853,-3.55769507396356));
#17284=CARTESIAN_POINT('Ctrl Pts',(87.2629283091363,-1.01031528612291,-3.58425857731229));
#17285=CARTESIAN_POINT('Ctrl Pts',(87.283977320029,-0.658195193161684,-3.67401356369224));
#17286=CARTESIAN_POINT('Ctrl Pts',(87.3001917683876,-0.390421990427456,
-3.7120286053518));
#17287=CARTESIAN_POINT('Ctrl Pts',(87.3200343578389,-0.0466224385883072,
-3.72319984360815));
#17288=CARTESIAN_POINT('Ctrl Pts',(87.3242618314156,0.0277165204521502,
-3.72338875439068));
#17289=CARTESIAN_POINT('Ctrl Pts',(87.3302099504557,0.134690041883209,-3.72045623482529));
#17290=CARTESIAN_POINT('Ctrl Pts',(87.3320078983521,0.167352699612359,-3.719130170331));
#17291=CARTESIAN_POINT('Ctrl Pts',(87.3351364793589,0.224861542560495,-3.71603619417132));
#17292=CARTESIAN_POINT('Ctrl Pts',(87.3364759358832,0.249713815552624,-3.71444892299767));
#17293=CARTESIAN_POINT('Ctrl Pts',(87.339518691028,0.306702147011486,-3.71023459424388));
#17294=CARTESIAN_POINT('Ctrl Pts',(87.3412133363148,0.338822743015615,-3.70743931023352));
#17295=CARTESIAN_POINT('Ctrl Pts',(87.3468914138761,0.44753004302278,-3.69655445479987));
#17296=CARTESIAN_POINT('Ctrl Pts',(87.3507843729499,0.523904181608227,-3.68650563295299));
#17297=CARTESIAN_POINT('Ctrl Pts',(87.3610051965339,0.727037625838374,-3.65333746757463));
#17298=CARTESIAN_POINT('Ctrl Pts',(87.3672049614466,0.853002435697202,-3.6259961623754));
#17299=CARTESIAN_POINT('Ctrl Pts',(87.3853294290354,1.21768742178242,-3.52677865571833));
#17300=CARTESIAN_POINT('Ctrl Pts',(87.3971897218197,1.45088336110006,-3.4374202971593));
#17301=CARTESIAN_POINT('Ctrl Pts',(87.4132164432478,1.73387672085105,-3.29501475000028));
#17302=CARTESIAN_POINT('Ctrl Pts',(87.4166890444941,1.79350651972013,-3.26294105661915));
#17303=CARTESIAN_POINT('Ctrl Pts',(87.422352220358,1.88777192734261,-3.20887267674082));
#17304=CARTESIAN_POINT('Ctrl Pts',(87.4245073942538,1.92297727551404,-3.1878997678052));
#17305=CARTESIAN_POINT('Ctrl Pts',(87.4290916599385,1.99640811883289,-3.14249576476093));
#17306=CARTESIAN_POINT('Ctrl Pts',(87.4315250083056,2.03454744586019,-3.11793865493081));
#17307=CARTESIAN_POINT('Ctrl Pts',(87.437602829122,2.12769925292349,-3.05552320442431));
#17308=CARTESIAN_POINT('Ctrl Pts',(87.4412757065344,2.18215837471395,-3.01687093218046));
#17309=CARTESIAN_POINT('Ctrl Pts',(87.4550181335572,2.37917856232542,-2.86890962359895));
#17310=CARTESIAN_POINT('Ctrl Pts',(87.4654029242124,2.51480052860258,-2.75079975746461));
#17311=CARTESIAN_POINT('Ctrl Pts',(87.4906169203798,2.8171903884149,-2.44633723384258));
#17312=CARTESIAN_POINT('Ctrl Pts',(87.5055598564812,2.97478281745828,-2.25206625253012));
#17313=CARTESIAN_POINT('Ctrl Pts',(87.5221979204017,3.13662762464533,-2.0056140061411));
#17314=CARTESIAN_POINT('Ctrl Pts',(87.524723416456,3.16080578772355,-1.96728938569164));
#17315=CARTESIAN_POINT('Ctrl Pts',(87.5286736405184,3.19811019125227,-1.90569451409617));
#17316=CARTESIAN_POINT('Ctrl Pts',(87.5301242732166,3.21169549468296,-1.88270882490503));
#17317=CARTESIAN_POINT('Ctrl Pts',(87.5330038715898,3.23846143424558,-1.83628914170717));
#17318=CARTESIAN_POINT('Ctrl Pts',(87.5344325671078,3.25163783794852,-1.81285458058579));
#17319=CARTESIAN_POINT('Ctrl Pts',(87.5382787954765,3.28677510326585,-1.74874623300434));
#17320=CARTESIAN_POINT('Ctrl Pts',(87.540668136028,3.3082347498521,-1.7078018532505));
#17321=CARTESIAN_POINT('Ctrl Pts',(87.5511302798696,3.40012586061098,-1.52424054512313));
#17322=CARTESIAN_POINT('Ctrl Pts',(87.5588340105021,3.46214236139758,-1.3775860026505));
#17323=CARTESIAN_POINT('Ctrl Pts',(87.5795487335213,3.6043153584574,-0.970483077624764));
#17324=CARTESIAN_POINT('Ctrl Pts',(87.5924355060725,3.66559280489559,-0.704518797517292));
#17325=CARTESIAN_POINT('Ctrl Pts',(87.6095350419798,3.70492816148626,-0.369610038076758));
#17326=CARTESIAN_POINT('Ctrl Pts',(87.6128804713385,3.7108238037798,-0.304779135170445));
#17327=CARTESIAN_POINT('Ctrl Pts',(87.6186060037733,3.71789194415081,-0.195291847803361));
#17328=CARTESIAN_POINT('Ctrl Pts',(87.6209585039582,3.71996591358417,-0.1507076332699));
#17329=CARTESIAN_POINT('Ctrl Pts',(87.6258257272487,3.7225703017399,-0.0593624922091599));
#17330=CARTESIAN_POINT('Ctrl Pts',(87.6283424018644,3.72302220549708,-0.0126074339512018));
#17331=CARTESIAN_POINT('Ctrl Pts',(87.6349442261392,3.72190919782321,0.108745468813719));
#17332=CARTESIAN_POINT('Ctrl Pts',(87.6390693189485,3.71898252928336,0.183307218808084));
#17333=CARTESIAN_POINT('Ctrl Pts',(87.6549751713529,3.69936344359356,0.466015731787855));
#17334=CARTESIAN_POINT('Ctrl Pts',(87.6671787102698,3.6674134402773,0.672697643241746));
#17335=CARTESIAN_POINT('Ctrl Pts',(87.6916779648745,3.56978379992552,1.07614544228474));
#17336=CARTESIAN_POINT('Ctrl Pts',(87.7039236488903,3.50465867448407,1.27232955497797));
#17337=CARTESIAN_POINT('Ctrl Pts',(87.7180507508391,3.40623009844991,1.50280464348935));
#17338=CARTESIAN_POINT('Ctrl Pts',(87.7205147400571,3.38812758013524,1.54318408365587));
#17339=CARTESIAN_POINT('Ctrl Pts',(87.7243925271119,3.35804459129501,1.60720427936572));
#17340=CARTESIAN_POINT('Ctrl Pts',(87.7258307251976,3.3465245237232,1.63105572939414));
#17341=CARTESIAN_POINT('Ctrl Pts',(87.7287099614352,3.32269575581642,1.67907591623779));
#17342=CARTESIAN_POINT('Ctrl Pts',(87.7301502727207,3.31037562820098,1.70323700841885));
#17343=CARTESIAN_POINT('Ctrl Pts',(87.7340677689931,3.27580365047861,1.76924390068868));
#17344=CARTESIAN_POINT('Ctrl Pts',(87.7365149537306,3.25301447287883,1.81080389995596));
#17345=CARTESIAN_POINT('Ctrl Pts',(87.7420889398034,3.19853845215192,1.9058009603829));
#17346=CARTESIAN_POINT('Ctrl Pts',(87.74518996026,3.16629500438848,1.95890329002019));
#17347=CARTESIAN_POINT('Ctrl Pts',(87.7565881115289,3.04136459826023,2.15350290523736));
#17348=CARTESIAN_POINT('Ctrl Pts',(87.7646270543949,2.9403959173098,2.28944312515968));
#17349=CARTESIAN_POINT('Ctrl Pts',(87.7818704548197,2.70692523298511,2.56274003902158));
#17350=CARTESIAN_POINT('Ctrl Pts',(87.7910765237114,2.57241523266802,2.69773109042674));
#17351=CARTESIAN_POINT('Ctrl Pts',(87.8041592762334,2.37624893711966,2.86653155596696));
#17352=CARTESIAN_POINT('Ctrl Pts',(87.8076717498739,2.32309130700325,2.90977803577831));
#17353=CARTESIAN_POINT('Ctrl Pts',(87.8136191764263,2.23257130861604,2.97935862146883));
#17354=CARTESIAN_POINT('Ctrl Pts',(87.8160221582096,2.19586222813033,3.00651646896838));
#17355=CARTESIAN_POINT('Ctrl Pts',(87.8209021046976,2.12111676162474,3.05971488463199));
#17356=CARTESIAN_POINT('Ctrl Pts',(87.8233791210617,2.08307778739298,3.08573786443446));
#17357=CARTESIAN_POINT('Ctrl Pts',(87.8297337741589,1.98530165133014,3.1499959130774));
#17358=CARTESIAN_POINT('Ctrl Pts',(87.8336457693517,1.9249388043878,3.18724121779741));
#17359=CARTESIAN_POINT('Ctrl Pts',(87.842434838972,1.78899196916851,3.26585261383944));
#17360=CARTESIAN_POINT('Ctrl Pts',(87.8473365025625,1.71296246437522,3.30636412224572));
#17361=CARTESIAN_POINT('Ctrl Pts',(87.8646942012464,1.44256292290409,3.43861261495007));
#17362=CARTESIAN_POINT('Ctrl Pts',(87.8774829307486,1.24172047149406,3.51612925744599));
#17363=CARTESIAN_POINT('Ctrl Pts',(87.8979093327466,0.907853699762734,3.61279422665573));
#17364=CARTESIAN_POINT('Ctrl Pts',(87.9056244925012,0.778483215665688,3.64286282434161));
#17365=CARTESIAN_POINT('Ctrl Pts',(87.9152138243616,0.609880139217438,3.67265498286814));
#17366=CARTESIAN_POINT('Ctrl Pts',(87.9173446773599,0.571882387746015,3.67876326663993));
#17367=CARTESIAN_POINT('Ctrl Pts',(87.9208210960351,0.50886551351341,3.68789343575293));
#17368=CARTESIAN_POINT('Ctrl Pts',(87.922183470224,0.483898752501437,3.69125239372366));
#17369=CARTESIAN_POINT('Ctrl Pts',(87.9250754732839,0.430275040529855,3.69791331365455));
#17370=CARTESIAN_POINT('Ctrl Pts',(87.9266010774839,0.40161068795367,3.70113610190029));
#17371=CARTESIAN_POINT('Ctrl Pts',(87.9310573710264,0.316896596990574,3.70966487880494));
#17372=CARTESIAN_POINT('Ctrl Pts',(87.9339428654183,0.260758826245031,3.71403317356625));
#17373=CARTESIAN_POINT('Ctrl Pts',(87.9407811663344,0.125423756418805,3.72148020688869));
#17374=CARTESIAN_POINT('Ctrl Pts',(87.9446883223599,0.0461841225284874,
3.72330688661744));
#17375=CARTESIAN_POINT('Ctrl Pts',(87.9560573757369,-0.187217556062976,
3.72123428886023));
#17376=CARTESIAN_POINT('Ctrl Pts',(87.9633811875971,-0.341147620794925,
3.71029048216468));
#17377=CARTESIAN_POINT('Ctrl Pts',(87.9791688657614,-0.666756416640207,
3.66670120513344));
#17378=CARTESIAN_POINT('Ctrl Pts',(87.9876415994009,-0.837705950818567,
3.63146032299565));
#17379=CARTESIAN_POINT('Ctrl Pts',(87.9998951845842,-1.07097413608624,3.56602012381194));
#17380=CARTESIAN_POINT('Ctrl Pts',(88.0033801533852,-1.13588333395329,3.54587837599045));
#17381=CARTESIAN_POINT('Ctrl Pts',(88.0090578889367,-1.23902946790542,3.51074862841467));
#17382=CARTESIAN_POINT('Ctrl Pts',(88.0112148840295,-1.2776340565427,3.49688447019403));
#17383=CARTESIAN_POINT('Ctrl Pts',(88.0157985028227,-1.35839172687864,3.46636597964745));
#17384=CARTESIAN_POINT('Ctrl Pts',(88.0182292967322,-1.40048534972577,3.44957413767248));
#17385=CARTESIAN_POINT('Ctrl Pts',(88.0242906514219,-1.5035908334653,3.40624541108988));
#17386=CARTESIAN_POINT('Ctrl Pts',(88.0279492723866,-1.56421615394356,3.37883415651275));
#17387=CARTESIAN_POINT('Ctrl Pts',(88.0415759974627,-1.78410681576667,3.27222578103474));
#17388=CARTESIAN_POINT('Ctrl Pts',(88.0518526138274,-1.93835925768443,3.18327666591451));
#17389=CARTESIAN_POINT('Ctrl Pts',(88.0758998126273,-2.27747090228849,2.95391618451089));
#17390=CARTESIAN_POINT('Ctrl Pts',(88.0897456316995,-2.45673161419878,2.80658633874833));
#17391=CARTESIAN_POINT('Ctrl Pts',(88.1029424526342,-2.62112000712061,2.64359555733703));
#17392=CARTESIAN_POINT('Origin',(80.1322559480305,0.,0.));
#17393=CARTESIAN_POINT('',(89.5984125828405,-2.62112000708803,2.64359555736933));
#17394=CARTESIAN_POINT('',(89.3502471949048,-2.62112000711957,2.64359555733806));
#17395=CARTESIAN_POINT('',(80.1322559480305,-2.62112000711956,2.64359555733806));
#17396=CARTESIAN_POINT('Ctrl Pts',(89.5984125828405,-2.62112000708803,2.64359555736933));
#17397=CARTESIAN_POINT('Ctrl Pts',(89.5983783641608,-2.62062322410473,2.64408811675992));
#17398=CARTESIAN_POINT('Ctrl Pts',(89.5983441417931,-2.62012629914963,2.64458053922071));
#17399=CARTESIAN_POINT('Ctrl Pts',(89.5940672226702,-2.55801239983286,2.70609694998344));
#17400=CARTESIAN_POINT('Ctrl Pts',(89.5897715287192,-2.49428457319044,2.76494692445715));
#17401=CARTESIAN_POINT('Ctrl Pts',(89.5818024515098,-2.37457448280402,2.86798494521362));
#17402=CARTESIAN_POINT('Ctrl Pts',(89.5781567756307,-2.31926640413608,2.91289274651102));
#17403=CARTESIAN_POINT('Ctrl Pts',(89.5720486682154,-2.22605659882886,2.98423687113263));
#17404=CARTESIAN_POINT('Ctrl Pts',(89.5696221294293,-2.18888958018596,3.01160419756669));
#17405=CARTESIAN_POINT('Ctrl Pts',(89.564744420832,-2.11398378151335,3.06464064227982));
#17406=CARTESIAN_POINT('Ctrl Pts',(89.5622942623307,-2.07626268607018,3.09032080947083));
#17407=CARTESIAN_POINT('Ctrl Pts',(89.5561154233189,-1.98096357064162,3.15266704013429));
#17408=CARTESIAN_POINT('Ctrl Pts',(89.5523562289654,-1.92283289339163,3.18845401018746));
#17409=CARTESIAN_POINT('Ctrl Pts',(89.5387248150602,-1.71159530661769,3.31062003856433));
#17410=CARTESIAN_POINT('Ctrl Pts',(89.5285562197113,-1.55341103921713,3.38772288606427));
#17411=CARTESIAN_POINT('Ctrl Pts',(89.5042347038918,-1.16972155402383,3.54220355641211));
#17412=CARTESIAN_POINT('Ctrl Pts',(89.4899833755887,-0.941045374096862,
3.60969434419777));
#17413=CARTESIAN_POINT('Ctrl Pts',(89.4733109962255,-0.653567184568792,
3.665342291024));
#17414=CARTESIAN_POINT('Ctrl Pts',(89.4702253776539,-0.599417279623072,
3.67458619475536));
#17415=CARTESIAN_POINT('Ctrl Pts',(89.4656234302423,-0.516859172122235,
3.68680593828053));
#17416=CARTESIAN_POINT('Ctrl Pts',(89.4640658087192,-0.488590273830709,
3.69065862383654));
#17417=CARTESIAN_POINT('Ctrl Pts',(89.4611700664737,-0.435353971747939,
3.69729162813848));
#17418=CARTESIAN_POINT('Ctrl Pts',(89.4598284813527,-0.410398360110441,
3.70014481674375));
#17419=CARTESIAN_POINT('Ctrl Pts',(89.456456987742,-0.346999767700094,3.70674391682602));
#17420=CARTESIAN_POINT('Ctrl Pts',(89.4544447785617,-0.308522879156999,
3.71014462828397));
#17421=CARTESIAN_POINT('Ctrl Pts',(89.4455349651245,-0.135760963104638,
3.72270755719113));
#17422=CARTESIAN_POINT('Ctrl Pts',(89.4389253008588,-0.00108147445861484,
3.72518283535709));
#17423=CARTESIAN_POINT('Ctrl Pts',(89.4220947337345,0.346743232374871,3.71270672055372));
#17424=CARTESIAN_POINT('Ctrl Pts',(89.4120381197272,0.558985311581401,3.6867273275733));
#17425=CARTESIAN_POINT('Ctrl Pts',(89.3974058109574,0.851795286390328,3.62500692511691));
#17426=CARTESIAN_POINT('Ctrl Pts',(89.3931568442392,0.935116938229867,3.6044119675721));
#17427=CARTESIAN_POINT('Ctrl Pts',(89.3852653390836,1.08561891704466,3.56164176340111));
#17428=CARTESIAN_POINT('Ctrl Pts',(89.381649922375,1.15302144112462,3.5403956330067));
#17429=CARTESIAN_POINT('Ctrl Pts',(89.3755879542324,1.26311629123043,3.50221488274077));
#17430=CARTESIAN_POINT('Ctrl Pts',(89.3731768517124,1.30617367567886,3.48638522468907));
#17431=CARTESIAN_POINT('Ctrl Pts',(89.3683282427091,1.39123173044083,3.45331754671148));
#17432=CARTESIAN_POINT('Ctrl Pts',(89.36589169485,1.43323141892593,3.43609884332223));
#17433=CARTESIAN_POINT('Ctrl Pts',(89.3597446531757,1.53728698918597,3.39119925772627));
#17434=CARTESIAN_POINT('Ctrl Pts',(89.356003766226,1.59891779859629,3.36258007367754));
#17435=CARTESIAN_POINT('Ctrl Pts',(89.3385012332598,1.87946910535744,3.22284471546164));
#17436=CARTESIAN_POINT('Ctrl Pts',(89.3240892785822,2.08781964671588,3.09194322582734));
#17437=CARTESIAN_POINT('Ctrl Pts',(89.3018288905159,2.38550101991659,2.86103045001828));
#17438=CARTESIAN_POINT('Ctrl Pts',(89.2940721916139,2.48492899756692,2.77511090781314));
#17439=CARTESIAN_POINT('Ctrl Pts',(89.2819941482718,2.63573790176689,2.63017358322949));
#17440=CARTESIAN_POINT('Ctrl Pts',(89.2775638755336,2.69016210078442,2.57448183728359));
#17441=CARTESIAN_POINT('Ctrl Pts',(89.2714489260246,2.76461953592262,2.49334864867993));
#17442=CARTESIAN_POINT('Ctrl Pts',(89.269675875928,2.78612688011295,2.46929257350742));
#17443=CARTESIAN_POINT('Ctrl Pts',(89.2665758784359,2.82364211182132,2.42621731722322));
#17444=CARTESIAN_POINT('Ctrl Pts',(89.2652406031047,2.83977606716401,2.40731327242714));
#17445=CARTESIAN_POINT('Ctrl Pts',(89.2621896989433,2.87657031098183,2.36331695699411));
#17446=CARTESIAN_POINT('Ctrl Pts',(89.2604831342135,2.89709311300202,2.33811364757034));
#17447=CARTESIAN_POINT('Ctrl Pts',(89.2549991535411,2.9627095556348,2.25534181007875));
#17448=CARTESIAN_POINT('Ctrl Pts',(89.2513004311705,3.00643963714966,2.19671038053934));
#17449=CARTESIAN_POINT('Ctrl Pts',(89.2341828314028,3.20405656256711,1.91478814402373));
#17450=CARTESIAN_POINT('Ctrl Pts',(89.2215597811034,3.33497924789401,1.67640183366802));
#17451=CARTESIAN_POINT('Ctrl Pts',(89.2037802820463,3.47483114918058,1.33911945690627));
#17452=CARTESIAN_POINT('Ctrl Pts',(89.1991494151813,3.5075135695305,1.2510154516963));
#17453=CARTESIAN_POINT('Ctrl Pts',(89.1906329048216,3.5603781639106,1.09007784498255));
#17454=CARTESIAN_POINT('Ctrl Pts',(89.1867820628437,3.58174196863675,1.01768654050678));
#17455=CARTESIAN_POINT('Ctrl Pts',(89.1804224464142,3.61281690981811,0.899238788898053));
#17456=CARTESIAN_POINT('Ctrl Pts',(89.1779559852729,3.6238811081814,0.853558362164017));
#17457=CARTESIAN_POINT('Ctrl Pts',(89.1730914913085,3.64377253339684,0.764059060087203));
#17458=CARTESIAN_POINT('Ctrl Pts',(89.1706964607138,3.65268128352727,0.720266431089842));
#17459=CARTESIAN_POINT('Ctrl Pts',(89.1647644245985,3.67258576521568,0.612527867379545));
#17460=CARTESIAN_POINT('Ctrl Pts',(89.1612013160963,3.68270194932705,0.548436175317296));
#17461=CARTESIAN_POINT('Ctrl Pts',(89.140610942521,3.7308000276898,0.181712396717437));
#17462=CARTESIAN_POINT('Ctrl Pts',(89.1225069996574,3.7331439834418,-0.124386153354806));
#17463=CARTESIAN_POINT('Ctrl Pts',(89.098915095069,3.68709889795588,-0.522912248360082));
#17464=CARTESIAN_POINT('Ctrl Pts',(89.0932918907188,3.67234351900059,-0.618085886174753));
#17465=CARTESIAN_POINT('Ctrl Pts',(89.084102188968,3.64162404748148,-0.775606014119531));
#17466=CARTESIAN_POINT('Ctrl Pts',(89.0804762276018,3.62770440805074,-0.83830305908965));
#17467=CARTESIAN_POINT('Ctrl Pts',(89.0752488758918,3.60483734450871,-0.930018155093909));
#17468=CARTESIAN_POINT('Ctrl Pts',(89.0735896779895,3.59714649009444,-0.95933482067506));
#17469=CARTESIAN_POINT('Ctrl Pts',(89.07058889883,3.58241797467355,-1.01280890788904));
#17470=CARTESIAN_POINT('Ctrl Pts',(89.0692418994431,3.57549244310308,-1.03699288710819));
#17471=CARTESIAN_POINT('Ctrl Pts',(89.0659934007909,3.55802841574153,-1.09572144579867));
#17472=CARTESIAN_POINT('Ctrl Pts',(89.0641057334838,3.54723158432662,-1.13018581169509));
#17473=CARTESIAN_POINT('Ctrl Pts',(89.0569367167298,3.50380542757732,-1.26204800350473));
#17474=CARTESIAN_POINT('Ctrl Pts',(89.0518189369649,3.46765012684196,-1.35824266117475));
#17475=CARTESIAN_POINT('Ctrl Pts',(89.0349855699098,3.33341721893172,-1.67493012477741));
#17476=CARTESIAN_POINT('Ctrl Pts',(89.023683582369,3.21790829069546,-1.88736171290549));
#17477=CARTESIAN_POINT('Ctrl Pts',(89.0075136338544,3.0321192529853,-2.16176904149654));
#17478=CARTESIAN_POINT('Ctrl Pts',(89.0030603253208,2.97889161431475,-2.23454605762287));
#17479=CARTESIAN_POINT('Ctrl Pts',(88.9948335641639,2.87772252040432,-2.36282562851171));
#17480=CARTESIAN_POINT('Ctrl Pts',(88.9910911700065,2.83068257878051,-2.41898059373968));
#17481=CARTESIAN_POINT('Ctrl Pts',(88.9848676364607,2.7511215014168,-2.50845771970211));
#17482=CARTESIAN_POINT('Ctrl Pts',(88.9824255227432,2.71957681224039,-2.5426229285879));
#17483=CARTESIAN_POINT('Ctrl Pts',(88.9775792497843,2.65641226263502,-2.60851429107209));
#17484=CARTESIAN_POINT('Ctrl Pts',(88.9751774219771,2.62484335254405,-2.64027840509861));
#17485=CARTESIAN_POINT('Ctrl Pts',(88.969171658286,2.54530597114271,-2.7174710352027));
#17486=CARTESIAN_POINT('Ctrl Pts',(88.9655397924824,2.49668797750549,-2.76220558799185));
#17487=CARTESIAN_POINT('Ctrl Pts',(88.9470850960456,2.24717863843847,-2.97981382718044));
#17488=CARTESIAN_POINT('Ctrl Pts',(88.9314822248832,2.02944322049996,-3.13216012224463));
#17489=CARTESIAN_POINT('Ctrl Pts',(88.906170933265,1.65405971034384,-3.33912468529458));
#17490=CARTESIAN_POINT('Ctrl Pts',(88.8965359133057,1.50563230882365,-3.40862806644198));
#17491=CARTESIAN_POINT('Ctrl Pts',(88.884642795626,1.30957450721378,-3.48512056870059));
#17492=CARTESIAN_POINT('Ctrl Pts',(88.8820350210653,1.26572753199235,-3.50128333212678));
#17493=CARTESIAN_POINT('Ctrl Pts',(88.8779885118063,1.19610701654822,-3.52546778220378));
#17494=CARTESIAN_POINT('Ctrl Pts',(88.8765217797147,1.17053179127583,-3.5340416653562));
#17495=CARTESIAN_POINT('Ctrl Pts',(88.8736418786013,1.11957848989705,-3.55050950673595));
#17496=CARTESIAN_POINT('Ctrl Pts',(88.872228406133,1.0942047082546,-3.55841114514145));
#17497=CARTESIAN_POINT('Ctrl Pts',(88.8684729008517,1.02589051638927,-3.57888501394662));
#17498=CARTESIAN_POINT('Ctrl Pts',(88.866156852475,0.982803286887197,-3.59095632487383));
#17499=CARTESIAN_POINT('Ctrl Pts',(88.8509584129739,0.694726520927777,-3.66609000663269));
#17500=CARTESIAN_POINT('Ctrl Pts',(88.8390667976081,0.44405234745131,-3.70482167298268));
#17501=CARTESIAN_POINT('Ctrl Pts',(88.8183654178315,0.0138108003517332,
-3.72696752168558));
#17502=CARTESIAN_POINT('Ctrl Pts',(88.809724245046,-0.164162344080656,-3.72337500708856));
#17503=CARTESIAN_POINT('Ctrl Pts',(88.7973539917731,-0.4074110144934,-3.70098724759685));
#17504=CARTESIAN_POINT('Ctrl Pts',(88.7939397649367,-0.473457085166123,
-3.69311901419517));
#17505=CARTESIAN_POINT('Ctrl Pts',(88.7881103829699,-0.584072730066627,
-3.67692511787763));
#17506=CARTESIAN_POINT('Ctrl Pts',(88.7857243619475,-0.628765992733442,
-3.66954661608876));
#17507=CARTESIAN_POINT('Ctrl Pts',(88.781130875323,-0.713628165726399,-3.6539407140514));
#17508=CARTESIAN_POINT('Ctrl Pts',(88.7789283040564,-0.753817710473505,
-3.64586156899731));
#17509=CARTESIAN_POINT('Ctrl Pts',(88.7730231059186,-0.860195246865727,
-3.62264282803465));
#17510=CARTESIAN_POINT('Ctrl Pts',(88.7692856344061,-0.926114235898302,
-3.60635391158795));
#17511=CARTESIAN_POINT('Ctrl Pts',(88.7558175497773,-1.15863765264743,-3.54210065517404));
#17512=CARTESIAN_POINT('Ctrl Pts',(88.7458003941647,-1.32228125109999,-3.48431911908711));
#17513=CARTESIAN_POINT('Ctrl Pts',(88.7207097738773,-1.71424589532725,-3.31431823997872));
#17514=CARTESIAN_POINT('Ctrl Pts',(88.7054904475159,-1.93625711959802,-3.18971159556248));
#17515=CARTESIAN_POINT('Ctrl Pts',(88.6886246738772,-2.18066475537463,-3.01754794215074));
#17516=CARTESIAN_POINT('Ctrl Pts',(88.6861158315554,-2.21699840101319,-2.9909551651464));
#17517=CARTESIAN_POINT('Ctrl Pts',(88.6821856526777,-2.27404496929703,-2.94759161994577));
#17518=CARTESIAN_POINT('Ctrl Pts',(88.6807388033406,-2.2950748920228,-2.93124687110775));
#17519=CARTESIAN_POINT('Ctrl Pts',(88.6778598228605,-2.3370243965377,-2.89791486339369));
#17520=CARTESIAN_POINT('Ctrl Pts',(88.6764280846079,-2.35793850266962,-2.88092340927177));
#17521=CARTESIAN_POINT('Ctrl Pts',(88.6725641530622,-2.41444352350375,-2.83398890250482));
#17522=CARTESIAN_POINT('Ctrl Pts',(88.6701605823034,-2.44966166347531,-2.80360281270346));
#17523=CARTESIAN_POINT('Ctrl Pts',(88.6588630634242,-2.61480297805074,-2.65563108924387));
#17524=CARTESIAN_POINT('Ctrl Pts',(88.6504219683624,-2.73689586753458,-2.52962092554381));
#17525=CARTESIAN_POINT('Ctrl Pts',(88.6307328282848,-3.00106509155236,-2.21536363321619));
#17526=CARTESIAN_POINT('Ctrl Pts',(88.6195323628153,-3.13503966291681,-2.02132292535156));
#17527=CARTESIAN_POINT('Ctrl Pts',(88.6039349864454,-3.28632488119421,-1.75058326728957));
#17528=CARTESIAN_POINT('Ctrl Pts',(88.6001134778783,-3.32086422689459,-1.68414157731951));
#17529=CARTESIAN_POINT('Ctrl Pts',(88.5937933316334,-3.3737057698613,-1.57453753931268));
#17530=CARTESIAN_POINT('Ctrl Pts',(88.5913362233642,-3.39323804458672,-1.53199033939784));
#17531=CARTESIAN_POINT('Ctrl Pts',(88.5864845423334,-3.42980995724489,-1.44819271146429));
#17532=CARTESIAN_POINT('Ctrl Pts',(88.5840928365297,-3.44692043440622,-1.40698179094277));
#17533=CARTESIAN_POINT('Ctrl Pts',(88.5781595289875,-3.48710994749023,-1.30504816430974));
#17534=CARTESIAN_POINT('Ctrl Pts',(88.5745915638923,-3.50934768756217,-1.24401149317139));
#17535=CARTESIAN_POINT('Ctrl Pts',(88.553966623892,-3.62699394460167,-0.892794377824449));
#17536=CARTESIAN_POINT('Ctrl Pts',(88.5358264700019,-3.68798470295983,-0.592353711252517));
#17537=CARTESIAN_POINT('Ctrl Pts',(88.5121769037604,-3.71907026873135,-0.191606689232467));
#17538=CARTESIAN_POINT('Ctrl Pts',(88.5065323665067,-3.72278981183138,-0.0950494822277428));
#17539=CARTESIAN_POINT('Ctrl Pts',(88.4973139553979,-3.72272295005873,0.0658804134627193));
#17540=CARTESIAN_POINT('Ctrl Pts',(88.4936798857592,-3.72102857088104,0.130206252110795));
#17541=CARTESIAN_POINT('Ctrl Pts',(88.4884465217943,-3.71608640439314,0.224690529694151));
#17542=CARTESIAN_POINT('Ctrl Pts',(88.4867888945916,-3.71413635131042,0.254902497261594));
#17543=CARTESIAN_POINT('Ctrl Pts',(88.4839293988324,-3.71008940424378,0.307593300712719));
#17544=CARTESIAN_POINT('Ctrl Pts',(88.4827193497549,-3.70815635433156,0.330081057069221));
#17545=CARTESIAN_POINT('Ctrl Pts',(88.4797113045783,-3.7027949605819,0.38643998925021));
#17546=CARTESIAN_POINT('Ctrl Pts',(88.4779268546235,-3.69910638263114,0.42028385159385));
#17547=CARTESIAN_POINT('Ctrl Pts',(88.4714594312061,-3.68388030997718,0.544183697253454));
#17548=CARTESIAN_POINT('Ctrl Pts',(88.4669047634828,-3.66951327957472,0.633864703046565));
#17549=CARTESIAN_POINT('Ctrl Pts',(88.4538739503025,-3.61813924745274,0.893378449656369));
#17550=CARTESIAN_POINT('Ctrl Pts',(88.44562527822,-3.57250571857085,1.06125601110274));
#17551=CARTESIAN_POINT('Ctrl Pts',(88.4284338128901,-3.45461863748153,1.39945659590232));
#17552=CARTESIAN_POINT('Ctrl Pts',(88.4194984320634,-3.38107645317056,1.56881596478263));
#17553=CARTESIAN_POINT('Ctrl Pts',(88.4067204799356,-3.26349299061986,1.79252714591052));
#17554=CARTESIAN_POINT('Ctrl Pts',(88.4032158750203,-3.23003119835978,1.85214410795675));
#17555=CARTESIAN_POINT('Ctrl Pts',(88.3972779647094,-3.17152755356454,1.94996478133264));
#17556=CARTESIAN_POINT('Ctrl Pts',(88.3948764007927,-3.14738933677125,1.98869047224285));
#17557=CARTESIAN_POINT('Ctrl Pts',(88.3899962656051,-3.09743808038409,2.06564067067064));
#17558=CARTESIAN_POINT('Ctrl Pts',(88.3875175776027,-3.07161437044837,2.10384860328771));
#17559=CARTESIAN_POINT('Ctrl Pts',(88.3811519324637,-3.00419673595804,2.1997096057063));
#17560=CARTESIAN_POINT('Ctrl Pts',(88.3772303670927,-2.96165025350118,2.25666728368062));
#17561=CARTESIAN_POINT('Ctrl Pts',(88.3684150657029,-2.86382866378502,2.38008812485602));
#17562=CARTESIAN_POINT('Ctrl Pts',(88.3634964901018,-2.8078174721378,2.44591366981495));
#17563=CARTESIAN_POINT('Ctrl Pts',(88.3549444113181,-2.70785514815031,2.55542887415017));
#17564=CARTESIAN_POINT('Ctrl Pts',(88.351345304935,-2.66502431353806,2.60006452616581));
#17565=CARTESIAN_POINT('Ctrl Pts',(88.3477258555205,-2.62111983094262,2.64359573201716));
#17566=CARTESIAN_POINT('',(88.2572559480606,-3.72274871244099,-0.00309621042271729));
#17567=CARTESIAN_POINT('Ctrl Pts',(88.1029424526342,-2.62112000712061,2.64359555733703));
#17568=CARTESIAN_POINT('Ctrl Pts',(88.1041532669587,-2.63620271695778,2.62864107899177));
#17569=CARTESIAN_POINT('Ctrl Pts',(88.105358311338,-2.65116024039027,2.6135547508114));
#17570=CARTESIAN_POINT('Ctrl Pts',(88.1090818796747,-2.69724005597925,2.56627515837679));
#17571=CARTESIAN_POINT('Ctrl Pts',(88.1115763284437,-2.72790974294777,2.53364971702599));
#17572=CARTESIAN_POINT('Ctrl Pts',(88.1154899655916,-2.77584500242704,2.48077793296012));
#17573=CARTESIAN_POINT('Ctrl Pts',(88.1169342969881,-2.79349439765197,2.46088678757825));
#17574=CARTESIAN_POINT('Ctrl Pts',(88.1198134978056,-2.82863138308299,2.42042165591336));
#17575=CARTESIAN_POINT('Ctrl Pts',(88.1212478706564,-2.84611124018731,2.3998432010622));
#17576=CARTESIAN_POINT('Ctrl Pts',(88.1251289890557,-2.89327084463644,2.34308367387563));
#17577=CARTESIAN_POINT('Ctrl Pts',(88.1275466613924,-2.92249551266324,2.30652934882947));
#17578=CARTESIAN_POINT('Ctrl Pts',(88.1382986841977,-3.05118439093271,2.13919056682107));
#17579=CARTESIAN_POINT('Ctrl Pts',(88.1462401225262,-3.14262052111368,2.00245028441192));
#17580=CARTESIAN_POINT('Ctrl Pts',(88.1668144288718,-3.35677608955448,1.63118478771012));
#17581=CARTESIAN_POINT('Ctrl Pts',(88.1793536890746,-3.46406346664572,1.38887158132868));
#17582=CARTESIAN_POINT('Ctrl Pts',(88.1960795984351,-3.56489226127524,1.07458863044898));
#17583=CARTESIAN_POINT('Ctrl Pts',(88.1994597821775,-3.58332838559592,1.01141217252422));
#17584=CARTESIAN_POINT('Ctrl Pts',(88.2052262966283,-3.61147194523394,0.904511005190628));
#17585=CARTESIAN_POINT('Ctrl Pts',(88.2075840319613,-3.62208249910761,0.861038856598137));
#17586=CARTESIAN_POINT('Ctrl Pts',(88.2124462260877,-3.6421329738008,0.771948335350112));
#17587=CARTESIAN_POINT('Ctrl Pts',(88.2149523062546,-3.65150536341464,0.726323033160018));
#17588=CARTESIAN_POINT('Ctrl Pts',(88.2200745264829,-3.66872512758083,0.633712597483294));
#17589=CARTESIAN_POINT('Ctrl Pts',(88.2226913962652,-3.67653162855893,0.586728746738759));
#17590=CARTESIAN_POINT('Ctrl Pts',(88.2354168265011,-3.70976514497697,0.359873053982928));
#17591=CARTESIAN_POINT('Ctrl Pts',(88.245881282912,-3.72290178407679,0.178473664449434));
#17592=CARTESIAN_POINT('Ctrl Pts',(88.2565361263338,-3.72274867707829,-0.00313844099074864));
#17593=CARTESIAN_POINT('Ctrl Pts',(88.2572559480606,-3.72274871244099,-0.00309621042271729));
#17594=CARTESIAN_POINT('Ctrl Pts',(88.2646021442827,-3.72263426646549,-0.140701072421199));
#17595=CARTESIAN_POINT('Ctrl Pts',(88.2719483405047,-3.71488660768827,-0.277983462742277));
#17596=CARTESIAN_POINT('Ctrl Pts',(88.2792945367267,-3.69963501555635,-0.414208056620568));
#17597=CARTESIAN_POINT('Ctrl Pts',(88.2867550257305,-3.68414613778178,-0.552552044987124));
#17598=CARTESIAN_POINT('Ctrl Pts',(88.2942155147343,-3.66091805396147,-0.689805171380509));
#17599=CARTESIAN_POINT('Ctrl Pts',(88.3016760037381,-3.63013505052346,-0.825219411708824));
#17600=CARTESIAN_POINT('Ctrl Pts',(88.3046127904125,-3.61801746490033,-0.878524595365555));
#17601=CARTESIAN_POINT('Ctrl Pts',(88.3075495770868,-3.60472971913711,-0.931545061605505));
#17602=CARTESIAN_POINT('Ctrl Pts',(88.3104863637612,-3.59028508188239,-0.98423604552605));
#17603=CARTESIAN_POINT('Ctrl Pts',(88.3164524120401,-3.56094096779148,-1.0912771720328));
#17604=CARTESIAN_POINT('Ctrl Pts',(88.3224184603191,-3.52675840703198,-1.19717735641402));
#17605=CARTESIAN_POINT('Ctrl Pts',(88.328384508598,-3.48784301668361,-1.30146788414905));
#17606=CARTESIAN_POINT('Ctrl Pts',(88.3343429893628,-3.44897698778097,-1.40562612665759));
#17607=CARTESIAN_POINT('Ctrl Pts',(88.3403014701276,-3.40539021220487,-1.50817838543764));
#17608=CARTESIAN_POINT('Ctrl Pts',(88.3462599508923,-3.3572386024678,-1.60866917935293));
#17609=CARTESIAN_POINT('Ctrl Pts',(88.3522124909595,-3.30913500063087,-1.70905978239142));
#17610=CARTESIAN_POINT('Ctrl Pts',(88.3581650310268,-3.25647579655805,-1.80739263475249));
#17611=CARTESIAN_POINT('Ctrl Pts',(88.364117571094,-3.19946543296315,-1.90323106998965));
#17612=CARTESIAN_POINT('Ctrl Pts',(88.3700659525545,-3.14249489836185,-1.99900254988424));
#17613=CARTESIAN_POINT('Ctrl Pts',(88.376014334015,-3.08117946358779,-2.09228272193326));
#17614=CARTESIAN_POINT('Ctrl Pts',(88.3819627154755,-3.01576972954598,-2.1826590436562));
#17615=CARTESIAN_POINT('Ctrl Pts',(88.3879088995304,-2.9503841586676,-2.27300197924993));
#17616=CARTESIAN_POINT('Ctrl Pts',(88.3938550835854,-2.88090753952243,-2.36044285979049));
#17617=CARTESIAN_POINT('Ctrl Pts',(88.3998012676404,-2.80763370279342,-2.44459823967836));
#17618=CARTESIAN_POINT('Ctrl Pts',(88.4057467165196,-2.73436892551189,-2.52874321474401));
#17619=CARTESIAN_POINT('Ctrl Pts',(88.4116921653989,-2.65730813807171,-2.60960318263874));
#17620=CARTESIAN_POINT('Ctrl Pts',(88.4176376142782,-2.57678485283428,-2.68682849930989));
#17621=CARTESIAN_POINT('Ctrl Pts',(88.423583789286,-2.49625173314121,-2.76406324764976));
#17622=CARTESIAN_POINT('Ctrl Pts',(88.4295299642938,-2.41225557608458,-2.83766217391017));
#17623=CARTESIAN_POINT('Ctrl Pts',(88.4354761393016,-2.32516550554824,-2.90731369726568));
#17624=CARTESIAN_POINT('Ctrl Pts',(88.441428237806,-2.23798867709732,-2.97703460649807));
#17625=CARTESIAN_POINT('Ctrl Pts',(88.4473803363105,-2.14771210457599,-3.04279999665133));
#17626=CARTESIAN_POINT('Ctrl Pts',(88.453332434815,-2.05473675010977,-3.10433961580371));
#17627=CARTESIAN_POINT('Ctrl Pts',(88.459287463955,-1.96171561735466,-3.16590953522739));
#17628=CARTESIAN_POINT('Ctrl Pts',(88.4652424930951,-1.86599341268227,-3.22324932332814));
#17629=CARTESIAN_POINT('Ctrl Pts',(88.4711975222352,-1.76799713788626,-3.27613395375189));
#17630=CARTESIAN_POINT('Ctrl Pts',(88.4771622299419,-1.66984159208639,-3.32910453630182));
#17631=CARTESIAN_POINT('Ctrl Pts',(88.4831269376485,-1.5694049662657,-3.37760530968939));
#17632=CARTESIAN_POINT('Ctrl Pts',(88.4890916453551,-1.46713619053383,-3.42145860137543));
#17633=CARTESIAN_POINT('Ctrl Pts',(88.4947508385346,-1.37010565918835,-3.46306571129821));
#17634=CARTESIAN_POINT('Ctrl Pts',(88.5004100317141,-1.27142630185272,-3.50048953684433));
#17635=CARTESIAN_POINT('Ctrl Pts',(88.5060692248936,-1.17149313307071,-3.5336201552612));
#17636=CARTESIAN_POINT('Ctrl Pts',(88.5120351479814,-1.06614355761611,-3.56854646278557));
#17637=CARTESIAN_POINT('Ctrl Pts',(88.5180010710692,-0.959060901017507,
-3.59881371921158));
#17638=CARTESIAN_POINT('Ctrl Pts',(88.523966994157,-0.850693777783829,-3.62424994432502));
#17639=CARTESIAN_POINT('Ctrl Pts',(88.5299253496939,-0.742464114205368,
-3.64965390453532));
#17640=CARTESIAN_POINT('Ctrl Pts',(88.5358837052307,-0.63295362662988,-3.67023892532855));
#17641=CARTESIAN_POINT('Ctrl Pts',(88.5418420607675,-0.522627803341301,
-3.68588222026622));
#17642=CARTESIAN_POINT('Ctrl Pts',(88.5477944757295,-0.412411976644462,
-3.70150991859128));
#17643=CARTESIAN_POINT('Ctrl Pts',(88.5537468906916,-0.301382841783696,
-3.71220563298313));
#17644=CARTESIAN_POINT('Ctrl Pts',(88.5596993056537,-0.190017136997689,
-3.71789739639856));
#17645=CARTESIAN_POINT('Ctrl Pts',(88.5656475627016,-0.0787292240061793,
-3.72358518397161));
#17646=CARTESIAN_POINT('Ctrl Pts',(88.5715958197495,0.0328943761053461,
-3.72427595236333));
#17647=CARTESIAN_POINT('Ctrl Pts',(88.5775440767974,0.144371408924188,-3.71994952368782));
#17648=CARTESIAN_POINT('Ctrl Pts',(88.5834901369028,0.255807268568044,-3.71562469294509));
#17649=CARTESIAN_POINT('Ctrl Pts',(88.5894361970082,0.367096252431375,-3.70628636522292));
#17650=CARTESIAN_POINT('Ctrl Pts',(88.5953822571136,0.477756352484418,-3.69196647197138));
#17651=CARTESIAN_POINT('Ctrl Pts',(88.6013275826489,0.588402781703338,-3.67764834778461));
#17652=CARTESIAN_POINT('Ctrl Pts',(88.6072729081842,0.69842006819559,-3.65834993549135));
#17653=CARTESIAN_POINT('Ctrl Pts',(88.6132182337196,0.807332333122118,-3.63415493153437));
#17654=CARTESIAN_POINT('Ctrl Pts',(88.6191642861319,0.916257913690046,-3.60995696949001));
#17655=CARTESIAN_POINT('Ctrl Pts',(88.6251103385442,1.02407779715116,-3.58086131636578));
#17656=CARTESIAN_POINT('Ctrl Pts',(88.6310563909565,1.1303280374453,-3.54700240911464));
#17657=CARTESIAN_POINT('Ctrl Pts',(88.6370083687989,1.23668415947741,-3.51310976038738));
#17658=CARTESIAN_POINT('Ctrl Pts',(88.6429603466413,1.34146711565789,-3.47444450230322));
#17659=CARTESIAN_POINT('Ctrl Pts',(88.6489123244836,1.44422970256022,-3.43119048272503));
#17660=CARTESIAN_POINT('Ctrl Pts',(88.6548672338371,1.54704290283419,-3.38791515936466));
#17661=CARTESIAN_POINT('Ctrl Pts',(88.6608221431906,1.64783337417348,-3.34004674994136));
#17662=CARTESIAN_POINT('Ctrl Pts',(88.666777052544,1.74617711412755,-3.28781584773192));
#17663=CARTESIAN_POINT('Ctrl Pts',(88.6727416432172,1.84468073849385,-3.23550003003012));
#17664=CARTESIAN_POINT('Ctrl Pts',(88.6787062338903,1.94072932268429,-3.17880775858277));
#17665=CARTESIAN_POINT('Ctrl Pts',(88.6846708245634,2.03392611576056,-3.11801413052077));
#17666=CARTESIAN_POINT('Ctrl Pts',(88.6903312450509,2.12237024643251,-3.0603207334965));
#17667=CARTESIAN_POINT('Ctrl Pts',(88.6959916655384,2.2082460307644,-2.9989341534039));
#17668=CARTESIAN_POINT('Ctrl Pts',(88.7016520860259,2.29124277537432,-2.93412237420238));
#17669=CARTESIAN_POINT('Ctrl Pts',(88.7076181048113,2.37872039979447,-2.8658114964006));
#17670=CARTESIAN_POINT('Ctrl Pts',(88.7135841235967,2.46328144756805,-2.79347504670955));
#17671=CARTESIAN_POINT('Ctrl Pts',(88.719550142382,2.54453405527325,-2.71739102891996));
#17672=CARTESIAN_POINT('Ctrl Pts',(88.725508592765,2.62568358713349,-2.64140353017932));
#17673=CARTESIAN_POINT('Ctrl Pts',(88.731467043148,2.70353272353865,-2.56167820019026));
#17674=CARTESIAN_POINT('Ctrl Pts',(88.737425493531,2.7777211860168,-2.47853436031326));
#17675=CARTESIAN_POINT('Ctrl Pts',(88.7433780023797,2.85183567065308,-2.39547342823124));
#17676=CARTESIAN_POINT('Ctrl Pts',(88.7493305112283,2.92229646595111,-2.30900107608306));
#17677=CARTESIAN_POINT('Ctrl Pts',(88.7552830200769,2.98877934918925,-2.2194741639316));
#17678=CARTESIAN_POINT('Ctrl Pts',(88.7612313691924,3.0552157728482,-2.13000981499135));
#17679=CARTESIAN_POINT('Ctrl Pts',(88.7671797183078,3.11767956629616,-2.03749548588472));
#17680=CARTESIAN_POINT('Ctrl Pts',(88.7731280674232,3.17588654864072,-1.94232134124684));
#17681=CARTESIAN_POINT('Ctrl Pts',(88.7790742184606,3.23407202190977,-1.84718236606427));
#17682=CARTESIAN_POINT('Ctrl Pts',(88.785020369498,3.28800359400462,-1.74938588457056));
#17683=CARTESIAN_POINT('Ctrl Pts',(88.7909665205354,3.33744058709227,-1.64935074806094));
#17684=CARTESIAN_POINT('Ctrl Pts',(88.796911935768,3.38687146261316,-1.54932799037107));
#17685=CARTESIAN_POINT('Ctrl Pts',(88.8028573510006,3.43180868055454,-1.44706750231301));
#17686=CARTESIAN_POINT('Ctrl Pts',(88.8088027662332,3.47205804118375,-1.34301173529917));
#17687=CARTESIAN_POINT('Ctrl Pts',(88.8147489070081,3.51231231360008,-1.23894326995253));
#17688=CARTESIAN_POINT('Ctrl Pts',(88.820695047783,3.54787744128388,-1.13307947907829));
#17689=CARTESIAN_POINT('Ctrl Pts',(88.8266411885579,3.57860806773621,-1.02588101650888));
#17690=CARTESIAN_POINT('Ctrl Pts',(88.8325932521278,3.60936930416032,-0.918575776359818));
#17691=CARTESIAN_POINT('Ctrl Pts',(88.8385453156978,3.63528630474838,-0.809933610416527));
#17692=CARTESIAN_POINT('Ctrl Pts',(88.8444973792677,3.65626411656129,-0.700428634798912));
#17693=CARTESIAN_POINT('Ctrl Pts',(88.8504523730391,3.67725225575308,-0.590869749870746));
#17694=CARTESIAN_POINT('Ctrl Pts',(88.8564073668105,3.69329630096893,-0.480447621677139));
#17695=CARTESIAN_POINT('Ctrl Pts',(88.862362360582,3.70435306530166,-0.369642976519477));
#17696=CARTESIAN_POINT('Ctrl Pts',(88.8683270325657,3.71542779937819,-0.258658248742223));
#17697=CARTESIAN_POINT('Ctrl Pts',(88.8742917045494,3.72149903216251,-0.147290178647985));
#17698=CARTESIAN_POINT('Ctrl Pts',(88.8802563765331,3.72257572318515,-0.0360214887612145));
#17699=CARTESIAN_POINT('Ctrl Pts',(88.8859159000748,3.72359733144901,0.0695547728663779));
#17700=CARTESIAN_POINT('Ctrl Pts',(88.8915754236166,3.72012280657342,0.175041267955078));
#17701=CARTESIAN_POINT('Ctrl Pts',(88.8972349471584,3.71220287368453,0.280031046686448));
#17702=CARTESIAN_POINT('Ctrl Pts',(88.9032012709903,3.70385360470569,0.390712275297176));
#17703=CARTESIAN_POINT('Ctrl Pts',(88.9091675948222,3.6905365666675,0.50119802511437));
#17704=CARTESIAN_POINT('Ctrl Pts',(88.9151339186541,3.67226589290483,0.611007998562921));
#17705=CARTESIAN_POINT('Ctrl Pts',(88.9210926761652,3.6540183894869,0.72067871415086));
#17706=CARTESIAN_POINT('Ctrl Pts',(88.9270514336763,3.63082981102373,0.829674949827213));
#17707=CARTESIAN_POINT('Ctrl Pts',(88.9330101911873,3.60276618805977,0.937519790016859));
#17708=CARTESIAN_POINT('Ctrl Pts',(88.9389630088252,3.57473053978036,1.04525712714507));
#17709=CARTESIAN_POINT('Ctrl Pts',(88.9449158264631,3.54182961757212,1.15184495044759));
#17710=CARTESIAN_POINT('Ctrl Pts',(88.950868644101,3.50418068271759,1.25681554150516));
#17711=CARTESIAN_POINT('Ctrl Pts',(88.9568173032376,3.46655804854129,1.36171280252696));
#17712=CARTESIAN_POINT('Ctrl Pts',(88.9627659623743,3.42419413993121,1.46499468741295));
#17713=CARTESIAN_POINT('Ctrl Pts',(88.9687146215109,3.37725613496972,1.56620833904989));
#17714=CARTESIAN_POINT('Ctrl Pts',(88.9746610832101,3.33033546892934,1.66738460231627));
#17715=CARTESIAN_POINT('Ctrl Pts',(88.9806075449093,3.27884424083381,1.76649377348942));
#17716=CARTESIAN_POINT('Ctrl Pts',(88.9865540066085,3.2229976213808,1.86310329694135));
#17717=CARTESIAN_POINT('Ctrl Pts',(88.9924997327737,3.16715790974735,1.95970087049975));
#17718=CARTESIAN_POINT('Ctrl Pts',(88.9984454589389,3.10696408677016,2.05379905038773));
#17719=CARTESIAN_POINT('Ctrl Pts',(89.0043911851041,3.04267673217578,2.14499087783052));
#17720=CARTESIAN_POINT('Ctrl Pts',(89.0103376367129,2.9783815338214,2.23619383167308));
#17721=CARTESIAN_POINT('Ctrl Pts',(89.0162840883218,2.90999205138104,2.32448938755635));
#17722=CARTESIAN_POINT('Ctrl Pts',(89.0222305399306,2.83781109306914,2.4095011439204));
#17723=CARTESIAN_POINT('Ctrl Pts',(89.0281829122409,2.7655582663663,2.49459754391186));
#17724=CARTESIAN_POINT('Ctrl Pts',(89.0341352845512,2.68950669308204,2.57640329466123));
#17725=CARTESIAN_POINT('Ctrl Pts',(89.0400876568615,2.60999833028177,2.6545764781649));
#17726=CARTESIAN_POINT('Ctrl Pts',(89.0460429586881,2.53045083668973,2.73278813533925));
#17727=CARTESIAN_POINT('Ctrl Pts',(89.0519982605147,2.44744347377688,2.80736338406813));
#17728=CARTESIAN_POINT('Ctrl Pts',(89.0579535623413,2.36135240111219,2.87799972207464));
#17729=CARTESIAN_POINT('Ctrl Pts',(89.0639185379399,2.27512148240209,2.94875080150818));
#17730=CARTESIAN_POINT('Ctrl Pts',(89.0698835135385,2.18579717817438,3.0155499338919));
#17731=CARTESIAN_POINT('Ctrl Pts',(89.0758484891371,2.09378622149929,3.07813690747499));
#17732=CARTESIAN_POINT('Ctrl Pts',(89.081504928855,2.00653449327098,3.13748659589294));
#17733=CARTESIAN_POINT('Ctrl Pts',(89.0871613685729,1.91686735019243,3.19304881204709));
#17734=CARTESIAN_POINT('Ctrl Pts',(89.0928178082907,1.82515095864938,3.24464043318227));
#17735=CARTESIAN_POINT('Ctrl Pts',(89.0987830432115,1.72842760457343,3.29904853357149));
#17736=CARTESIAN_POINT('Ctrl Pts',(89.1047482781323,1.62911316686676,3.34921567300339));
#17737=CARTESIAN_POINT('Ctrl Pts',(89.1107135130531,1.52761502358576,3.39488731804387));
#17738=CARTESIAN_POINT('Ctrl Pts',(89.1166711804925,1.4262456405835,3.44050102415506));
#17739=CARTESIAN_POINT('Ctrl Pts',(89.1226288479319,1.32269843816678,3.48163040728767));
#17740=CARTESIAN_POINT('Ctrl Pts',(89.1285865153713,1.21740676315428,3.51806599362863));
#17741=CARTESIAN_POINT('Ctrl Pts',(89.1345382431768,1.11222006110562,3.55446525467145));
#17742=CARTESIAN_POINT('Ctrl Pts',(89.1404899709822,1.00529273785723,3.58617989128365));
#17743=CARTESIAN_POINT('Ctrl Pts',(89.1464416987876,0.897078898501409,3.61304816081429));
#17744=CARTESIAN_POINT('Ctrl Pts',(89.1523892728783,0.788940581655154,3.63989767896197));
#17745=CARTESIAN_POINT('Ctrl Pts',(89.158336846969,0.679517938242419,3.66190745780231));
#17746=CARTESIAN_POINT('Ctrl Pts',(89.1642844210597,0.569280388242783,3.67896553423135));
#17747=CARTESIAN_POINT('Ctrl Pts',(89.1702298009894,0.459083506746855,3.6960173176464));
#17748=CARTESIAN_POINT('Ctrl Pts',(89.176175180919,0.348072727954916,3.70812096659158));
#17749=CARTESIAN_POINT('Ctrl Pts',(89.1821205608486,0.236727189724005,3.71521571381062));
#17750=CARTESIAN_POINT('Ctrl Pts',(89.1880652097681,0.125395341908594,3.72230958869981));
#17751=CARTESIAN_POINT('Ctrl Pts',(89.1940098586876,0.0137292326501387,
3.72439576015319));
#17752=CARTESIAN_POINT('Ctrl Pts',(89.199954507607,-0.0977881239321674,
3.72146544325187));
#17753=CARTESIAN_POINT('Ctrl Pts',(89.2058998877447,-0.209319197645145,
3.71853476590854));
#17754=CARTESIAN_POINT('Ctrl Pts',(89.2118452678825,-0.320701065401263,
3.71058638477275));
#17755=CARTESIAN_POINT('Ctrl Pts',(89.2177906480202,-0.431452730676845,
3.69766360066617));
#17756=CARTESIAN_POINT('Ctrl Pts',(89.2237419645574,-0.542314980325008,
3.68472791329562));
#17757=CARTESIAN_POINT('Ctrl Pts',(89.2296932810946,-0.652545355448581,
3.66680794954585));
#17758=CARTESIAN_POINT('Ctrl Pts',(89.2356445976319,-0.761669852515796,
3.64399870997076));
#17759=CARTESIAN_POINT('Ctrl Pts',(89.2415988506798,-0.87084819401371,3.62117821581441));
#17760=CARTESIAN_POINT('Ctrl Pts',(89.2475531037277,-0.9789191659806,3.59346374235548));
#17761=CARTESIAN_POINT('Ctrl Pts',(89.2535073567756,-1.08542260946939,3.56100060676106));
#17762=CARTESIAN_POINT('Ctrl Pts',(89.2594713065714,-1.19209949823035,3.52848460360477));
#17763=CARTESIAN_POINT('Ctrl Pts',(89.2654352563672,-1.29720336343462,3.49120462383835));
#17764=CARTESIAN_POINT('Ctrl Pts',(89.271399206163,-1.40029229414812,3.44935487496567));
#17765=CARTESIAN_POINT('Ctrl Pts',(89.277066360583,-1.49825101435125,3.40958777473466));
#17766=CARTESIAN_POINT('Ctrl Pts',(89.2827335150031,-1.59439024991325,3.36569493467304));
#17767=CARTESIAN_POINT('Ctrl Pts',(89.2884006694231,-1.68835254050114,3.31788083895178));
#17768=CARTESIAN_POINT('Ctrl Pts',(89.2943662008,-1.78726196685464,3.26754932032008));
#17769=CARTESIAN_POINT('Ctrl Pts',(89.3003317321768,-1.8840781706993,3.2127099734771));
#17770=CARTESIAN_POINT('Ctrl Pts',(89.3062972635537,-1.97836354151181,3.15356072719662));
#17771=CARTESIAN_POINT('Ctrl Pts',(89.3122561474734,-2.07254384909974,3.09447739157113));
#17772=CARTESIAN_POINT('Ctrl Pts',(89.3182150313931,-2.16419857771386,3.03109391957071));
#17773=CARTESIAN_POINT('Ctrl Pts',(89.3241739153128,-2.25291301874604,2.96365492128631));
#17774=CARTESIAN_POINT('Ctrl Pts',(89.3301264569248,-2.34153303701452,2.89628770135644));
#17775=CARTESIAN_POINT('Ctrl Pts',(89.3360789985367,-2.42721866449201,2.82487379474726));
#17776=CARTESIAN_POINT('Ctrl Pts',(89.3420315401486,-2.50958348575806,2.74970149116416));
#17777=CARTESIAN_POINT('Ctrl Pts',(89.344770091734,-2.54747659538451,2.71511740178278));
#17778=CARTESIAN_POINT('Ctrl Pts',(89.3475086433194,-2.58466723458277,2.67973841252858));
#17779=CARTESIAN_POINT('Ctrl Pts',(89.3502471949048,-2.62112000711957,2.64359555733806));
#17780=CARTESIAN_POINT('Origin',(81.4430005297901,0.,0.));
#17781=CARTESIAN_POINT('',(82.8471929193648,-4.43299894467431,0.00305884233546028));
#17782=CARTESIAN_POINT('',(82.4431778927679,1.9715882987731,3.9704317876197));
#17783=CARTESIAN_POINT('Ctrl Pts',(82.8471929193386,-4.43299894467391,0.00305884291686582));
#17784=CARTESIAN_POINT('Ctrl Pts',(82.838350910046,-4.43286333405117,0.199591245476362));
#17785=CARTESIAN_POINT('Ctrl Pts',(82.8295089007534,-4.41965490319418,0.395644430212545));
#17786=CARTESIAN_POINT('Ctrl Pts',(82.8206668914608,-4.39358256713249,0.589848476974774));
#17787=CARTESIAN_POINT('Ctrl Pts',(82.8188675761831,-4.38827694585923,0.629368262214482));
#17788=CARTESIAN_POINT('Ctrl Pts',(82.8170682609054,-4.3824387600355,0.668811577215154));
#17789=CARTESIAN_POINT('Ctrl Pts',(82.8152689456277,-4.37606998213278,0.708167008181277));
#17790=CARTESIAN_POINT('Ctrl Pts',(82.8095434643006,-4.35580431807122,0.833397304344789));
#17791=CARTESIAN_POINT('Ctrl Pts',(82.8038179829734,-4.33012882713862,0.957942294294973));
#17792=CARTESIAN_POINT('Ctrl Pts',(82.7980925016463,-4.29910184415742,1.08130122239931));
#17793=CARTESIAN_POINT('Ctrl Pts',(82.792373877528,-4.26811202110914,1.20451240782769));
#17794=CARTESIAN_POINT('Ctrl Pts',(82.7866552534097,-4.23178355475547,1.32653997614935));
#17795=CARTESIAN_POINT('Ctrl Pts',(82.7809366292914,-4.19022620725604,1.44689091918662));
#17796=CARTESIAN_POINT('Ctrl Pts',(82.7752234540714,-4.14870845700185,1.56712718777775));
#17797=CARTESIAN_POINT('Ctrl Pts',(82.7695102788515,-4.10197186958025,1.68568963731331));
#17798=CARTESIAN_POINT('Ctrl Pts',(82.7637971036315,-4.05017655073995,1.80209847340156));
#17799=CARTESIAN_POINT('Ctrl Pts',(82.7577924778341,-3.99573895768253,1.92444576248378));
#17800=CARTESIAN_POINT('Ctrl Pts',(82.7517878520368,-3.9357130141655,2.04441348614045));
#17801=CARTESIAN_POINT('Ctrl Pts',(82.7457832262395,-3.87034305857968,2.16146561594306));
#17802=CARTESIAN_POINT('Ctrl Pts',(82.7400762563077,-3.80821356316094,2.27271534369876));
#17803=CARTESIAN_POINT('Ctrl Pts',(82.734369286376,-3.74125734116528,2.38133119183427));
#17804=CARTESIAN_POINT('Ctrl Pts',(82.7286623164443,-3.66973201008125,2.48687675090364));
#17805=CARTESIAN_POINT('Ctrl Pts',(82.7229561860919,-3.5982172014279,2.59240678266523));
#17806=CARTESIAN_POINT('Ctrl Pts',(82.7172500557396,-3.52213484344504,2.69486709560078));
#17807=CARTESIAN_POINT('Ctrl Pts',(82.7115439253873,-3.44178611010701,2.79384991942561));
#17808=CARTESIAN_POINT('Ctrl Pts',(82.705837369286,-3.36143138174511,2.89284012861131));
#17809=CARTESIAN_POINT('Ctrl Pts',(82.7001308131848,-3.27680989489711,2.98835202452487));
#17810=CARTESIAN_POINT('Ctrl Pts',(82.6944242570835,-3.18826305183751,3.08001099223489));
#17811=CARTESIAN_POINT('Ctrl Pts',(82.6887160099204,-3.0996899691001,3.17169712185942));
#17812=CARTESIAN_POINT('Ctrl Pts',(82.6830077627572,-3.00718949135207,3.259527766406));
#17813=CARTESIAN_POINT('Ctrl Pts',(82.677299515594,-2.91113944295518,3.34316558723474));
#17814=CARTESIAN_POINT('Ctrl Pts',(82.6715852762598,-2.8149885670524,3.42689120596689));
#17815=CARTESIAN_POINT('Ctrl Pts',(82.6658710369255,-2.71528098050195,3.50641495259866));
#17816=CARTESIAN_POINT('Ctrl Pts',(82.6601567975912,-2.61242735439016,3.58143997828165));
#17817=CARTESIAN_POINT('Ctrl Pts',(82.6544390802149,-2.50951112515441,3.65651066886883));
#17818=CARTESIAN_POINT('Ctrl Pts',(82.6487213628387,-2.40344537098648,3.72707696357266));
#17819=CARTESIAN_POINT('Ctrl Pts',(82.6430036454624,-2.29466821463525,3.79288633954969));
#17820=CARTESIAN_POINT('Ctrl Pts',(82.6372780135051,-2.18574048672624,3.8587868102068));
#17821=CARTESIAN_POINT('Ctrl Pts',(82.6315523815478,-2.07409420998285,3.91991702478709));
#17822=CARTESIAN_POINT('Ctrl Pts',(82.6258267495906,-1.96019076016078,3.9760710737838));
#17823=CARTESIAN_POINT('Ctrl Pts',(82.6237798612255,-1.91947077537578,3.99614590052816));
#17824=CARTESIAN_POINT('Ctrl Pts',(82.6217329728604,-1.87846248902875,4.0155852111556));
#17825=CARTESIAN_POINT('Ctrl Pts',(82.6196860844953,-1.83718750489339,4.03438112625265));
#17826=CARTESIAN_POINT('Ctrl Pts',(82.6140967735162,-1.72448046823902,4.08570596467894));
#17827=CARTESIAN_POINT('Ctrl Pts',(82.608507462537,-1.60940687031023,4.13240137103484));
#17828=CARTESIAN_POINT('Ctrl Pts',(82.6029181515579,-1.49239253067008,4.17423688048488));
#17829=CARTESIAN_POINT('Ctrl Pts',(82.5973357789645,-1.37552344875908,4.21602045671786));
#17830=CARTESIAN_POINT('Ctrl Pts',(82.591753406371,-1.25671880267868,4.25295598841567));
#17831=CARTESIAN_POINT('Ctrl Pts',(82.5861710337776,-1.13642768496985,4.28485952124852));
#17832=CARTESIAN_POINT('Ctrl Pts',(82.5805940635969,-1.0162529805341,4.31673217902799));
#17833=CARTESIAN_POINT('Ctrl Pts',(82.5750170934162,-0.894595065335974,
4.34358241337939));
#17834=CARTESIAN_POINT('Ctrl Pts',(82.5694401232355,-0.771920950848933,
4.36527513974096));
#17835=CARTESIAN_POINT('Ctrl Pts',(82.5638668802236,-0.649328821226295,
4.3869533685434));
#17836=CARTESIAN_POINT('Ctrl Pts',(82.5582936372118,-0.525722252229353,
4.40348087016432));
#17837=CARTESIAN_POINT('Ctrl Pts',(82.5527203942,-0.401580620582193,4.41477315444099));
#17838=CARTESIAN_POINT('Ctrl Pts',(82.5471490536151,-0.277481364689749,
4.42606158409562));
#17839=CARTESIAN_POINT('Ctrl Pts',(82.5415777130302,-0.152847824230017,
4.43211830966476));
#17840=CARTESIAN_POINT('Ctrl Pts',(82.5360063724452,-0.0281660667782649,
4.43291051936335));
#17841=CARTESIAN_POINT('Ctrl Pts',(82.5304355573441,0.09650393080331,4.43370265434144));
#17842=CARTESIAN_POINT('Ctrl Pts',(82.524864742243,0.2212217189773,4.42923125828579));
#17843=CARTESIAN_POINT('Ctrl Pts',(82.5192939271418,0.345500417941909,4.41951563649253));
#17844=CARTESIAN_POINT('Ctrl Pts',(82.513722261215,0.469798097883816,4.40979853084083));
#17845=CARTESIAN_POINT('Ctrl Pts',(82.5081505952881,0.593656139356998,4.39483564139945));
#17846=CARTESIAN_POINT('Ctrl Pts',(82.5025789293612,0.716592740410878,4.37469814323119));
#17847=CARTESIAN_POINT('Ctrl Pts',(82.4970019744931,0.839646039857502,4.35454152940779));
#17848=CARTESIAN_POINT('Ctrl Pts',(82.491425019625,0.961775740501727,4.32920056909857));
#17849=CARTESIAN_POINT('Ctrl Pts',(82.4858480647569,1.08251016603548,4.29879759240068));
#17850=CARTESIAN_POINT('Ctrl Pts',(82.4802681803071,1.20330801352119,4.26837864497927));
#17851=CARTESIAN_POINT('Ctrl Pts',(82.4746882958573,1.32270872795416,4.23289250833582));
#17852=CARTESIAN_POINT('Ctrl Pts',(82.4691084114075,1.44025740494804,4.19251089533376));
#17853=CARTESIAN_POINT('Ctrl Pts',(82.4635205574568,1.55797397149176,4.15207160706898));
#17854=CARTESIAN_POINT('Ctrl Pts',(82.457932703506,1.67383283321428,4.10672303810115));
#17855=CARTESIAN_POINT('Ctrl Pts',(82.4523448495553,1.78740045057869,4.05668443797039));
#17856=CARTESIAN_POINT('Ctrl Pts',(82.4492891972928,1.84950356744689,4.02932141756052));
#17857=CARTESIAN_POINT('Ctrl Pts',(82.4462335450304,1.91092196963203,4.00055672895153));
#17858=CARTESIAN_POINT('Ctrl Pts',(82.4431778927679,1.9715882987731,3.9704317876197));
#17859=CARTESIAN_POINT('',(82.4430005297901,-1.97158113240048,3.97043534620102));
#17860=CARTESIAN_POINT('Origin',(82.4430005297901,0.,0.));
#17861=CARTESIAN_POINT('',(82.6638081402658,-4.43299984791433,0.00116120262292478));
#17862=CARTESIAN_POINT('Ctrl Pts',(82.4430005297901,-1.97158113240048,3.97043534620102));
#17863=CARTESIAN_POINT('Ctrl Pts',(82.4494638984827,-2.10057436133302,3.90638176159495));
#17864=CARTESIAN_POINT('Ctrl Pts',(82.4559272671753,-2.22637526730531,3.83607233314734));
#17865=CARTESIAN_POINT('Ctrl Pts',(82.4623906358678,-2.34842827658618,3.75983691531035));
#17866=CARTESIAN_POINT('Ctrl Pts',(82.4689240795752,-2.47180456894732,3.68277496284602));
#17867=CARTESIAN_POINT('Ctrl Pts',(82.4754575232826,-2.59135104040891,3.59965787543973));
#17868=CARTESIAN_POINT('Ctrl Pts',(82.4819909669899,-2.7065244273022,3.51087090682875));
#17869=CARTESIAN_POINT('Ctrl Pts',(82.4884591884542,-2.82054805811389,3.42297028323097));
#17870=CARTESIAN_POINT('Ctrl Pts',(82.4949274099185,-2.93028537609616,3.32951260882839));
#17871=CARTESIAN_POINT('Ctrl Pts',(82.5013956313828,-3.03524125502932,3.23091310990687));
#17872=CARTESIAN_POINT('Ctrl Pts',(82.5079616862117,-3.14178461621387,3.1308222704704));
#17873=CARTESIAN_POINT('Ctrl Pts',(82.5145277410406,-3.24340054762542,3.02543291106605));
#17874=CARTESIAN_POINT('Ctrl Pts',(82.5210937958695,-3.33960719737278,2.9152208779535));
#17875=CARTESIAN_POINT('Ctrl Pts',(82.5276598506984,-3.43581384712013,2.80500884484095));
#17876=CARTESIAN_POINT('Ctrl Pts',(82.5342259055274,-3.52661104005606,2.68997426850115));
#17877=CARTESIAN_POINT('Ctrl Pts',(82.5407919603563,-3.61155585484342,2.57063286125153));
#17878=CARTESIAN_POINT('Ctrl Pts',(82.5465587614237,-3.68616075251107,2.46581830020199));
#17879=CARTESIAN_POINT('Ctrl Pts',(82.5523255624912,-3.7562202228349,2.35772393653131));
#17880=CARTESIAN_POINT('Ctrl Pts',(82.5580923635586,-3.82144896825721,2.24677920210373));
#17881=CARTESIAN_POINT('Ctrl Pts',(82.5638586415672,-3.88667179731824,2.13584453055759));
#17882=CARTESIAN_POINT('Ctrl Pts',(82.5696249195757,-3.94706457906038,2.02206033693403));
#17883=CARTESIAN_POINT('Ctrl Pts',(82.5753911975842,-4.0023868138301,1.90588268067027));
#17884=CARTESIAN_POINT('Ctrl Pts',(82.5811602666648,-4.05773582641746,1.78964879052325));
#17885=CARTESIAN_POINT('Ctrl Pts',(82.5869293357453,-4.10800922004284,1.67101947165996));
#17886=CARTESIAN_POINT('Ctrl Pts',(82.5926984048258,-4.15301362796875,1.55047309099703));
#17887=CARTESIAN_POINT('Ctrl Pts',(82.5984688920149,-4.19802909853494,1.42989707854227));
#17888=CARTESIAN_POINT('Ctrl Pts',(82.604239379204,-4.23777287589598,1.307403430887));
#17889=CARTESIAN_POINT('Ctrl Pts',(82.6100098663931,-4.27210103753376,1.18348710390227));
#17890=CARTESIAN_POINT('Ctrl Pts',(82.6157858342638,-4.30646180330307,1.05945308392053));
#17891=CARTESIAN_POINT('Ctrl Pts',(82.6215618021345,-4.33539658350209,0.933994060690117));
#17892=CARTESIAN_POINT('Ctrl Pts',(82.6273377700051,-4.35881219075801,0.807617041486446));
#17893=CARTESIAN_POINT('Ctrl Pts',(82.6310863103109,-4.37400866510629,0.725599730999895));
#17894=CARTESIAN_POINT('Ctrl Pts',(82.6348348506167,-4.3868815826507,0.643195975333012));
#17895=CARTESIAN_POINT('Ctrl Pts',(82.6385833909225,-4.39741715450987,0.560545599592328));
#17896=CARTESIAN_POINT('Ctrl Pts',(82.6469916406956,-4.42104921191562,0.375154768395029));
#17897=CARTESIAN_POINT('Ctrl Pts',(82.6553998904686,-4.43295082854589,0.188297149485439));
#17898=CARTESIAN_POINT('Ctrl Pts',(82.6638081402417,-4.43299984791419,0.00116120315987237));
#17899=CARTESIAN_POINT('',(83.91380814028,-4.43299997457298,-0.000474800938941028));
#17900=CARTESIAN_POINT('Ctrl Pts',(82.6638081402658,-4.43299984791433,0.00116120262292773));
#17901=CARTESIAN_POINT('Ctrl Pts',(82.66952634519,-4.43303318453861,-0.126104485083569));
#17902=CARTESIAN_POINT('Ctrl Pts',(82.6752445501142,-4.42758176932235,-0.253494044019376));
#17903=CARTESIAN_POINT('Ctrl Pts',(82.6809627550384,-4.41663987684345,-0.380501246090336));
#17904=CARTESIAN_POINT('Ctrl Pts',(82.6866768648111,-4.40570582051381,-0.507417490642293));
#17905=CARTESIAN_POINT('Ctrl Pts',(82.6923909745838,-4.38928914747985,-0.633951529973464));
#17906=CARTESIAN_POINT('Ctrl Pts',(82.6981050843566,-4.36743618383699,-0.759598696754644));
#17907=CARTESIAN_POINT('Ctrl Pts',(82.7038171800945,-4.34559092264133,-0.885201577063616));
#17908=CARTESIAN_POINT('Ctrl Pts',(82.7095292758324,-4.31831324733326,-1.00991781644859));
#17909=CARTESIAN_POINT('Ctrl Pts',(82.7152413715703,-4.28570112928413,-1.13324967701418));
#17910=CARTESIAN_POINT('Ctrl Pts',(82.7209525265382,-4.25309438238174,-1.25656122508364));
#17911=CARTESIAN_POINT('Ctrl Pts',(82.7266636815061,-4.21515504130049,-1.37848846485092));
#17912=CARTESIAN_POINT('Ctrl Pts',(82.732374836474,-4.17203169315451,-1.49854614587417));
#17913=CARTESIAN_POINT('Ctrl Pts',(82.7380863123118,-4.12890592220823,-1.61861057210152));
#17914=CARTESIAN_POINT('Ctrl Pts',(82.7437977881496,-4.08059569829891,-1.73680485750822));
#17915=CARTESIAN_POINT('Ctrl Pts',(82.7495092639875,-4.02729859725175,-1.85266160120355));
#17916=CARTESIAN_POINT('Ctrl Pts',(82.755222322258,-3.97398672960537,-1.96855044439523));
#17917=CARTESIAN_POINT('Ctrl Pts',(82.7609353805286,-3.91568540085796,-2.08210009715756));
#17918=CARTESIAN_POINT('Ctrl Pts',(82.7666484387991,-3.85263896726242,-2.19286615823473));
#17919=CARTESIAN_POINT('Ctrl Pts',(82.7723680894829,-3.78951978311419,-2.30376003450624));
#17920=CARTESIAN_POINT('Ctrl Pts',(82.7780877401667,-3.72164475296699,-2.41186355794363));
#17921=CARTESIAN_POINT('Ctrl Pts',(82.7838073908506,-3.64930283253258,-2.5167593918509));
#17922=CARTESIAN_POINT('Ctrl Pts',(82.7895303907495,-3.57691855135525,-2.62171664886426));
#17923=CARTESIAN_POINT('Ctrl Pts',(82.7952533906484,-3.50006240656649,-2.72346215752109));
#17924=CARTESIAN_POINT('Ctrl Pts',(82.8009763905473,-3.41906405993374,-2.82161123368713));
#17925=CARTESIAN_POINT('Ctrl Pts',(82.8067090419939,-3.33792911371723,-2.91992583326824));
#17926=CARTESIAN_POINT('Ctrl Pts',(82.8124416934405,-3.2526382714049,-3.01463158537872));
#17927=CARTESIAN_POINT('Ctrl Pts',(82.8181743448871,-3.16355907605327,-3.10537968247378));
#17928=CARTESIAN_POINT('Ctrl Pts',(82.8235049806097,-3.08072676969314,-3.18976385490041));
#17929=CARTESIAN_POINT('Ctrl Pts',(82.8288356163323,-2.99461937718249,-3.27072621832306));
#17930=CARTESIAN_POINT('Ctrl Pts',(82.8341662520549,-2.90555695574893,-3.34801848514894));
#17931=CARTESIAN_POINT('Ctrl Pts',(82.839824058202,-2.8110282838068,-3.43005460337752));
#17932=CARTESIAN_POINT('Ctrl Pts',(82.8454818643491,-2.71284674301988,-3.50823656309188));
#17933=CARTESIAN_POINT('Ctrl Pts',(82.8511396704962,-2.61136200335535,-3.5822168398119));
#17934=CARTESIAN_POINT('Ctrl Pts',(82.8567897948495,-2.51001505293713,-3.65609667102054));
#17935=CARTESIAN_POINT('Ctrl Pts',(82.8624399192028,-2.40537414749344,-3.72578592549306));
#17936=CARTESIAN_POINT('Ctrl Pts',(82.8680900435561,-2.29782447308528,-3.79097503168912));
#17937=CARTESIAN_POINT('Ctrl Pts',(82.8737339750989,-2.19039267834028,-3.85609268746079));
#17938=CARTESIAN_POINT('Ctrl Pts',(82.8793779066417,-2.08005880157589,-3.91671979497149));
#17939=CARTESIAN_POINT('Ctrl Pts',(82.8850218381844,-1.9672391924985,-3.97258844577409));
#17940=CARTESIAN_POINT('Ctrl Pts',(82.8906610595198,-1.85451373831238,-4.02841047075708));
#17941=CARTESIAN_POINT('Ctrl Pts',(82.8963002808551,-1.73930704246086,-4.07948175888407));
#17942=CARTESIAN_POINT('Ctrl Pts',(82.9019395021905,-1.62206187633748,-4.1255792647012));
#17943=CARTESIAN_POINT('Ctrl Pts',(82.9075758918359,-1.5048755839357,-4.17165362302481));
#17944=CARTESIAN_POINT('Ctrl Pts',(82.9132122814814,-1.38565323531322,-4.2127590163154));
#17945=CARTESIAN_POINT('Ctrl Pts',(82.9188486711269,-1.26485905207188,-4.24871987525558));
#17946=CARTESIAN_POINT('Ctrl Pts',(82.9244837033836,-1.14409395920267,-4.28467207388829));
#17947=CARTESIAN_POINT('Ctrl Pts',(82.9301187356403,-1.02175817495687,-4.31548208507233));
#17948=CARTESIAN_POINT('Ctrl Pts',(82.935753767897,-0.898332042706435,-4.34102390468503));
#17949=CARTESIAN_POINT('Ctrl Pts',(82.9413887767732,-0.774906422566319,
-4.36656561832156));
#17950=CARTESIAN_POINT('Ctrl Pts',(82.9470237856495,-0.650390862901795,
-4.38683910150858));
#17951=CARTESIAN_POINT('Ctrl Pts',(82.9526587945257,-0.525276262369073,
-4.40176939970639));
#17952=CARTESIAN_POINT('Ctrl Pts',(82.9582951137571,-0.400132567904806,
-4.41670316976977));
#17953=CARTESIAN_POINT('Ctrl Pts',(82.9639314329885,-0.274389960519799,
-4.42629123631845));
#17954=CARTESIAN_POINT('Ctrl Pts',(82.9695677522199,-0.1485441952278,-4.43051053740583));
#17955=CARTESIAN_POINT('Ctrl Pts',(82.9752099321354,-0.0225675746294041,
-4.43473422575198));
#17956=CARTESIAN_POINT('Ctrl Pts',(82.980852112051,0.103512009964471,-4.43357798956721));
#17957=CARTESIAN_POINT('Ctrl Pts',(82.9864942919665,0.22919885795583,-4.4270709146694));
#17958=CARTESIAN_POINT('Ctrl Pts',(82.9921397286903,0.35495825556051,-4.42056008372411));
#17959=CARTESIAN_POINT('Ctrl Pts',(82.9977851654142,0.480324059807185,-4.40869230250852));
#17960=CARTESIAN_POINT('Ctrl Pts',(83.003430602138,0.604807415447957,-4.39154835908921));
#17961=CARTESIAN_POINT('Ctrl Pts',(83.0090844057058,0.729475262183915,-4.37437900741447));
#17962=CARTESIAN_POINT('Ctrl Pts',(83.0147382092735,0.853257648687448,-4.35191795361543));
#17963=CARTESIAN_POINT('Ctrl Pts',(83.0203920128412,0.975677264387951,-4.32429680708395));
#17964=CARTESIAN_POINT('Ctrl Pts',(83.0235110462899,1.0432124858663,-4.3090590509628));
#17965=CARTESIAN_POINT('Ctrl Pts',(83.0266300797386,1.11033323896754,-4.29225175525319));
#17966=CARTESIAN_POINT('Ctrl Pts',(83.0297491131872,1.1769618225775,-4.27390335269705));
#17967=CARTESIAN_POINT('Ctrl Pts',(83.0354745794598,1.29926884958629,-4.24022203387839));
#17968=CARTESIAN_POINT('Ctrl Pts',(83.0412000457323,1.42030983933144,-4.20123662023261));
#17969=CARTESIAN_POINT('Ctrl Pts',(83.0469255120049,1.53959327565377,-4.15705924248882));
#17970=CARTESIAN_POINT('Ctrl Pts',(83.0526441242172,1.65873391559655,-4.11293475029054));
#17971=CARTESIAN_POINT('Ctrl Pts',(83.0583627364296,1.77612081943256,-4.06363079762116));
#17972=CARTESIAN_POINT('Ctrl Pts',(83.0640813486419,1.89127573333345,-4.00930980350783));
#17973=CARTESIAN_POINT('Ctrl Pts',(83.0697945150905,2.00632098663147,-3.95504053860658));
#17974=CARTESIAN_POINT('Ctrl Pts',(83.075507681539,2.11913812300309,-3.89576390865514));
#17975=CARTESIAN_POINT('Ctrl Pts',(83.0812208479875,2.22926746805393,-3.83169095255299));
#17976=CARTESIAN_POINT('Ctrl Pts',(83.0872254782513,2.34501518942459,-3.76434924025204));
#17977=CARTESIAN_POINT('Ctrl Pts',(83.0932301085152,2.45779323152163,-3.69170908293691));
#17978=CARTESIAN_POINT('Ctrl Pts',(83.099234738779,2.56709511962265,-3.6140713394743));
#17979=CARTESIAN_POINT('Ctrl Pts',(83.1049417078618,2.67097870090478,-3.54028224970026));
#17980=CARTESIAN_POINT('Ctrl Pts',(83.1106486769446,2.77172211169826,-3.4619793890988));
#17981=CARTESIAN_POINT('Ctrl Pts',(83.1163556460274,2.86891935081674,-3.37946604636136));
#17982=CARTESIAN_POINT('Ctrl Pts',(83.1220617784329,2.96610234021447,-3.29696480059398));
#17983=CARTESIAN_POINT('Ctrl Pts',(83.1277679108385,3.05973988983671,-3.21025455741205));
#17984=CARTESIAN_POINT('Ctrl Pts',(83.1334740432441,3.14945917911302,-3.11967881024646));
#17985=CARTESIAN_POINT('Ctrl Pts',(83.1391806042983,3.23918520816516,-3.02909625896731));
#17986=CARTESIAN_POINT('Ctrl Pts',(83.1448871653525,3.32499211215973,-2.93464790798709));
#17987=CARTESIAN_POINT('Ctrl Pts',(83.1505937264068,3.40654438100098,-2.83671365849122));
#17988=CARTESIAN_POINT('Ctrl Pts',(83.1563019814222,3.48812085818393,-2.73875033775294));
#17989=CARTESIAN_POINT('Ctrl Pts',(83.1620102364376,3.56543993364672,-2.63729936448726));
#17990=CARTESIAN_POINT('Ctrl Pts',(83.1677184914531,3.63820709300359,-2.53277281816162));
#17991=CARTESIAN_POINT('Ctrl Pts',(83.173432742932,3.71105069351727,-2.42813646776792));
#17992=CARTESIAN_POINT('Ctrl Pts',(83.179146994411,3.77933260400223,-2.32041841957391));
#17993=CARTESIAN_POINT('Ctrl Pts',(83.1848612458899,3.84280211367408,-2.21005902978677));
#17994=CARTESIAN_POINT('Ctrl Pts',(83.1905789779027,3.90631028243734,-2.09963242042033));
#17995=CARTESIAN_POINT('Ctrl Pts',(83.1962967099154,3.96500002782284,-1.98656161562392));
#17996=CARTESIAN_POINT('Ctrl Pts',(83.2020144419281,4.01866767330937,-1.87130946972921));
#17997=CARTESIAN_POINT('Ctrl Pts',(83.2077400921353,4.07240964037243,-1.75589771703413));
#17998=CARTESIAN_POINT('Ctrl Pts',(83.2134657423425,4.12111546961183,-1.63829895735629));
#17999=CARTESIAN_POINT('Ctrl Pts',(83.2191913925498,4.16463033859644,-1.51899412205647));
#18000=CARTESIAN_POINT('Ctrl Pts',(83.2212382531397,4.18018645312964,-1.47634388029783));
#18001=CARTESIAN_POINT('Ctrl Pts',(83.2232851137297,4.1950796382993,-1.4334757262206));
#18002=CARTESIAN_POINT('Ctrl Pts',(83.2253319743196,4.20930439677606,-1.39041198760718));
#18003=CARTESIAN_POINT('Ctrl Pts',(83.2310481942998,4.24902954905002,-1.27014888600867));
#18004=CARTESIAN_POINT('Ctrl Pts',(83.2367644142801,4.28365637951515,-1.14800097222107));
#18005=CARTESIAN_POINT('Ctrl Pts',(83.2424806342603,4.31300545590474,-1.02443786406786));
#18006=CARTESIAN_POINT('Ctrl Pts',(83.2481900066406,4.3423193743169,-0.901022775188253));
#18007=CARTESIAN_POINT('Ctrl Pts',(83.253899379021,4.36636802621654,-0.776196249202119));
#18008=CARTESIAN_POINT('Ctrl Pts',(83.2596087514013,4.38502115367675,-0.650444833792572));
#18009=CARTESIAN_POINT('Ctrl Pts',(83.2653126965135,4.40365654967427,-0.524812956328336));
#18010=CARTESIAN_POINT('Ctrl Pts',(83.2710166416257,4.41690656945924,-0.398258330848222));
#18011=CARTESIAN_POINT('Ctrl Pts',(83.276720586738,4.42469170305703,-0.271279068300975));
#18012=CARTESIAN_POINT('Ctrl Pts',(83.2824205200588,4.43247136108805,-0.144389114873869));
#18013=CARTESIAN_POINT('Ctrl Pts',(83.2881204533796,4.43479375906451,-0.0170755150908258));
#18014=CARTESIAN_POINT('Ctrl Pts',(83.2938203867003,4.43163111181196,0.110157563609088));
#18015=CARTESIAN_POINT('Ctrl Pts',(83.2995183245726,4.42846957174779,0.23734610019774));
#18016=CARTESIAN_POINT('Ctrl Pts',(83.3052162624448,4.41982681393095,0.364453774179399));
#18017=CARTESIAN_POINT('Ctrl Pts',(83.310914200317,4.4057271570083,0.490975781479656));
#18018=CARTESIAN_POINT('Ctrl Pts',(83.3166112906413,4.39162959735927,0.617478969083135));
#18019=CARTESIAN_POINT('Ctrl Pts',(83.3223083809656,4.37207679727301,0.743396267566183));
#18020=CARTESIAN_POINT('Ctrl Pts',(83.32800547129,4.34714496198324,0.868227896064));
#18021=CARTESIAN_POINT('Ctrl Pts',(83.3337029902522,4.32221125087115,0.993068916648394));
#18022=CARTESIAN_POINT('Ctrl Pts',(83.3394005092144,4.29189777752478,1.11682371416384));
#18023=CARTESIAN_POINT('Ctrl Pts',(83.3450980281766,4.25633179186417,1.23900309828763));
#18024=CARTESIAN_POINT('Ctrl Pts',(83.3507972519518,4.22075516414081,1.36121904095599));
#18025=CARTESIAN_POINT('Ctrl Pts',(83.3564964757269,4.17992300858298,1.48185825013476));
#18026=CARTESIAN_POINT('Ctrl Pts',(83.3621956995021,4.13401216616899,1.60044756551621));
#18027=CARTESIAN_POINT('Ctrl Pts',(83.3679010547031,4.08805193125264,1.71916446346274));
#18028=CARTESIAN_POINT('Ctrl Pts',(83.3736064099041,4.03700224421237,1.8358266926203));
#18029=CARTESIAN_POINT('Ctrl Pts',(83.3793117651051,3.98108787463452,1.94998162412829));
#18030=CARTESIAN_POINT('Ctrl Pts',(83.3850206254083,3.92513915389531,2.06420668706227));
#18031=CARTESIAN_POINT('Ctrl Pts',(83.3907294857114,3.86431998684683,2.17592103443391));
#18032=CARTESIAN_POINT('Ctrl Pts',(83.3964383460145,3.79890005935971,2.28469852256196));
#18033=CARTESIAN_POINT('Ctrl Pts',(83.4021554039637,3.73338619203564,2.39363220987718));
#18034=CARTESIAN_POINT('Ctrl Pts',(83.4078724619128,3.66325859195248,2.49962028578032));
#18035=CARTESIAN_POINT('Ctrl Pts',(83.4135895198619,3.58882923436517,2.60226703598342));
#18036=CARTESIAN_POINT('Ctrl Pts',(83.4160312917253,3.55704024205838,2.64610775768649));
#18037=CARTESIAN_POINT('Ctrl Pts',(83.4184730635886,3.52446702502304,2.68933939325408));
#18038=CARTESIAN_POINT('Ctrl Pts',(83.4209148354519,3.49113598849276,2.7319331085974));
#18039=CARTESIAN_POINT('Ctrl Pts',(83.4266198983286,3.41325989285673,2.83145093326986));
#18040=CARTESIAN_POINT('Ctrl Pts',(83.4323249612053,3.33100226602438,2.92779324457393));
#18041=CARTESIAN_POINT('Ctrl Pts',(83.438030024082,3.24465148343176,3.0205505708503));
#18042=CARTESIAN_POINT('Ctrl Pts',(83.4437280321523,3.15840748109027,3.11319319462721));
#18043=CARTESIAN_POINT('Ctrl Pts',(83.4494260402227,3.06808066251407,3.2022593622306));
#18044=CARTESIAN_POINT('Ctrl Pts',(83.455124048293,2.97400091869034,3.28737091543212));
#18045=CARTESIAN_POINT('Ctrl Pts',(83.4608164367597,2.88001396007733,3.37239852821163));
#18046=CARTESIAN_POINT('Ctrl Pts',(83.4665088252263,2.78228173585553,3.45347902008985));
#18047=CARTESIAN_POINT('Ctrl Pts',(83.4722012136929,2.6811720661167,3.53026986955325));
#18048=CARTESIAN_POINT('Ctrl Pts',(83.477889412659,2.58013681136487,3.60700420226529));
#18049=CARTESIAN_POINT('Ctrl Pts',(83.4835776116252,2.47572937575758,3.67945493462437));
#18050=CARTESIAN_POINT('Ctrl Pts',(83.4892658105913,2.3683514681524,3.74731908479921));
#18051=CARTESIAN_POINT('Ctrl Pts',(83.4949517923112,2.26101541619517,3.81515678169291));
#18052=CARTESIAN_POINT('Ctrl Pts',(83.5006377740312,2.15071153226204,3.87841123787996));
#18053=CARTESIAN_POINT('Ctrl Pts',(83.5063237557511,2.03787109472943,3.93682237359857));
#18054=CARTESIAN_POINT('Ctrl Pts',(83.5120087552445,1.92505014985086,3.99522341906863));
#18055=CARTESIAN_POINT('Ctrl Pts',(83.5176937547379,1.80969387814875,4.04878262428713));
#18056=CARTESIAN_POINT('Ctrl Pts',(83.5233787542313,1.69225830281663,4.09728578897642));
#18057=CARTESIAN_POINT('Ctrl Pts',(83.5290640603275,1.57481639396105,4.14579156953345));
#18058=CARTESIAN_POINT('Ctrl Pts',(83.5347493664237,1.45529532835186,4.1892406145228));
#18059=CARTESIAN_POINT('Ctrl Pts',(83.5404346725199,1.33417075941755,4.22746701757863));
#18060=CARTESIAN_POINT('Ctrl Pts',(83.5461215739581,1.21301220196906,4.26570414726618));
#18061=CARTESIAN_POINT('Ctrl Pts',(83.5518084753962,1.09024962761543,4.29871559940692));
#18062=CARTESIAN_POINT('Ctrl Pts',(83.5574953768344,0.966372968624036,4.32638559140453));
#18063=CARTESIAN_POINT('Ctrl Pts',(83.5631883104399,0.842364912113645,4.35408493330816));
#18064=CARTESIAN_POINT('Ctrl Pts',(83.5688812440455,0.717240802444245,4.37643141553077));
#18065=CARTESIAN_POINT('Ctrl Pts',(83.574574177651,0.591500159325903,4.39336050894044));
#18066=CARTESIAN_POINT('Ctrl Pts',(83.5802705426044,0.465683727534138,4.41029980615933));
#18067=CARTESIAN_POINT('Ctrl Pts',(83.5859669075578,0.33925041991595,4.42181517388166));
#18068=CARTESIAN_POINT('Ctrl Pts',(83.5916632725112,0.212702699705993,4.42789414524984));
#18069=CARTESIAN_POINT('Ctrl Pts',(83.5973678301151,0.0859729754876457,
4.43398185954245));
#18070=CARTESIAN_POINT('Ctrl Pts',(83.6030723877191,-0.0408710906136837,
4.43461756341891));
#18071=CARTESIAN_POINT('Ctrl Pts',(83.6087769453231,-0.167328842256537,
4.4298408615377));
#18072=CARTESIAN_POINT('Ctrl Pts',(83.6113505290768,-0.224379649305718,
4.4276858754351));
#18073=CARTESIAN_POINT('Ctrl Pts',(83.6139241128306,-0.281351919387955,
4.42442999190873));
#18074=CARTESIAN_POINT('Ctrl Pts',(83.6164976965844,-0.338200276830494,
4.420080267682));
#18075=CARTESIAN_POINT('Ctrl Pts',(83.6222109841139,-0.464402119368476,
4.4104239955109));
#18076=CARTESIAN_POINT('Ctrl Pts',(83.6279242716434,-0.590383458300955,
4.39534367157767));
#18077=CARTESIAN_POINT('Ctrl Pts',(83.6336375591729,-0.715642314386609,
4.37485372073849));
#18078=CARTESIAN_POINT('Ctrl Pts',(83.6393439004404,-0.840748879722081,
4.3543886817505));
#18079=CARTESIAN_POINT('Ctrl Pts',(83.6450502417078,-0.965134319568548,
4.32852716489467));
#18080=CARTESIAN_POINT('Ctrl Pts',(83.6507565829752,-1.08829986702525,4.29733549998517));
#18081=CARTESIAN_POINT('Ctrl Pts',(83.6564574025489,-1.21134623436123,4.26617401743159));
#18082=CARTESIAN_POINT('Ctrl Pts',(83.6621582221225,-1.3331746737723,4.22969274740485));
#18083=CARTESIAN_POINT('Ctrl Pts',(83.6678590416961,-1.45329519728146,4.18800932061506));
#18084=CARTESIAN_POINT('Ctrl Pts',(83.6735557591892,-1.5733292868919,4.14635588754312));
#18085=CARTESIAN_POINT('Ctrl Pts',(83.6792524766823,-1.6916575311311,4.09950787836922));
#18086=CARTESIAN_POINT('Ctrl Pts',(83.6849491941753,-1.80780418804368,4.04763301420617));
#18087=CARTESIAN_POINT('Ctrl Pts',(83.6906437933859,-1.92390765667619,3.9957774393298));
#18088=CARTESIAN_POINT('Ctrl Pts',(83.6963383925965,-2.03783078739654,3.93889888846478));
#18089=CARTESIAN_POINT('Ctrl Pts',(83.7020329918071,-2.14911725028655,3.87721343809195));
#18090=CARTESIAN_POINT('Ctrl Pts',(83.7077266679151,-2.26038567348426,3.81553798701746));
#18091=CARTESIAN_POINT('Ctrl Pts',(83.7134203440232,-2.36901793033941,3.74905737964579));
#18092=CARTESIAN_POINT('Ctrl Pts',(83.7191140201312,-2.47458224161525,3.67803367704572));
#18093=CARTESIAN_POINT('Ctrl Pts',(83.7248080528019,-2.58015316378562,3.60700552663368));
#18094=CARTESIAN_POINT('Ctrl Pts',(83.7305020854726,-2.68265542734863,3.53143393775299));
#18095=CARTESIAN_POINT('Ctrl Pts',(83.7361961181433,-2.78168662765078,3.45162403884734));
#18096=CARTESIAN_POINT('Ctrl Pts',(83.7418917869822,-2.88074628435806,3.37179120673671));
#18097=CARTESIAN_POINT('Ctrl Pts',(83.7475874558211,-2.97633258319261,3.28771789193997));
#18098=CARTESIAN_POINT('Ctrl Pts',(83.75328312466,-3.06807696429394,3.19974885595243));
#18099=CARTESIAN_POINT('Ctrl Pts',(83.7589848401618,-3.15991874349887,3.11168642986101));
#18100=CARTESIAN_POINT('Ctrl Pts',(83.7646865556636,-3.24791017329906,3.0197203012298));
#18101=CARTESIAN_POINT('Ctrl Pts',(83.7703882711653,-3.33172006525766,2.92423159253153));
#18102=CARTESIAN_POINT('Ctrl Pts',(83.7760934383249,-3.41558069336201,2.8286850776611));
#18103=CARTESIAN_POINT('Ctrl Pts',(83.7817986054845,-3.49525449117515,2.72961204476918));
#18104=CARTESIAN_POINT('Ctrl Pts',(83.7875037726441,-3.57045198052145,2.6274249094485));
#18105=CARTESIAN_POINT('Ctrl Pts',(83.7932170873008,-3.6457568587145,2.52509184161452));
#18106=CARTESIAN_POINT('Ctrl Pts',(83.7989304019574,-3.71657244207957,2.41963612160936));
#18107=CARTESIAN_POINT('Ctrl Pts',(83.804643716614,-3.78265359926121,2.31149751200303));
#18108=CARTESIAN_POINT('Ctrl Pts',(83.8071226636483,-3.81132551713363,2.26457730863935));
#18109=CARTESIAN_POINT('Ctrl Pts',(83.8096016106825,-3.83910672862993,2.21715231825351));
#18110=CARTESIAN_POINT('Ctrl Pts',(83.8120805577167,-3.8659800018218,2.16925969526793));
#18111=CARTESIAN_POINT('Ctrl Pts',(83.8180254810596,-3.93042653774616,2.05440529603959));
#18112=CARTESIAN_POINT('Ctrl Pts',(83.8239704044024,-3.98983198688334,1.93653249703956));
#18113=CARTESIAN_POINT('Ctrl Pts',(83.8299153277452,-4.04391631419735,1.81610292763614));
#18114=CARTESIAN_POINT('Ctrl Pts',(83.8358508814789,-4.09791540088159,1.69586316353951));
#18115=CARTESIAN_POINT('Ctrl Pts',(83.8417864352125,-4.14660992797813,1.57307497537607));
#18116=CARTESIAN_POINT('Ctrl Pts',(83.8477219889461,-4.18976514839525,1.44822546631817));
#18117=CARTESIAN_POINT('Ctrl Pts',(83.853645865327,-4.23283546708994,1.32362158080853));
#18118=CARTESIAN_POINT('Ctrl Pts',(83.8595697417078,-4.27038809194831,1.19696479106409));
#18119=CARTESIAN_POINT('Ctrl Pts',(83.8654936180886,-4.30223616830599,1.06876234594966));
#18120=CARTESIAN_POINT('Ctrl Pts',(83.8714105761186,-4.33404705007198,0.940709625344368));
#18121=CARTESIAN_POINT('Ctrl Pts',(83.8773275341486,-4.36016656697666,0.811115184524049));
#18122=CARTESIAN_POINT('Ctrl Pts',(83.8832444921787,-4.38045717906978,0.680502683562672));
#18123=CARTESIAN_POINT('Ctrl Pts',(83.8891531086527,-4.40071918604579,0.550074316321375));
#18124=CARTESIAN_POINT('Ctrl Pts',(83.8950617251268,-4.41516861656605,0.418631097111072));
#18125=CARTESIAN_POINT('Ctrl Pts',(83.9009703416008,-4.42371876807926,0.286707622750609));
#18126=CARTESIAN_POINT('Ctrl Pts',(83.9052496078144,-4.42991114401917,0.191163146459511));
#18127=CARTESIAN_POINT('Ctrl Pts',(83.9095288740281,-4.43301023979327,0.095367055746549));
#18128=CARTESIAN_POINT('Ctrl Pts',(83.9138081402417,-4.43299997457307,-0.000474800080565356));
#18129=CARTESIAN_POINT('',(85.1638081402016,-4.43299950255766,-0.00210007702333454));
#18130=CARTESIAN_POINT('Ctrl Pts',(83.91380814028,-4.43299997457298,-0.000474800938941129));
#18131=CARTESIAN_POINT('Ctrl Pts',(83.9198146375964,-4.43298556599779,-0.135001100795744));
#18132=CARTESIAN_POINT('Ctrl Pts',(83.9258211349128,-4.42684326063918,-0.269394591604568));
#18133=CARTESIAN_POINT('Ctrl Pts',(83.9318276322292,-4.4146348479927,-0.403098200056139));
#18134=CARTESIAN_POINT('Ctrl Pts',(83.9381472811142,-4.4017899439988,-0.543772509151691));
#18135=CARTESIAN_POINT('Ctrl Pts',(83.9444669299992,-4.38222954173958,-0.683682637169625));
#18136=CARTESIAN_POINT('Ctrl Pts',(83.9507865788842,-4.35608620402984,-0.822193397602375));
#18137=CARTESIAN_POINT('Ctrl Pts',(83.9568184974464,-4.33113315887183,-0.95439783524233));
#18138=CARTESIAN_POINT('Ctrl Pts',(83.9628504160087,-4.30018351207985,-1.08532723336189));
#18139=CARTESIAN_POINT('Ctrl Pts',(83.9688823345709,-4.26340353906825,-1.21444607252044));
#18140=CARTESIAN_POINT('Ctrl Pts',(83.9749228194931,-4.22657133218006,-1.34374828259957));
#18141=CARTESIAN_POINT('Ctrl Pts',(83.9809633044154,-4.18389237439995,-1.47123449090566));
#18142=CARTESIAN_POINT('Ctrl Pts',(83.9870037893376,-4.13558151938089,-1.59638795302246));
#18143=CARTESIAN_POINT('Ctrl Pts',(83.9930571147078,-4.08716796846467,-1.72180745777232));
#18144=CARTESIAN_POINT('Ctrl Pts',(83.9991104400779,-4.033098721031,-1.84488400437242));
#18145=CARTESIAN_POINT('Ctrl Pts',(84.0051637654481,-3.97363566494557,-1.96512305016062));
#18146=CARTESIAN_POINT('Ctrl Pts',(84.0059969832484,-3.96545079567714,-1.98167350914348));
#18147=CARTESIAN_POINT('Ctrl Pts',(84.0068302010488,-3.95716380076966,-1.99817025067915));
#18148=CARTESIAN_POINT('Ctrl Pts',(84.0076634188491,-3.94877542780791,-2.01461202734929));
#18149=CARTESIAN_POINT('Ctrl Pts',(84.0133739097053,-3.89128538489826,-2.12729638826019));
#18150=CARTESIAN_POINT('Ctrl Pts',(84.0190844005613,-3.82887916097553,-2.23769221763686));
#18151=CARTESIAN_POINT('Ctrl Pts',(84.0247948914174,-3.76176283356058,-2.34534206120179));
#18152=CARTESIAN_POINT('Ctrl Pts',(84.0304984050993,-3.6947285100087,-2.45286037636863));
#18153=CARTESIAN_POINT('Ctrl Pts',(84.0362019187812,-3.62299574155127,-2.55763904467317));
#18154=CARTESIAN_POINT('Ctrl Pts',(84.0419054324631,-3.54681729055957,-2.65924352164063));
#18155=CARTESIAN_POINT('Ctrl Pts',(84.0476033971757,-3.47071295385949,-2.76074914724346));
#18156=CARTESIAN_POINT('Ctrl Pts',(84.0533013618884,-3.39017177929827,-2.85908640886412));
#18157=CARTESIAN_POINT('Ctrl Pts',(84.0589993266011,-3.30549051446267,-2.95384858427058));
#18158=CARTESIAN_POINT('Ctrl Pts',(84.0646931655529,-3.22087056531951,-3.04854214463671));
#18159=CARTESIAN_POINT('Ctrl Pts',(84.0703870045047,-3.13211675741254,-3.13966547422476));
#18160=CARTESIAN_POINT('Ctrl Pts',(84.0760808434565,-3.03956660109192,-3.22684425988093));
#18161=CARTESIAN_POINT('Ctrl Pts',(84.0817725395899,-2.94705127508153,-3.3139902366876));
#18162=CARTESIAN_POINT('Ctrl Pts',(84.0874642357232,-2.85074273159858,-3.39719434791402));
#18163=CARTESIAN_POINT('Ctrl Pts',(84.0931559318566,-2.75101565081883,-3.47611879672572));
#18164=CARTESIAN_POINT('Ctrl Pts',(84.0988466905102,-2.65130499609671,-3.55503024588341));
#18165=CARTESIAN_POINT('Ctrl Pts',(84.1045374491637,-2.54817723703542,-3.62966318704529));
#18166=CARTESIAN_POINT('Ctrl Pts',(84.1102282078173,-2.44204005555012,-3.69972017416031));
#18167=CARTESIAN_POINT('Ctrl Pts',(84.1159193118143,-2.33589643313382,-3.76978141268103));
#18168=CARTESIAN_POINT('Ctrl Pts',(84.1216104158113,-2.22674335831257,-3.83526592490555));
#18169=CARTESIAN_POINT('Ctrl Pts',(84.1273015198083,-2.1150169611824,-3.89591994962817));
#18170=CARTESIAN_POINT('Ctrl Pts',(84.1329942519059,-2.00325860156997,-3.95659132614266));
#18171=CARTESIAN_POINT('Ctrl Pts',(84.1386869840035,-1.88892580592011,-4.01242927568396));
#18172=CARTESIAN_POINT('Ctrl Pts',(84.1443797161011,-1.77247825695833,-4.06322652932494));
#18173=CARTESIAN_POINT('Ctrl Pts',(84.1500784986159,-1.65590694382871,-4.11407777190669));
#18174=CARTESIAN_POINT('Ctrl Pts',(84.1557772811306,-1.53721675604236,-4.15987746213883));
#18175=CARTESIAN_POINT('Ctrl Pts',(84.1614760636454,-1.41688654766952,-4.20046682060853));
#18176=CARTESIAN_POINT('Ctrl Pts',(84.167178296002,-1.2964834956349,-4.24108075044348));
#18177=CARTESIAN_POINT('Ctrl Pts',(84.1728805283586,-1.17443882806854,-4.27647795407286));
#18178=CARTESIAN_POINT('Ctrl Pts',(84.1785827607152,-1.05124421479158,-4.3065501971842));
#18179=CARTESIAN_POINT('Ctrl Pts',(84.184293163262,-0.927873087587349,-4.33666552797276));
#18180=CARTESIAN_POINT('Ctrl Pts',(84.1900035658089,-0.803349115433806,
-4.36144058594429));
#18181=CARTESIAN_POINT('Ctrl Pts',(84.1957139683557,-0.678172125810452,
-4.38081859562499));
#18182=CARTESIAN_POINT('Ctrl Pts',(84.1982247388976,-0.623133852152641,
-4.38933878933599));
#18183=CARTESIAN_POINT('Ctrl Pts',(84.2007355094395,-0.567969378517666,
-4.39681629432521));
#18184=CARTESIAN_POINT('Ctrl Pts',(84.2032462799814,-0.512721254578061,
-4.40324947227657));
#18185=CARTESIAN_POINT('Ctrl Pts',(84.208957745036,-0.387043609430515,-4.41788357381866));
#18186=CARTESIAN_POINT('Ctrl Pts',(84.2146692100905,-0.26054526117373,-4.42715530760686));
#18187=CARTESIAN_POINT('Ctrl Pts',(84.2203806751451,-0.133721359890292,
-4.43098268986791));
#18188=CARTESIAN_POINT('Ctrl Pts',(84.2260851767589,-0.00705208280799532,
-4.4348054057694));
#18189=CARTESIAN_POINT('Ctrl Pts',(84.2317896783727,0.119941562127036,-4.43319696397356));
#18190=CARTESIAN_POINT('Ctrl Pts',(84.2374941799866,0.246757627535567,-4.42612693822184));
#18191=CARTESIAN_POINT('Ctrl Pts',(84.2431931450881,0.373450611428637,-4.41906377429382));
#18192=CARTESIAN_POINT('Ctrl Pts',(84.2488921101896,0.499965962500836,-4.40654959625833));
#18193=CARTESIAN_POINT('Ctrl Pts',(84.2545910752912,0.625800519172279,-4.38860600990835));
#18194=CARTESIAN_POINT('Ctrl Pts',(84.2602859258295,0.751544225271094,-4.37067537854577));
#18195=CARTESIAN_POINT('Ctrl Pts',(84.2659807763678,0.876607721485549,-4.34732319692061));
#18196=CARTESIAN_POINT('Ctrl Pts',(84.271675626906,1.00049223376467,-4.318622962262));
#18197=CARTESIAN_POINT('Ctrl Pts',(84.2773683475706,1.12433041324489,-4.28993346148913));
#18198=CARTESIAN_POINT('Ctrl Pts',(84.2830610682352,1.24699009734483,-4.25589997462425));
#18199=CARTESIAN_POINT('Ctrl Pts',(84.2887537888998,1.36798230660267,-4.21664717623161));
#18200=CARTESIAN_POINT('Ctrl Pts',(84.2944455798391,1.48895475562298,-4.17740078853786));
#18201=CARTESIAN_POINT('Ctrl Pts',(84.3001373707785,1.6082598919955,-4.13293690795331));
#18202=CARTESIAN_POINT('Ctrl Pts',(84.3058291617178,1.72542403151994,-4.08343004243411));
#18203=CARTESIAN_POINT('Ctrl Pts',(84.3115213046565,1.84259541686544,-4.03392011524528));
#18204=CARTESIAN_POINT('Ctrl Pts',(84.3172134475951,1.95762517436972,-3.97936673818128));
#18205=CARTESIAN_POINT('Ctrl Pts',(84.3229055905338,2.07006021194999,-3.91999231107684));
#18206=CARTESIAN_POINT('Ctrl Pts',(84.3285993671343,2.18252751871783,-3.86060084333661));
#18207=CARTESIAN_POINT('Ctrl Pts',(84.3342931437348,2.2923982713242,-3.79638575927441));
#18208=CARTESIAN_POINT('Ctrl Pts',(84.3399869203353,2.39924501807703,-3.72761483300415));
#18209=CARTESIAN_POINT('Ctrl Pts',(84.3456867501181,2.50620535601741,-3.6587707948103));
#18210=CARTESIAN_POINT('Ctrl Pts',(84.351386579901,2.61013493331779,-3.58536146017421));
#18211=CARTESIAN_POINT('Ctrl Pts',(84.3570864096839,2.71063602804441,-3.50769743898582));
#18212=CARTESIAN_POINT('Ctrl Pts',(84.3627896923141,2.81119800440306,-3.42998637042571));
#18213=CARTESIAN_POINT('Ctrl Pts',(84.3684929749443,2.90832705621915,-3.34801573778199));
#18214=CARTESIAN_POINT('Ctrl Pts',(84.3741962575746,3.00166042348645,-3.26213483811984));
#18215=CARTESIAN_POINT('Ctrl Pts',(84.3799077059024,3.09512742117307,-3.17613097813847));
#18216=CARTESIAN_POINT('Ctrl Pts',(84.3856191542302,3.18478760174866,-3.08620595416674));
#18217=CARTESIAN_POINT('Ctrl Pts',(84.391330602558,3.27031650948386,-2.99274438063082));
#18218=CARTESIAN_POINT('Ctrl Pts',(84.3938301154099,3.30774670088692,-2.95184260041503));
#18219=CARTESIAN_POINT('Ctrl Pts',(84.3963296282619,3.3443862002125,-2.91026390191573));
#18220=CARTESIAN_POINT('Ctrl Pts',(84.3988291411138,3.38021038982991,-2.86804231497478));
#18221=CARTESIAN_POINT('Ctrl Pts',(84.4045403172651,3.46206564303368,-2.77156954820392));
#18222=CARTESIAN_POINT('Ctrl Pts',(84.4102514934165,3.5399137973655,-2.67144091763106));
#18223=CARTESIAN_POINT('Ctrl Pts',(84.4159626695678,3.61341209461349,-2.56802298169252));
#18224=CARTESIAN_POINT('Ctrl Pts',(84.4216668798357,3.6868207464796,-2.46473118391919));
#18225=CARTESIAN_POINT('Ctrl Pts',(84.4273710901036,3.7558898671908,-2.35815838504291));
#18226=CARTESIAN_POINT('Ctrl Pts',(84.4330753003716,3.82031583393719,-2.24870538954501));
#18227=CARTESIAN_POINT('Ctrl Pts',(84.4387739720551,3.8846792453711,-2.1393586689962));
#18228=CARTESIAN_POINT('Ctrl Pts',(84.4444726437386,3.94440827244869,-2.02713765864749));
#18229=CARTESIAN_POINT('Ctrl Pts',(84.4501713154221,3.99924191897012,-1.91247302557505));
#18230=CARTESIAN_POINT('Ctrl Pts',(84.455865870837,4.05403595801321,-1.79789121714149));
#18231=CARTESIAN_POINT('Ctrl Pts',(84.461560426252,4.10394148266522,-1.68086965789851));
#18232=CARTESIAN_POINT('Ctrl Pts',(84.4672549816669,4.14874311284873,-1.56186413736607));
#18233=CARTESIAN_POINT('Ctrl Pts',(84.4729474057725,4.19352797506243,-1.44290315719891));
#18234=CARTESIAN_POINT('Ctrl Pts',(84.4786398298781,4.23321260059651,-1.32196006511392));
#18235=CARTESIAN_POINT('Ctrl Pts',(84.4843322539837,4.26762962970939,-1.19951087682708));
#18236=CARTESIAN_POINT('Ctrl Pts',(84.4900237475625,4.30204103275377,-1.07708170501287));
#18237=CARTESIAN_POINT('Ctrl Pts',(84.4957152411413,4.33118644417461,-0.953147310833609));
#18238=CARTESIAN_POINT('Ctrl Pts',(84.5014067347201,4.35494845637367,-0.828198612851177));
#18239=CARTESIAN_POINT('Ctrl Pts',(84.5070985798207,4.37871193617777,-0.703242197704976));
#18240=CARTESIAN_POINT('Ctrl Pts',(84.5127904249213,4.39709128089044,-0.577271746302338));
#18241=CARTESIAN_POINT('Ctrl Pts',(84.5184822700218,4.41002035645222,-0.450787594857083));
#18242=CARTESIAN_POINT('Ctrl Pts',(84.5241757486305,4.42295314254171,-0.324267143604716));
#18243=CARTESIAN_POINT('Ctrl Pts',(84.5298692272391,4.43043250721369,-0.197233095956277));
#18244=CARTESIAN_POINT('Ctrl Pts',(84.5355627058477,4.43244429394526,-0.0701896080064969));
#18245=CARTESIAN_POINT('Ctrl Pts',(84.541262239029,4.43445822005588,0.0569889808327634));
#18246=CARTESIAN_POINT('Ctrl Pts',(84.5469617722102,4.4309929529109,0.184176630558526));
#18247=CARTESIAN_POINT('Ctrl Pts',(84.5526613053914,4.42208646834404,0.31087017626094));
#18248=CARTESIAN_POINT('Ctrl Pts',(84.5583642918138,4.41317458750389,0.437640483225464));
#18249=CARTESIAN_POINT('Ctrl Pts',(84.5640672782362,4.39881496678714,0.563915693839469));
#18250=CARTESIAN_POINT('Ctrl Pts',(84.5697702646585,4.37909716271554,0.689200289826353));
#18251=CARTESIAN_POINT('Ctrl Pts',(84.5754814199594,4.35935111513531,0.814664341728014));
#18252=CARTESIAN_POINT('Ctrl Pts',(84.5811925752603,4.33423163784856,0.939134555313065));
#18253=CARTESIAN_POINT('Ctrl Pts',(84.5869037305611,4.30387891674065,1.06212770891042));
#18254=CARTESIAN_POINT('Ctrl Pts',(84.5894064877895,4.29057766889308,1.11602608638165));
#18255=CARTESIAN_POINT('Ctrl Pts',(84.5919092450178,4.27627207253842,1.16964103157631));
#18256=CARTESIAN_POINT('Ctrl Pts',(84.5944120022462,4.26097685905561,1.22293303438601));
#18257=CARTESIAN_POINT('Ctrl Pts',(84.6001231015456,4.22607435951755,1.34454128166795));
#18258=CARTESIAN_POINT('Ctrl Pts',(84.6058342008451,4.18590781848005,1.46484180421131));
#18259=CARTESIAN_POINT('Ctrl Pts',(84.6115453001445,4.140592234111,1.58334612476858));
#18260=CARTESIAN_POINT('Ctrl Pts',(84.617249431588,4.09533193725281,1.70170586352247));
#18261=CARTESIAN_POINT('Ctrl Pts',(84.6229535630315,4.04493523656118,1.818273390522));
#18262=CARTESIAN_POINT('Ctrl Pts',(84.6286576944749,3.98956732935321,1.93257380830785));
#18263=CARTESIAN_POINT('Ctrl Pts',(84.634356285467,3.93425320127051,2.04676320552606));
#18264=CARTESIAN_POINT('Ctrl Pts',(84.6400548764591,3.87397764784127,2.15868951808578));
#18265=CARTESIAN_POINT('Ctrl Pts',(84.6457534674512,3.80895435337528,2.26789676438402));
#18266=CARTESIAN_POINT('Ctrl Pts',(84.6514479404111,3.74397804736939,2.37702509311312));
#18267=CARTESIAN_POINT('Ctrl Pts',(84.657142413371,3.6742610323866,2.48343792453169));
#18268=CARTESIAN_POINT('Ctrl Pts',(84.662836886331,3.60006319251113,2.58670330921939));
#18269=CARTESIAN_POINT('Ctrl Pts',(84.6685292256521,3.5258931535212,2.68993000182194));
#18270=CARTESIAN_POINT('Ctrl Pts',(84.6742215649733,3.44724586040078,2.79001126890387));
#18271=CARTESIAN_POINT('Ctrl Pts',(84.6799139042944,3.36442465521006,2.88654390914371));
#18272=CARTESIAN_POINT('Ctrl Pts',(84.6856053116618,3.28161700956417,2.98306074499313));
#18273=CARTESIAN_POINT('Ctrl Pts',(84.6912967190292,3.19463707092638,3.07602980678651));
#18274=CARTESIAN_POINT('Ctrl Pts',(84.6969881263966,3.10382828035472,3.16508120054925));
#18275=CARTESIAN_POINT('Ctrl Pts',(84.7026798839471,3.0130139024665,3.25413807349878));
#18276=CARTESIAN_POINT('Ctrl Pts',(84.7083716414975,2.91837048910615,3.33927651950545));
#18277=CARTESIAN_POINT('Ctrl Pts',(84.7140633990479,2.82027774807047,3.42016409310117));
#18278=CARTESIAN_POINT('Ctrl Pts',(84.7197567888548,2.72215687644153,3.50107486326993));
#18279=CARTESIAN_POINT('Ctrl Pts',(84.7254501786618,2.62058501715931,3.57773208207322));
#18280=CARTESIAN_POINT('Ctrl Pts',(84.7311435684687,2.5159738764591,3.64984444229824));
#18281=CARTESIAN_POINT('Ctrl Pts',(84.7368430114296,2.41125151426046,3.72203347164957));
#18282=CARTESIAN_POINT('Ctrl Pts',(84.7425424543906,2.30348374786703,3.78966776794911));
#18283=CARTESIAN_POINT('Ctrl Pts',(84.7482418973515,2.1931103637717,3.85249995876926));
#18284=CARTESIAN_POINT('Ctrl Pts',(84.7539447926189,2.08267012353876,3.91537020874317));
#18285=CARTESIAN_POINT('Ctrl Pts',(84.7596476878863,1.96962147595197,3.97343237656758));
#18286=CARTESIAN_POINT('Ctrl Pts',(84.7653505831536,1.85442644308312,4.02648625568175));
#18287=CARTESIAN_POINT('Ctrl Pts',(84.7710616466507,1.73906641691927,4.07961612361341));
#18288=CARTESIAN_POINT('Ctrl Pts',(84.7767727101477,1.62155423549691,4.12772322845963));
#18289=CARTESIAN_POINT('Ctrl Pts',(84.7824837736447,1.50236975911596,4.1706563160843));
#18290=CARTESIAN_POINT('Ctrl Pts',(84.7849874702226,1.45011998710461,4.18947792866547));
#18291=CARTESIAN_POINT('Ctrl Pts',(84.7874911668006,1.39754898808281,4.20730580431343));
#18292=CARTESIAN_POINT('Ctrl Pts',(84.7899948633785,1.34469785821158,4.22413028564712));
#18293=CARTESIAN_POINT('Ctrl Pts',(84.7957060737223,1.22413855311901,4.26250879870963));
#18294=CARTESIAN_POINT('Ctrl Pts',(84.8014172840661,1.10174897916768,4.29578114366027));
#18295=CARTESIAN_POINT('Ctrl Pts',(84.8071284944099,0.977999442804644,4.32377220605732));
#18296=CARTESIAN_POINT('Ctrl Pts',(84.8128327385545,0.854400848862536,4.35172912659941));
#18297=CARTESIAN_POINT('Ctrl Pts',(84.8185369826992,0.729445978649419,4.37441749312619));
#18298=CARTESIAN_POINT('Ctrl Pts',(84.8242412268438,0.603621667297139,4.39171149812569));
#18299=CARTESIAN_POINT('Ctrl Pts',(84.8299399320477,0.47791953399142,4.40898871028346));
#18300=CARTESIAN_POINT('Ctrl Pts',(84.8356386372515,0.35135003268023,4.42088192981958));
#18301=CARTESIAN_POINT('Ctrl Pts',(84.8413373424554,0.224411137252003,4.42731618946256));
#18302=CARTESIAN_POINT('Ctrl Pts',(84.8470319309937,0.0975639407203271,
4.43374580108566));
#18303=CARTESIAN_POINT('Ctrl Pts',(84.852726519532,-0.0296517215462163,
4.43472428139404));
#18304=CARTESIAN_POINT('Ctrl Pts',(84.8584211080703,-0.156732262753133,
4.43022843630126));
#18305=CARTESIAN_POINT('Ctrl Pts',(84.8641135645791,-0.283765225549177,
4.42573427443364));
#18306=CARTESIAN_POINT('Ctrl Pts',(84.8698060210878,-0.410662769618349,
4.41576987647275));
#18307=CARTESIAN_POINT('Ctrl Pts',(84.8754984775965,-0.536921139781867,
4.40036415420989));
#18308=CARTESIAN_POINT('Ctrl Pts',(84.8811900031187,-0.663158860714335,
4.38496095151321));
#18309=CARTESIAN_POINT('Ctrl Pts',(84.8868815286408,-0.788757219601314,
4.36411824296008));
#18310=CARTESIAN_POINT('Ctrl Pts',(84.8925730541629,-0.913217949425142,
4.33791677846034));
#18311=CARTESIAN_POINT('Ctrl Pts',(84.8982649307097,-1.03768635535937,4.31171369798635));
#18312=CARTESIAN_POINT('Ctrl Pts',(84.9039568072564,-1.16101660207895,4.28015128646399));
#18313=CARTESIAN_POINT('Ctrl Pts',(84.9096486838031,-1.28272148158459,4.24336123853266));
#18314=CARTESIAN_POINT('Ctrl Pts',(84.915342193323,-1.40446127765892,4.20656063570624));
#18315=CARTESIAN_POINT('Ctrl Pts',(84.9210357028429,-1.52457439694119,4.16452952832993));
#18316=CARTESIAN_POINT('Ctrl Pts',(84.9267292123628,-1.64259012738771,4.11744904927899));
#18317=CARTESIAN_POINT('Ctrl Pts',(84.9324287754738,-1.76073133737822,4.07031851218053));
#18318=CARTESIAN_POINT('Ctrl Pts',(84.9381283385848,-1.87677033494921,4.01812803219668));
#18319=CARTESIAN_POINT('Ctrl Pts',(84.9438279016958,-1.99025740351014,3.9611064701385));
#18320=CARTESIAN_POINT('Ctrl Pts',(84.9495309175265,-2.10381322103226,3.90405036517419));
#18321=CARTESIAN_POINT('Ctrl Pts',(84.9552339333572,-2.21481368183004,3.84215754205619));
#18322=CARTESIAN_POINT('Ctrl Pts',(84.960936949188,-2.3228359939973,3.77570151693571));
#18323=CARTESIAN_POINT('Ctrl Pts',(84.9666481328379,-2.43101301496091,3.70915031396307));
#18324=CARTESIAN_POINT('Ctrl Pts',(84.9723593164879,-2.53620304061023,3.63802308244691));
#18325=CARTESIAN_POINT('Ctrl Pts',(84.9780705001378,-2.63801412851126,3.5626353248368));
#18326=CARTESIAN_POINT('Ctrl Pts',(84.9805729082622,-2.68262360163107,3.52960347913115));
#18327=CARTESIAN_POINT('Ctrl Pts',(84.9830753163866,-2.7265848239857,3.49575418657852));
#18328=CARTESIAN_POINT('Ctrl Pts',(84.9855777245109,-2.76986702128935,3.4611162483184));
#18329=CARTESIAN_POINT('Ctrl Pts',(84.9912243167992,-2.86753171440395,3.38295700916141));
#18330=CARTESIAN_POINT('Ctrl Pts',(84.9968709090875,-2.96205339025877,3.30052625266452));
#18331=CARTESIAN_POINT('Ctrl Pts',(85.0025175013757,-3.053030434426,3.21410861149224));
#18332=CARTESIAN_POINT('Ctrl Pts',(85.0081571642047,-3.1438958321889,3.12779702145622));
#18333=CARTESIAN_POINT('Ctrl Pts',(85.0137968270336,-3.23122495445217,3.03750855549499));
#18334=CARTESIAN_POINT('Ctrl Pts',(85.0194364898626,-3.31464763040675,2.94356927661621));
#18335=CARTESIAN_POINT('Ctrl Pts',(85.025070718161,-3.39798991803049,2.84972052014929));
#18336=CARTESIAN_POINT('Ctrl Pts',(85.0307049464594,-3.47743297650439,2.752228252434));
#18337=CARTESIAN_POINT('Ctrl Pts',(85.0363391747578,-3.55264247977328,2.65145628116143));
#18338=CARTESIAN_POINT('Ctrl Pts',(85.0419695096807,-3.6278000116239,2.55075394553382));
#18339=CARTESIAN_POINT('Ctrl Pts',(85.0475998446036,-3.69872956427739,2.44677674203878));
#18340=CARTESIAN_POINT('Ctrl Pts',(85.0532301795266,-3.76513660798485,2.33992207631201));
#18341=CARTESIAN_POINT('Ctrl Pts',(85.0588585031136,-3.83151992897065,2.23310558249219));
#18342=CARTESIAN_POINT('Ctrl Pts',(85.0644868267007,-3.89338373725461,2.12341401726423));
#18343=CARTESIAN_POINT('Ctrl Pts',(85.0701151502877,-3.9504767177598,2.01127390040187));
#18344=CARTESIAN_POINT('Ctrl Pts',(85.0757428051582,-4.00756291489102,1.89914710721509));
#18345=CARTESIAN_POINT('Ctrl Pts',(85.0813704600287,-4.05987922626133,1.78457270583772));
#18346=CARTESIAN_POINT('Ctrl Pts',(85.0869981148991,-4.10722052283786,1.66800137193573));
#18347=CARTESIAN_POINT('Ctrl Pts',(85.092626442901,-4.15456748197023,1.55141609478051));
#18348=CARTESIAN_POINT('Ctrl Pts',(85.0982547709027,-4.19693809021681,1.43283378979986));
#18349=CARTESIAN_POINT('Ctrl Pts',(85.1038830989045,-4.23417579195539,1.31272402385989));
#18350=CARTESIAN_POINT('Ctrl Pts',(85.1095163365026,-4.27144597617936,1.19250948604803));
#18351=CARTESIAN_POINT('Ctrl Pts',(85.1151495741007,-4.3035741926547,1.07076521833574));
#18352=CARTESIAN_POINT('Ctrl Pts',(85.1207828116988,-4.33045408028453,0.947974925062423));
#18353=CARTESIAN_POINT('Ctrl Pts',(85.1264187717764,-4.35734695865774,0.82512528863957));
#18354=CARTESIAN_POINT('Ctrl Pts',(85.132054731854,-4.37898638639673,0.701229022711327));
#18355=CARTESIAN_POINT('Ctrl Pts',(85.1376906919317,-4.39531760270183,0.576777401931996));
#18356=CARTESIAN_POINT('Ctrl Pts',(85.1433341965746,-4.41167068075284,0.452159184270924));
#18357=CARTESIAN_POINT('Ctrl Pts',(85.1489777012174,-4.42270132347423,0.326984534477598));
#18358=CARTESIAN_POINT('Ctrl Pts',(85.1546212058603,-4.42840682077849,0.201747440337038));
#18359=CARTESIAN_POINT('Ctrl Pts',(85.1576835173074,-4.43150277104552,0.133790556936706));
#18360=CARTESIAN_POINT('Ctrl Pts',(85.1607458287545,-4.43303167658465,0.0658152632455171));
#18361=CARTESIAN_POINT('Ctrl Pts',(85.1638081402016,-4.43299950255766,-0.00210007702333399));
#18362=CARTESIAN_POINT('',(86.4138081166213,-4.43234892329218,0.00349148966335142));
#18363=CARTESIAN_POINT('Ctrl Pts',(85.1638081402417,-4.43299950255724,-0.00210007791362036));
#18364=CARTESIAN_POINT('Ctrl Pts',(85.1695922887089,-4.43293873165559,-0.130379783652825));
#18365=CARTESIAN_POINT('Ctrl Pts',(85.1753764371761,-4.42731018443659,-0.258519691248014));
#18366=CARTESIAN_POINT('Ctrl Pts',(85.1811605856433,-4.4161479401985,-0.386168836495802));
#18367=CARTESIAN_POINT('Ctrl Pts',(85.186871750214,-4.40512654021482,-0.512207315617334));
#18368=CARTESIAN_POINT('Ctrl Pts',(85.1925829147847,-4.38868807156609,-0.637968011965168));
#18369=CARTESIAN_POINT('Ctrl Pts',(85.1982940793554,-4.36685208303201,-0.762949464197328));
#18370=CARTESIAN_POINT('Ctrl Pts',(85.2039982771344,-4.34504273123389,-0.887778457201997));
#18371=CARTESIAN_POINT('Ctrl Pts',(85.2097024749135,-4.31784902678548,-1.01182970738669));
#18372=CARTESIAN_POINT('Ctrl Pts',(85.2154066726925,-4.28534238745932,-1.1346054918977));
#18373=CARTESIAN_POINT('Ctrl Pts',(85.2211053309981,-4.25286731605446,-1.25726204611044));
#18374=CARTESIAN_POINT('Ctrl Pts',(85.2268039893037,-4.21508967804332,-1.3786452156635));
#18375=CARTESIAN_POINT('Ctrl Pts',(85.2325026476092,-4.17213209911054,-1.49826658094328));
#18376=CARTESIAN_POINT('Ctrl Pts',(85.2381971887755,-4.12920555596306,-1.61780152275365));
#18377=CARTESIAN_POINT('Ctrl Pts',(85.2438917299418,-4.08110665480784,-1.73557681927961));
#18378=CARTESIAN_POINT('Ctrl Pts',(85.2495862711081,-4.0280079617409,-1.85111881308358));
#18379=CARTESIAN_POINT('Ctrl Pts',(85.2552786797146,-3.97492915370609,-1.96661753734309));
#18380=CARTESIAN_POINT('Ctrl Pts',(85.2609710883212,-3.91685444308981,-2.07988425972799));
#18381=CARTESIAN_POINT('Ctrl Pts',(85.2666634969278,-3.85400454625176,-2.19046523767686));
#18382=CARTESIAN_POINT('Ctrl Pts',(85.2723549742321,-3.79116493192394,-2.30102812410777));
#18383=CARTESIAN_POINT('Ctrl Pts',(85.2780464515365,-3.72355188249408,-2.4089057932066));
#18384=CARTESIAN_POINT('Ctrl Pts',(85.2837379288408,-3.65143183865771,-2.5136695342938));
#18385=CARTESIAN_POINT('Ctrl Pts',(85.2894297569057,-3.57930735012866,-2.61843973187502));
#18386=CARTESIAN_POINT('Ctrl Pts',(85.2951215849706,-3.50267554109995,-2.72009529096247));
#18387=CARTESIAN_POINT('Ctrl Pts',(85.3008134130355,-3.4218456062896,-2.81823732973583));
#18388=CARTESIAN_POINT('Ctrl Pts',(85.3065068738609,-3.34099248456491,-2.91640752158208));
#18389=CARTESIAN_POINT('Ctrl Pts',(85.3122003346864,-3.25593909499697,-3.01106188008166));
#18390=CARTESIAN_POINT('Ctrl Pts',(85.3178937955118,-3.16703390178018,-3.10183578949225));
#18391=CARTESIAN_POINT('Ctrl Pts',(85.3235933098706,-3.07803418072511,-3.19270621364082));
#18392=CARTESIAN_POINT('Ctrl Pts',(85.3292928242293,-2.98517475863295,-3.27968766553765));
#18393=CARTESIAN_POINT('Ctrl Pts',(85.334992338588,-2.88884005763955,-3.36245328909966));
#18394=CARTESIAN_POINT('Ctrl Pts',(85.3406953055672,-2.79244699954045,-3.44526904996622));
#18395=CARTESIAN_POINT('Ctrl Pts',(85.3463982725464,-2.69257478182457,-3.52386364849936));
#18396=CARTESIAN_POINT('Ctrl Pts',(85.3521012395256,-2.58963866509213,-3.59795227654006));
#18397=CARTESIAN_POINT('Ctrl Pts',(85.3578123745955,-2.48655511781412,-3.67214701822872));
#18398=CARTESIAN_POINT('Ctrl Pts',(85.3635235096653,-2.38039924212008,-3.74182268439385));
#18399=CARTESIAN_POINT('Ctrl Pts',(85.3692346447352,-2.27161316217369,-3.80673910866495));
#18400=CARTESIAN_POINT('Ctrl Pts',(85.3717375787487,-2.22393710892605,-3.83518906202039));
#18401=CARTESIAN_POINT('Ctrl Pts',(85.3742405127622,-2.17575617093942,-3.86272552896489));
#18402=CARTESIAN_POINT('Ctrl Pts',(85.3767434467757,-2.1271088057357,-3.88933119296386));
#18403=CARTESIAN_POINT('Ctrl Pts',(85.3824546235107,-2.01610559955142,-3.95003980470837));
#18404=CARTESIAN_POINT('Ctrl Pts',(85.3881658002456,-1.90233012796066,-4.00608616132336));
#18405=CARTESIAN_POINT('Ctrl Pts',(85.3938769769806,-1.78621056061312,-4.05720850254878));
#18406=CARTESIAN_POINT('Ctrl Pts',(85.3995811871163,-1.67023263806625,-4.10826848379477));
#18407=CARTESIAN_POINT('Ctrl Pts',(85.405285397252,-1.55191667062105,-4.15441623982777));
#18408=CARTESIAN_POINT('Ctrl Pts',(85.4109896073877,-1.43171647466371,-4.1954352499087));
#18409=CARTESIAN_POINT('Ctrl Pts',(85.4166882782262,-1.31163300382476,-4.23641442686982));
#18410=CARTESIAN_POINT('Ctrl Pts',(85.4223869490648,-1.18966932105934,-4.27227464011371));
#18411=CARTESIAN_POINT('Ctrl Pts',(85.4280856199033,-1.06629989185179,-4.30284714353611));
#18412=CARTESIAN_POINT('Ctrl Pts',(85.4337801737631,-0.943019590326126,
-4.33339755999275));
#18413=CARTESIAN_POINT('Ctrl Pts',(85.4394747276228,-0.818335949775803,
-4.35866777406351));
#18414=CARTESIAN_POINT('Ctrl Pts',(85.4451692814826,-0.692738838989604,
-4.37853878605127));
#18415=CARTESIAN_POINT('Ctrl Pts',(85.450861702975,-0.567188758961247,-4.39840235719308));
#18416=CARTESIAN_POINT('Ctrl Pts',(85.4565541244674,-0.440726282431298,
-4.41287068393357));
#18417=CARTESIAN_POINT('Ctrl Pts',(85.4622465459597,-0.313851400797239,
-4.42187588001038));
#18418=CARTESIAN_POINT('Ctrl Pts',(85.4679380362658,-0.186997273801771,
-4.43087960298561));
#18419=CARTESIAN_POINT('Ctrl Pts',(85.4736295265719,-0.0597312739027152,
-4.4344219446511));
#18420=CARTESIAN_POINT('Ctrl Pts',(85.479321016878,0.0674420884110509,-4.43248695031477));
#18421=CARTESIAN_POINT('Ctrl Pts',(85.4850128580468,0.194623290568652,-4.43055183669204));
#18422=CARTESIAN_POINT('Ctrl Pts',(85.4907046992156,0.321711444657403,-4.42313872156896));
#18423=CARTESIAN_POINT('Ctrl Pts',(85.4963965403845,0.448203160089113,-4.41028376947404));
#18424=CARTESIAN_POINT('Ctrl Pts',(85.5020900144023,0.574731162877896,-4.39742512961004));
#18425=CARTESIAN_POINT('Ctrl Pts',(85.5077834884201,0.700661989670943,-4.37912158748894));
#18426=CARTESIAN_POINT('Ctrl Pts',(85.513476962438,0.8254989944824,-4.35546098709523));
#18427=CARTESIAN_POINT('Ctrl Pts',(85.5191764900517,0.950468732450611,-4.33177522952809));
#18428=CARTESIAN_POINT('Ctrl Pts',(85.5248760176654,1.07434193384025,-4.30272111557916));
#18429=CARTESIAN_POINT('Ctrl Pts',(85.5305755452792,1.19663344072943,-4.26843734972508));
#18430=CARTESIAN_POINT('Ctrl Pts',(85.5362785255672,1.31899902967836,-4.23413281536421));
#18431=CARTESIAN_POINT('Ctrl Pts',(85.5419815058553,1.43978063662821,-4.19459244198594));
#18432=CARTESIAN_POINT('Ctrl Pts',(85.5476844861433,1.55851099892977,-4.15000391159032));
#18433=CARTESIAN_POINT('Ctrl Pts',(85.5533956344894,1.6774114120533,-4.10535151954972));
#18434=CARTESIAN_POINT('Ctrl Pts',(85.5591067828354,1.79425434779688,-4.05563668943388));
#18435=CARTESIAN_POINT('Ctrl Pts',(85.5648179311815,1.90859480129164,-4.00109421089813));
#18436=CARTESIAN_POINT('Ctrl Pts',(85.5673207234236,1.95870213218812,-3.97719210157135));
#18437=CARTESIAN_POINT('Ctrl Pts',(85.5698235156658,2.00832921938153,-3.95236344800934));
#18438=CARTESIAN_POINT('Ctrl Pts',(85.572326307908,2.0574403354243,-3.92663065059207));
#18439=CARTESIAN_POINT('Ctrl Pts',(85.5780374789707,2.16950796136399,-3.86791047178718));
#18440=CARTESIAN_POINT('Ctrl Pts',(85.5837486500335,2.27923261035931,-3.80429821675079));
#18441=CARTESIAN_POINT('Ctrl Pts',(85.5894598210962,2.38615904545413,-3.73600508696086));
#18442=CARTESIAN_POINT('Ctrl Pts',(85.595164025495,2.4929550483602,-3.66779526325316));
#18443=CARTESIAN_POINT('Ctrl Pts',(85.6008682298937,2.59695929464167,-3.59491613750161));
#18444=CARTESIAN_POINT('Ctrl Pts',(85.6065724342925,2.69773997708178,-3.5176253376468));
#18445=CARTESIAN_POINT('Ctrl Pts',(85.6122710993368,2.79842279137251,-3.44040959490972));
#18446=CARTESIAN_POINT('Ctrl Pts',(85.617969764381,2.89588795592724,-3.35879094451206));
#18447=CARTESIAN_POINT('Ctrl Pts',(85.6236684294253,2.98973197395674,-3.27307068727529));
#18448=CARTESIAN_POINT('Ctrl Pts',(85.6293629774406,3.08350819390913,-3.18741235906428));
#18449=CARTESIAN_POINT('Ctrl Pts',(85.635057525456,3.1736681804886,-3.09765859001536));
#18450=CARTESIAN_POINT('Ctrl Pts',(85.6407520734714,3.25984129678212,-3.0041510813862));
#18451=CARTESIAN_POINT('Ctrl Pts',(85.6464444890665,3.34598214408774,-2.91067858823279));
#18452=CARTESIAN_POINT('Ctrl Pts',(85.6521369046616,3.42813881953182,-2.81345544345195));
#18453=CARTESIAN_POINT('Ctrl Pts',(85.6578293202567,3.50597761159519,-2.71286011194704));
#18454=CARTESIAN_POINT('Ctrl Pts',(85.6635208046343,3.58380367007668,-2.61228123674696));
#18455=CARTESIAN_POINT('Ctrl Pts',(85.669212289012,3.65731300600262,-2.50833158768141));
#18456=CARTESIAN_POINT('Ctrl Pts',(85.6749037733897,3.72621262094353,-2.401422183524));
#18457=CARTESIAN_POINT('Ctrl Pts',(85.6805956086053,3.79511648303695,-2.29450618919122));
#18458=CARTESIAN_POINT('Ctrl Pts',(85.686287443821,3.85940984275311,-2.18463041242818));
#18459=CARTESIAN_POINT('Ctrl Pts',(85.6919792790366,3.91884369741315,-2.07223383700904));
#18460=CARTESIAN_POINT('Ctrl Pts',(85.6976727470829,3.97829460200788,-1.95980501811048));
#18461=CARTESIAN_POINT('Ctrl Pts',(85.7033662151292,4.03288304176703,-1.84485431468707));
#18462=CARTESIAN_POINT('Ctrl Pts',(85.7090596831755,4.08240676234838,-1.72784375067082));
#18463=CARTESIAN_POINT('Ctrl Pts',(85.7147592048222,4.13198313920451,-1.61070877474976));
#18464=CARTESIAN_POINT('Ctrl Pts',(85.720458726469,4.17648388924956,-1.49150993326182));
#18465=CARTESIAN_POINT('Ctrl Pts',(85.7261582481158,4.21575545488691,-1.37072788860198));
#18466=CARTESIAN_POINT('Ctrl Pts',(85.7318612224313,4.25505081054023,-1.24987267632775));
#18467=CARTESIAN_POINT('Ctrl Pts',(85.7375641967469,4.28911056445968,-1.12743273421331));
#18468=CARTESIAN_POINT('Ctrl Pts',(85.7432671710625,4.31783184116141,-1.00390098687701));
#18469=CARTESIAN_POINT('Ctrl Pts',(85.7489783134796,4.34659425399479,-0.880192310838207));
#18470=CARTESIAN_POINT('Ctrl Pts',(85.7546894558966,4.37000284883321,-0.755389098597385));
#18471=CARTESIAN_POINT('Ctrl Pts',(85.7604005983137,4.38800629490597,-0.62999186968215));
#18472=CARTESIAN_POINT('Ctrl Pts',(85.7629034552226,4.39589614357319,-0.575037659503052));
#18473=CARTESIAN_POINT('Ctrl Pts',(85.7654063121315,4.4027485801784,-0.519969400137956));
#18474=CARTESIAN_POINT('Ctrl Pts',(85.7679091690404,4.40856243807245,-0.464829247806832));
#18475=CARTESIAN_POINT('Ctrl Pts',(85.7736203402623,4.42182885285391,-0.339007092317808));
#18476=CARTESIAN_POINT('Ctrl Pts',(85.7793315114841,4.42972492539324,-0.212422456316731));
#18477=CARTESIAN_POINT('Ctrl Pts',(85.7850426827059,4.43217402107225,-0.0855712973619365));
#18478=CARTESIAN_POINT('Ctrl Pts',(85.7907468872527,4.43462012926359,0.0411251243660879));
#18479=CARTESIAN_POINT('Ctrl Pts',(85.7964510917996,4.43163247187119,0.168087026574939));
#18480=CARTESIAN_POINT('Ctrl Pts',(85.8021552963464,4.4231860418647,0.294812209810472));
#18481=CARTESIAN_POINT('Ctrl Pts',(85.8078539615275,4.4147478142051,0.421414329939794));
#18482=CARTESIAN_POINT('Ctrl Pts',(85.8135526267087,4.4008613886107,0.547779792491482));
#18483=CARTESIAN_POINT('Ctrl Pts',(85.8192512918899,4.38155380009099,0.673405744635561));
#18484=CARTESIAN_POINT('Ctrl Pts',(85.8249458400308,4.36226016047252,0.79894093743919));
#18485=CARTESIAN_POINT('Ctrl Pts',(85.8306403881718,4.33755321349061,0.923737290004157));
#18486=CARTESIAN_POINT('Ctrl Pts',(85.8363349363128,4.30751183518414,1.04729689665758));
#18487=CARTESIAN_POINT('Ctrl Pts',(85.842027352016,4.27748170647394,1.17081023393959));
#18488=CARTESIAN_POINT('Ctrl Pts',(85.8477197677193,4.24212121245362,1.29308735892681));
#18489=CARTESIAN_POINT('Ctrl Pts',(85.8534121834226,4.2015602976528,1.41364071290682));
#18490=CARTESIAN_POINT('Ctrl Pts',(85.8591036678975,4.16100601825514,1.53417434543552));
#18491=CARTESIAN_POINT('Ctrl Pts',(85.8647951523725,4.11525313751914,1.65298438968496));
#18492=CARTESIAN_POINT('Ctrl Pts',(85.8704866368474,4.06448126504001,1.76959912017913));
#18493=CARTESIAN_POINT('Ctrl Pts',(85.8761784721493,4.01370626294856,1.88622103888362));
#18494=CARTESIAN_POINT('Ctrl Pts',(85.8818703074511,3.95791181314679,2.00064700870561));
#18495=CARTESIAN_POINT('Ctrl Pts',(85.887562142753,3.89732519136754,2.11242641356615));
#18496=CARTESIAN_POINT('Ctrl Pts',(85.8932556108743,3.83672118907633,2.22423788463581));
#18497=CARTESIAN_POINT('Ctrl Pts',(85.8989490789955,3.771322470121,2.33340092960423));
#18498=CARTESIAN_POINT('Ctrl Pts',(85.9046425471168,3.70140140394464,2.43949106308604));
#18499=CARTESIAN_POINT('Ctrl Pts',(85.9103420688211,3.63140599415773,2.54569399695831));
#18500=CARTESIAN_POINT('Ctrl Pts',(85.9160415905253,3.55687885651625,2.64881716228718));
#18501=CARTESIAN_POINT('Ctrl Pts',(85.9217411122296,3.47813487125343,2.74846626636946));
#18502=CARTESIAN_POINT('Ctrl Pts',(85.9274440865927,3.39934318442251,2.84817573593246));
#18503=CARTESIAN_POINT('Ctrl Pts',(85.9331470609559,3.31632982143383,2.94440665005461));
#18504=CARTESIAN_POINT('Ctrl Pts',(85.9388500353191,3.22944796762092,3.0368000962245));
#18505=CARTESIAN_POINT('Ctrl Pts',(85.944561177768,3.14244167726211,3.12932587291913));
#18506=CARTESIAN_POINT('Ctrl Pts',(85.9502723202169,3.05155611777546,3.21800292888566));
#18507=CARTESIAN_POINT('Ctrl Pts',(85.9559834626658,2.95717937360453,3.30251103742711));
#18508=CARTESIAN_POINT('Ctrl Pts',(85.9584863185014,2.91581963043415,3.33954594147888));
#18509=CARTESIAN_POINT('Ctrl Pts',(85.9609891743371,2.87378979081121,3.37578072053583));
#18510=CARTESIAN_POINT('Ctrl Pts',(85.9634920301727,2.83112429126425,3.41119103062457));
#18511=CARTESIAN_POINT('Ctrl Pts',(85.9692032026784,2.73376749408617,3.49199248411575));
#18512=CARTESIAN_POINT('Ctrl Pts',(85.9749143751842,2.63279861011643,3.56874735740786));
#18513=CARTESIAN_POINT('Ctrl Pts',(85.9806255476899,2.52858789811429,3.64111689478791));
#18514=CARTESIAN_POINT('Ctrl Pts',(85.9863297535422,2.42450430535391,3.7133981537123));
#18515=CARTESIAN_POINT('Ctrl Pts',(85.9920339593944,2.31718707696461,3.78130449344741));
#18516=CARTESIAN_POINT('Ctrl Pts',(85.9977381652467,2.20704029072567,3.84453666325522));
#18517=CARTESIAN_POINT('Ctrl Pts',(86.0034368317531,2.09700046786776,3.90770742839655));
#18518=CARTESIAN_POINT('Ctrl Pts',(86.0091354982595,1.98413689906786,3.96621285812227));
#18519=CARTESIAN_POINT('Ctrl Pts',(86.0148341647659,1.8688830600145,4.01979665007956));
#18520=CARTESIAN_POINT('Ctrl Pts',(86.0205287142502,1.75371248651015,4.07334173023434));
#18521=CARTESIAN_POINT('Ctrl Pts',(86.0262232637346,1.63615544044178,4.1219720817462));
#18522=CARTESIAN_POINT('Ctrl Pts',(86.031917813219,1.51667002306284,4.165477288516));
#18523=CARTESIAN_POINT('Ctrl Pts',(86.0376102302877,1.39722934891961,4.20896620406161));
#18524=CARTESIAN_POINT('Ctrl Pts',(86.0433026473565,1.27586211372183,4.24733365451933));
#18525=CARTESIAN_POINT('Ctrl Pts',(86.0489950644252,1.15304612211939,4.28041746098035));
#18526=CARTESIAN_POINT('Ctrl Pts',(86.054686550279,1.03025022182269,4.31349585530519));
#18527=CARTESIAN_POINT('Ctrl Pts',(86.0603780361328,0.906006421814709,4.34129222110404));
#18528=CARTESIAN_POINT('Ctrl Pts',(86.0660695219865,0.780806886217592,4.36369449050173));
#18529=CARTESIAN_POINT('Ctrl Pts',(86.0717613586791,0.655599632977198,4.38609814083685));
#18530=CARTESIAN_POINT('Ctrl Pts',(86.0774531953717,0.529436919905267,4.40310696314175));
#18531=CARTESIAN_POINT('Ctrl Pts',(86.0831450320643,0.402819771366682,4.41466026233006));
#18532=CARTESIAN_POINT('Ctrl Pts',(86.0888385015867,0.276166299885106,4.42621687583899));
#18533=CARTESIAN_POINT('Ctrl Pts',(86.0945319711091,0.14905853094495,4.43231481657198));
#18534=CARTESIAN_POINT('Ctrl Pts',(86.1002254406316,0.0220007440576986,
4.43294540540044));
#18535=CARTESIAN_POINT('Ctrl Pts',(86.1059249637453,-0.105192137239539,
4.43357666470356));
#18536=CARTESIAN_POINT('Ctrl Pts',(86.111624486859,-0.232334530872,4.42872896347229));
#18537=CARTESIAN_POINT('Ctrl Pts',(86.1173240099726,-0.358923714736252,
4.41844574109493));
#18538=CARTESIAN_POINT('Ctrl Pts',(86.1230269857519,-0.485589583983631,
4.4081562893319));
#18539=CARTESIAN_POINT('Ctrl Pts',(86.1287299615311,-0.611701180417469,
4.39242480622584));
#18540=CARTESIAN_POINT('Ctrl Pts',(86.1344329373103,-0.736763988310469,
4.37134622576717));
#18541=CARTESIAN_POINT('Ctrl Pts',(86.1401440811732,-0.862005917335847,
4.35023745552414));
#18542=CARTESIAN_POINT('Ctrl Pts',(86.1458552250361,-0.986195668909993,
4.32376637898218));
#18543=CARTESIAN_POINT('Ctrl Pts',(86.151566368899,-1.10885157311499,4.29207842295553));
#18544=CARTESIAN_POINT('Ctrl Pts',(86.154069209701,-1.16260406281344,4.27819155349802));
#18545=CARTESIAN_POINT('Ctrl Pts',(86.1565720505031,-1.21606220092094,4.26330340480065));
#18546=CARTESIAN_POINT('Ctrl Pts',(86.1590748913052,-1.26918663554271,4.24742913821523));
#18547=CARTESIAN_POINT('Ctrl Pts',(86.1647860630679,-1.39040999528434,4.21120603405196));
#18548=CARTESIAN_POINT('Ctrl Pts',(86.1704972348306,-1.51026837993683,4.16973328146862));
#18549=CARTESIAN_POINT('Ctrl Pts',(86.1762084065934,-1.62827458282358,4.12313119885006));
#18550=CARTESIAN_POINT('Ctrl Pts',(86.1819126116936,-1.74613683812524,4.07658596288097));
#18551=CARTESIAN_POINT('Ctrl Pts',(86.1876168167939,-1.86215103851585,4.02492399025031));
#18552=CARTESIAN_POINT('Ctrl Pts',(86.1933210218942,-1.97584410367757,3.96831564747093));
#18553=CARTESIAN_POINT('Ctrl Pts',(86.1990196876406,-2.08942676149783,3.91176227705615));
#18554=CARTESIAN_POINT('Ctrl Pts',(86.204718353387,-2.20069241403268,3.85027227151843));
#18555=CARTESIAN_POINT('Ctrl Pts',(86.2104170191334,-2.30918742425279,3.78406427530939));
#18556=CARTESIAN_POINT('Ctrl Pts',(86.2161115678507,-2.41760405171904,3.71790411139291));
#18557=CARTESIAN_POINT('Ctrl Pts',(86.221806116568,-2.52325368122513,3.64703294803797));
#18558=CARTESIAN_POINT('Ctrl Pts',(86.2275006652853,-2.62570720997412,3.57171536484781));
#18559=CARTESIAN_POINT('Ctrl Pts',(86.2331930815794,-2.72812237320855,3.4964259856431));
#18560=CARTESIAN_POINT('Ctrl Pts',(86.2388854978734,-2.82734349431179,3.41669373329982));
#18561=CARTESIAN_POINT('Ctrl Pts',(86.2445779141674,-2.92297069027303,3.33282632967948));
#18562=CARTESIAN_POINT('Ctrl Pts',(86.2502693992418,-3.01858224262913,3.24897264588575));
#18563=CARTESIAN_POINT('Ctrl Pts',(86.2559608843163,-3.11060073929695,3.16098541946339));
#18564=CARTESIAN_POINT('Ctrl Pts',(86.2616523693908,-3.19866003939449,3.06921210612444));
#18565=CARTESIAN_POINT('Ctrl Pts',(86.2673442053004,-3.28672476765249,2.97743313568545));
#18566=CARTESIAN_POINT('Ctrl Pts',(86.27303604121,-3.3708295375752,2.88186790218265));
#18567=CARTESIAN_POINT('Ctrl Pts',(86.2787278771196,-3.45064604946544,2.78289971815525));
#18568=CARTESIAN_POINT('Ctrl Pts',(86.2844213458561,-3.53048545845897,2.68390314295066));
#18569=CARTESIAN_POINT('Ctrl Pts',(86.2901148145927,-3.60603391168587,2.58150198578219));
#18570=CARTESIAN_POINT('Ctrl Pts',(86.2958082833293,-3.6770045935842,2.47611110791917));
#18571=CARTESIAN_POINT('Ctrl Pts',(86.301507805657,-3.74805073519088,2.37060817301099));
#18572=CARTESIAN_POINT('Ctrl Pts',(86.3072073279847,-3.81450916416067,2.26210950190459));
#18573=CARTESIAN_POINT('Ctrl Pts',(86.3129068503124,-3.87613730269169,2.15105755633874));
#18574=CARTESIAN_POINT('Ctrl Pts',(86.3186098253045,-3.93780277440074,2.03993833757344));
#18575=CARTESIAN_POINT('Ctrl Pts',(86.3243128002966,-3.99463194833798,1.92626311952929));
#18576=CARTESIAN_POINT('Ctrl Pts',(86.3300157752888,-4.04642965167852,1.8104960850598));
#18577=CARTESIAN_POINT('Ctrl Pts',(86.3357269183697,-4.09830154230549,1.69456324319747));
#18578=CARTESIAN_POINT('Ctrl Pts',(86.3414380614506,-4.14512742613423,1.57653297279318));
#18579=CARTESIAN_POINT('Ctrl Pts',(86.3471492045315,-4.18676127389963,1.45688676134225));
#18580=CARTESIAN_POINT('Ctrl Pts',(86.3496520538335,-4.20500687645996,1.40445304841033));
#18581=CARTESIAN_POINT('Ctrl Pts',(86.3521549031355,-4.22225598356386,1.35170915067926));
#18582=CARTESIAN_POINT('Ctrl Pts',(86.3546577524375,-4.23849939450282,1.29869622421843));
#18583=CARTESIAN_POINT('Ctrl Pts',(86.361543519039,-4.28318779681662,1.1528485944062));
#18584=CARTESIAN_POINT('Ctrl Pts',(86.3684292856406,-4.32037172905848,1.00460305815416));
#18585=CARTESIAN_POINT('Ctrl Pts',(86.3753150522421,-4.34983235093349,0.854662224959333));
#18586=CARTESIAN_POINT('Ctrl Pts',(86.3821258148638,-4.37897206970221,0.706354638996579));
#18587=CARTESIAN_POINT('Ctrl Pts',(86.3889365774854,-4.40055579046778,0.556388511698405));
#18588=CARTESIAN_POINT('Ctrl Pts',(86.3957473401071,-4.41441820880992,0.405463781030341));
#18589=CARTESIAN_POINT('Ctrl Pts',(86.4017675963939,-4.42667165468834,0.272056465415288));
#18590=CARTESIAN_POINT('Ctrl Pts',(86.4077878526808,-4.43289274202569,0.137900439209401));
#18591=CARTESIAN_POINT('Ctrl Pts',(86.4138081089676,-4.43299862449031,0.00349217224992315));
#18592=CARTESIAN_POINT('',(87.6638081644291,-4.43227616981233,-0.00345667368086795));
#18593=CARTESIAN_POINT('Ctrl Pts',(86.4138081402417,-4.43034383484303,0.0034893830850436));
#18594=CARTESIAN_POINT('Ctrl Pts',(86.4592856313511,-4.42253105442582,-1.01124001134147));
#18595=CARTESIAN_POINT('Ctrl Pts',(86.5699574095046,-3.57721990853862,-3.49240746487907));
#18596=CARTESIAN_POINT('Ctrl Pts',(86.7458234747023,0.510683341348773,-5.18931099460031));
#18597=CARTESIAN_POINT('Ctrl Pts',(86.9414063358345,4.60181158071817,-2.45215751524593));
#18598=CARTESIAN_POINT('Ctrl Pts',(87.1369891969671,4.59217127324197,2.47016372199963));
#18599=CARTESIAN_POINT('Ctrl Pts',(87.3325720580992,0.490353289406007,5.19127149832776));
#18600=CARTESIAN_POINT('Ctrl Pts',(87.5081783725243,-3.58484425455734,3.48089885108923));
#18601=CARTESIAN_POINT('Ctrl Pts',(87.618590399905,-4.42252617546647,1.00556395309676));
#18602=CARTESIAN_POINT('Ctrl Pts',(87.6638081402417,-4.43019710367684,-0.00345451242541441));
#18603=CARTESIAN_POINT('',(88.9138081402808,-4.43299954096812,0.00201736869289629));
#18604=CARTESIAN_POINT('Ctrl Pts',(87.6638081728344,-4.4329986517271,-0.00345742472382504));
#18605=CARTESIAN_POINT('Ctrl Pts',(87.6705757511896,-4.43288079608067,-0.154568139619312));
#18606=CARTESIAN_POINT('Ctrl Pts',(87.6773433295449,-4.42503256386582,-0.305361128860425));
#18607=CARTESIAN_POINT('Ctrl Pts',(87.6841109079001,-4.40957434100509,-0.455129795936879));
#18608=CARTESIAN_POINT('Ctrl Pts',(87.6909538833469,-4.39394389922306,-0.606567024692115));
#18609=CARTESIAN_POINT('Ctrl Pts',(87.6977968587938,-4.37053302507896,-0.756956934271215));
#18610=CARTESIAN_POINT('Ctrl Pts',(87.7046398342406,-4.33951570976822,-0.905589534322728));
#18611=CARTESIAN_POINT('Ctrl Pts',(87.7110058162818,-4.31066047365515,-1.04386161640392));
#18612=CARTESIAN_POINT('Ctrl Pts',(87.7173717983229,-4.27522281140193,-1.1806130378423));
#18613=CARTESIAN_POINT('Ctrl Pts',(87.7237377803641,-4.23337995783103,-1.31528823177072));
#18614=CARTESIAN_POINT('Ctrl Pts',(87.7294489573705,-4.19584106098065,-1.43611073266965));
#18615=CARTESIAN_POINT('Ctrl Pts',(87.7351601343769,-4.1530676566428,-1.55551126187134));
#18616=CARTESIAN_POINT('Ctrl Pts',(87.7408713113832,-4.1051853535367,-1.67300394892175));
#18617=CARTESIAN_POINT('Ctrl Pts',(87.7465755217392,-4.05736145857781,-1.79035331516853));
#18618=CARTESIAN_POINT('Ctrl Pts',(87.7522797320952,-4.00444121260155,-1.90579910278776));
#18619=CARTESIAN_POINT('Ctrl Pts',(87.7579839424511,-3.94660011590412,-2.01887011101397));
#18620=CARTESIAN_POINT('Ctrl Pts',(87.7636826134589,-3.88881518858871,-2.13183131619322));
#18621=CARTESIAN_POINT('Ctrl Pts',(87.7693812844667,-3.82611910009916,-2.24242197751844));
#18622=CARTESIAN_POINT('Ctrl Pts',(87.7750799554746,-3.75873541441771,-2.35019086127109));
#18623=CARTESIAN_POINT('Ctrl Pts',(87.7807745094528,-3.69140041037253,-2.45788188692578));
#18624=CARTESIAN_POINT('Ctrl Pts',(87.786469063431,-3.6193847603393,-2.56275485516058));
#18625=CARTESIAN_POINT('Ctrl Pts',(87.7921636174092,-3.54295769399091,-2.66438356446489));
#18626=CARTESIAN_POINT('Ctrl Pts',(87.7978560389441,-3.46655924733509,-2.76597421680122));
#18627=CARTESIAN_POINT('Ctrl Pts',(87.8035484604791,-3.3857529085027,-2.86432270729645));
#18628=CARTESIAN_POINT('Ctrl Pts',(87.809240882014,-3.30085072918975,-2.95903252155287));
#18629=CARTESIAN_POINT('Ctrl Pts',(87.8149323723154,-3.21596243917818,-3.05372684205912));
#18630=CARTESIAN_POINT('Ctrl Pts',(87.8206238626167,-3.12697990780726,-3.14478337323757));
#18631=CARTESIAN_POINT('Ctrl Pts',(87.8263153529181,-3.03425455143084,-3.23183977281072));
#18632=CARTESIAN_POINT('Ctrl Pts',(87.832007194035,-2.94152347959329,-3.31890153841843));
#18633=CARTESIAN_POINT('Ctrl Pts',(87.8376990351518,-2.84504941492009,-3.40196240881344));
#18634=CARTESIAN_POINT('Ctrl Pts',(87.8433908762687,-2.74521921707215,-3.48069827049369));
#18635=CARTESIAN_POINT('Ctrl Pts',(87.8490843501873,-2.64536038122838,-3.55945671889947));
#18636=CARTESIAN_POINT('Ctrl Pts',(87.8547778241059,-2.5421438102242,-3.63388744331551));
#18637=CARTESIAN_POINT('Ctrl Pts',(87.8604712980245,-2.43598745958902,-3.70370815490706));
#18638=CARTESIAN_POINT('Ctrl Pts',(87.8661708254683,-2.32971823935071,-3.77360310262259));
#18639=CARTESIAN_POINT('Ctrl Pts',(87.8718703529121,-2.22050333247716,-3.83887803149167));
#18640=CARTESIAN_POINT('Ctrl Pts',(87.8775698803559,-2.10878781240466,-3.89929518788377));
#18641=CARTESIAN_POINT('Ctrl Pts',(87.8832728604334,-1.99700461781569,-3.95974894350437));
#18642=CARTESIAN_POINT('Ctrl Pts',(87.8889758405108,-1.8827181507044,-4.01533889009331));
#18643=CARTESIAN_POINT('Ctrl Pts',(87.8946788205883,-1.76639468899386,-4.06587491232752));
#18644=CARTESIAN_POINT('Ctrl Pts',(87.9003899686633,-1.64990462495538,-4.11648331393236));
#18645=CARTESIAN_POINT('Ctrl Pts',(87.9061011167384,-1.53137211262844,-4.16202319497411));
#18646=CARTESIAN_POINT('Ctrl Pts',(87.9118122648134,-1.41128019930832,-4.20235376890621));
#18647=CARTESIAN_POINT('Ctrl Pts',(87.9143150570411,-1.35865240830802,-4.22002780670894));
#18648=CARTESIAN_POINT('Ctrl Pts',(87.9168178492688,-1.30572529828921,-4.2367020811707));
#18649=CARTESIAN_POINT('Ctrl Pts',(87.9193206414965,-1.25254012004275,-4.25236784011958));
#18650=CARTESIAN_POINT('Ctrl Pts',(87.9250318052834,-1.13117596498531,-4.28811579962354));
#18651=CARTESIAN_POINT('Ctrl Pts',(87.9307429690702,-1.00809299213488,-4.31871910368859));
#18652=CARTESIAN_POINT('Ctrl Pts',(87.936454132857,-0.883765194782438,-4.34401290058986));
#18653=CARTESIAN_POINT('Ctrl Pts',(87.94215833,-0.759589056096376,-4.36927584338138));
#18654=CARTESIAN_POINT('Ctrl Pts',(87.947862527143,-0.634171501678992,-4.38924208537194));
#18655=CARTESIAN_POINT('Ctrl Pts',(87.953566724286,-0.508001978349318,-4.403796429218));
#18656=CARTESIAN_POINT('Ctrl Pts',(87.9592653821028,-0.381954977810399,
-4.41833663939073));
#18657=CARTESIAN_POINT('Ctrl Pts',(87.9649640399195,-0.255157855715425,
-4.42747536357883));
#18658=CARTESIAN_POINT('Ctrl Pts',(87.9706626977363,-0.128110090345371,
-4.43114847469047));
#18659=CARTESIAN_POINT('Ctrl Pts',(87.9763572385605,-0.00115411057021916,
-4.43481893216482));
#18660=CARTESIAN_POINT('Ctrl Pts',(87.9820517793847,0.12605175445124,-4.43303162403448));
#18661=CARTESIAN_POINT('Ctrl Pts',(87.987746320209,0.253003539893165,-4.42577430613012));
#18662=CARTESIAN_POINT('Ctrl Pts',(87.9934387286927,0.379907787798938,-4.4185197057536));
#18663=CARTESIAN_POINT('Ctrl Pts',(87.9991311371764,0.506557747435535,-4.40579919098026));
#18664=CARTESIAN_POINT('Ctrl Pts',(88.00482354566,0.63245041801114,-4.38765261486795));
#18665=CARTESIAN_POINT('Ctrl Pts',(88.010515022978,0.758322495028929,-4.36950900717757));
#18666=CARTESIAN_POINT('Ctrl Pts',(88.0162065002959,0.883437134455935,-4.34594116058187));
#18667=CARTESIAN_POINT('Ctrl Pts',(88.0218979776139,1.00729794900592,-4.31704063473214));
#18668=CARTESIAN_POINT('Ctrl Pts',(88.0275898058288,1.13116639995466,-4.28813832707643));
#18669=CARTESIAN_POINT('Ctrl Pts',(88.0332816340438,1.2537804835487,-4.25390277696927));
#18670=CARTESIAN_POINT('Ctrl Pts',(88.0389734622587,1.37465597623267,-4.21447623637953));
#18671=CARTESIAN_POINT('Ctrl Pts',(88.0446669233707,1.49556614621698,-4.17503838492803));
#18672=CARTESIAN_POINT('Ctrl Pts',(88.0503603844827,1.61473635372315,-4.13040670415919));
#18673=CARTESIAN_POINT('Ctrl Pts',(88.0560538455948,1.73169994193205,-4.0807725140116));
#18674=CARTESIAN_POINT('Ctrl Pts',(88.0617533604442,1.84878789506444,-4.03108554887347));
#18675=CARTESIAN_POINT('Ctrl Pts',(88.0674528752937,1.96366417657744,-3.97638561031657));
#18676=CARTESIAN_POINT('Ctrl Pts',(88.0731523901432,2.07588415770217,-3.91691127852051));
#18677=CARTESIAN_POINT('Ctrl Pts',(88.0788553577306,2.18817212113683,-3.85740091746819));
#18678=CARTESIAN_POINT('Ctrl Pts',(88.084558325318,2.29780023476497,-3.7931106029559));
#18679=CARTESIAN_POINT('Ctrl Pts',(88.0902612929054,2.4043517590273,-3.72432297456361));
#18680=CARTESIAN_POINT('Ctrl Pts',(88.0959724287579,2.51105589525509,-3.65543682280207));
#18681=CARTESIAN_POINT('Ctrl Pts',(88.1016835646103,2.61467431828384,-3.58204072535583));
#18682=CARTESIAN_POINT('Ctrl Pts',(88.1073947004628,2.71482204360294,-3.50445862745839));
#18683=CARTESIAN_POINT('Ctrl Pts',(88.1098976345181,2.75871228868591,-3.47045788226004));
#18684=CARTESIAN_POINT('Ctrl Pts',(88.1124005685735,2.80193638633805,-3.43565363688784));
#18685=CARTESIAN_POINT('Ctrl Pts',(88.1149035026288,2.84446417661572,-3.40007537386304));
#18686=CARTESIAN_POINT('Ctrl Pts',(88.1206146717402,2.94150364982505,-3.31889326025948));
#18687=CARTESIAN_POINT('Ctrl Pts',(88.1263258408516,3.03521459496464,-3.23342829836434));
#18688=CARTESIAN_POINT('Ctrl Pts',(88.1320370099629,3.12519701718668,-3.1439835565358));
#18689=CARTESIAN_POINT('Ctrl Pts',(88.1377412123272,3.21506967470595,-3.05464792352271));
#18690=CARTESIAN_POINT('Ctrl Pts',(88.1434454146914,3.3012225772479,-2.96134244794028));
#18691=CARTESIAN_POINT('Ctrl Pts',(88.1491496170557,3.38328848545012,-2.86441058932211));
#18692=CARTESIAN_POINT('Ctrl Pts',(88.1548482799858,3.46527469825097,-2.76757286264675));
#18693=CARTESIAN_POINT('Ctrl Pts',(88.1605469429159,3.5431815578693,-2.66711606340454));
#18694=CARTESIAN_POINT('Ctrl Pts',(88.1662456058459,3.61667876495443,-2.56342031495573));
#18695=CARTESIAN_POINT('Ctrl Pts',(88.1719401516709,3.6901228726136,-2.45979948343144));
#18696=CARTESIAN_POINT('Ctrl Pts',(88.1776346974958,3.75916343848788,-2.3529446846301));
#18697=CARTESIAN_POINT('Ctrl Pts',(88.1833292433207,3.82351085388271,-2.24326854171344));
#18698=CARTESIAN_POINT('Ctrl Pts',(88.189021656621,3.88783417210612,-2.13363347091754));
#18699=CARTESIAN_POINT('Ctrl Pts',(88.1947140699213,3.94746763271936,-2.02117950050547));
#18700=CARTESIAN_POINT('Ctrl Pts',(88.2004064832217,4.0021655180592,-1.90634733615308));
#18701=CARTESIAN_POINT('Ctrl Pts',(88.2060979652404,4.05685445479885,-1.79153395839767));
#18702=CARTESIAN_POINT('Ctrl Pts',(88.2117894472592,4.10660925078805,-1.67434352083793));
#18703=CARTESIAN_POINT('Ctrl Pts',(88.217480929278,4.15123088658256,-1.55523989348363));
#18704=CARTESIAN_POINT('Ctrl Pts',(88.2231727620735,4.19585527249231,-1.43612892554904));
#18705=CARTESIAN_POINT('Ctrl Pts',(88.228864594869,4.23534572894581,-1.31510490710335));
#18706=CARTESIAN_POINT('Ctrl Pts',(88.2345564276645,4.26955216788328,-1.19264969111771));
#18707=CARTESIAN_POINT('Ctrl Pts',(88.2402498932322,4.30376841935809,-1.07015934734863));
#18708=CARTESIAN_POINT('Ctrl Pts',(88.2459433587999,4.33269753054817,-0.946237373589296));
#18709=CARTESIAN_POINT('Ctrl Pts',(88.2516368243676,4.35623998860488,-0.821378208671102));
#18710=CARTESIAN_POINT('Ctrl Pts',(88.2573363434618,4.37980747797038,-0.696386288358162));
#18711=CARTESIAN_POINT('Ctrl Pts',(88.263035862556,4.397976804961,-0.570455579934879));
#18712=CARTESIAN_POINT('Ctrl Pts',(88.2687353816502,4.41070000104378,-0.444088392994422));
#18713=CARTESIAN_POINT('Ctrl Pts',(88.2744383533676,4.42343090451393,-0.317644656038224));
#18714=CARTESIAN_POINT('Ctrl Pts',(88.280141325085,4.43070908200215,-0.19076431168318));
#18715=CARTESIAN_POINT('Ctrl Pts',(88.2858442968024,4.43253869514335,-0.0639508878508889));
#18716=CARTESIAN_POINT('Ctrl Pts',(88.2915554365745,4.43437092873946,0.0630441639184597));
#18717=CARTESIAN_POINT('Ctrl Pts',(88.2972665763467,4.43073902727015,0.189971705676443));
#18718=CARTESIAN_POINT('Ctrl Pts',(88.3029777161188,4.42169913418975,0.316331735217335));
#18719=CARTESIAN_POINT('Ctrl Pts',(88.3054805986663,4.41773743976013,0.371708477033451));
#18720=CARTESIAN_POINT('Ctrl Pts',(88.3079834812138,4.41273775705088,0.426976332165075));
#18721=CARTESIAN_POINT('Ctrl Pts',(88.3104863637613,4.40670789966582,0.482093857068187));
#18722=CARTESIAN_POINT('Ctrl Pts',(88.3161975759169,4.39294864642833,0.60786399299958));
#18723=CARTESIAN_POINT('Ctrl Pts',(88.3219087880726,4.37377955462869,0.733238601419334));
#18724=CARTESIAN_POINT('Ctrl Pts',(88.3276200002283,4.34923107730234,0.857716757576488));
#18725=CARTESIAN_POINT('Ctrl Pts',(88.3333242458431,4.3247125442268,0.982043075186615));
#18726=CARTESIAN_POINT('Ctrl Pts',(88.339028491458,4.2948277567347,1.10547472776412));
#18727=CARTESIAN_POINT('Ctrl Pts',(88.3447327370728,4.25965894325909,1.22751565656527));
#18728=CARTESIAN_POINT('Ctrl Pts',(88.3504314434066,4.2245242815287,1.34943807381331));
#18729=CARTESIAN_POINT('Ctrl Pts',(88.3561301497404,4.18411591410322,1.46997207321479));
#18730=CARTESIAN_POINT('Ctrl Pts',(88.3618288560741,4.13856706284499,1.58863201098763));
#18731=CARTESIAN_POINT('Ctrl Pts',(88.3675234454031,4.09305111815007,1.70720622342061));
#18732=CARTESIAN_POINT('Ctrl Pts',(88.373218034732,4.04240222360458,1.82390869754284));
#18733=CARTESIAN_POINT('Ctrl Pts',(88.378912624061,3.98680320857934,1.93826963450947));
#18734=CARTESIAN_POINT('Ctrl Pts',(88.3846050808537,3.9312250145309,2.05258774506246));
#18735=CARTESIAN_POINT('Ctrl Pts',(88.3902975376465,3.87070056010836,2.16456570357824));
#18736=CARTESIAN_POINT('Ctrl Pts',(88.3959899944392,3.80546038042305,2.27375466861103));
#18737=CARTESIAN_POINT('Ctrl Pts',(88.4016815199299,3.74023087421623,2.38292577001936));
#18738=CARTESIAN_POINT('Ctrl Pts',(88.4073730454205,3.67028738199691,2.48930844301699));
#18739=CARTESIAN_POINT('Ctrl Pts',(88.4130645709112,3.59590560802497,2.59247986649357));
#18740=CARTESIAN_POINT('Ctrl Pts',(88.4187564471111,3.52151925068205,2.69565764734622));
#18741=CARTESIAN_POINT('Ctrl Pts',(88.4244483233109,3.44269430109197,2.79562346133372));
#18742=CARTESIAN_POINT('Ctrl Pts',(88.4301401995108,3.35974855879223,2.89198523884433));
#18743=CARTESIAN_POINT('Ctrl Pts',(88.4358337083682,3.27677902433815,2.98837465676445));
#18744=CARTESIAN_POINT('Ctrl Pts',(88.4415272172257,3.18968660604424,3.08115767926207));
#18745=CARTESIAN_POINT('Ctrl Pts',(88.4472207260832,3.09882761858552,3.1699773485455));
#18746=CARTESIAN_POINT('Ctrl Pts',(88.4529202880598,3.00787203335399,3.25889144747728));
#18747=CARTESIAN_POINT('Ctrl Pts',(88.4586198500364,2.91314216926165,3.34383350083435));
#18748=CARTESIAN_POINT('Ctrl Pts',(88.464319412013,2.8150294694347,3.42448508336862));
#18749=CARTESIAN_POINT('Ctrl Pts',(88.4700224264379,2.71685733889655,3.50518551973035));
#18750=CARTESIAN_POINT('Ctrl Pts',(88.4757254408628,2.61529860898164,3.58159006836629));
#18751=CARTESIAN_POINT('Ctrl Pts',(88.4814284552876,2.51077463990583,3.65342301240984));
#18752=CARTESIAN_POINT('Ctrl Pts',(88.4871396371286,2.40610097968761,3.72535883003875));
#18753=CARTESIAN_POINT('Ctrl Pts',(88.4928508189695,2.29845393850136,3.79270975882326));
#18754=CARTESIAN_POINT('Ctrl Pts',(88.4985620008105,2.18828076329471,3.85524529712369));
#18755=CARTESIAN_POINT('Ctrl Pts',(88.5010644088382,2.14000735058376,3.882645831272));
#18756=CARTESIAN_POINT('Ctrl Pts',(88.5035668168659,2.0912492400767,3.90912250451395));
#18757=CARTESIAN_POINT('Ctrl Pts',(88.5060692248936,2.04204523170036,3.93465885073787));
#18758=CARTESIAN_POINT('Ctrl Pts',(88.5117803174121,1.92974993812405,3.99293888910686));
#18759=CARTESIAN_POINT('Ctrl Pts',(88.5174914099306,1.81478444621793,4.04649764867552));
#18760=CARTESIAN_POINT('Ctrl Pts',(88.5232025024492,1.69758250154027,4.09508274036854));
#18761=CARTESIAN_POINT('Ctrl Pts',(88.5289066283904,1.58052352362568,4.14360856637862));
#18762=CARTESIAN_POINT('Ctrl Pts',(88.5346107543316,1.46123388602126,4.18717264322623));
#18763=CARTESIAN_POINT('Ctrl Pts',(88.5403148802727,1.34017199207094,4.2255683678848));
#18764=CARTESIAN_POINT('Ctrl Pts',(88.5460134670361,1.21922765922719,4.26392680712076));
#18765=CARTESIAN_POINT('Ctrl Pts',(88.5517120537995,1.09651487294086,4.29712676105349));
#18766=CARTESIAN_POINT('Ctrl Pts',(88.5574106405628,0.972511642647691,4.32500983870727));
#18767=CARTESIAN_POINT('Ctrl Pts',(88.5631051105638,0.848597994537073,4.35287277312005));
#18768=CARTESIAN_POINT('Ctrl Pts',(88.5687995805647,0.723396145975541,4.37542638874733));
#18769=CARTESIAN_POINT('Ctrl Pts',(88.5744940505657,0.597398424925402,4.39256236403044));
#18770=CARTESIAN_POINT('Ctrl Pts',(88.5801863888238,0.471447871519799,4.40969192440712));
#18771=CARTESIAN_POINT('Ctrl Pts',(88.5858787270819,0.344702432910642,4.4214078232891));
#18772=CARTESIAN_POINT('Ctrl Pts',(88.59157106534,0.217663446340325,4.42765306049686));
#18773=CARTESIAN_POINT('Ctrl Pts',(88.5972624728252,0.0906452323342379,
4.43389727652527));
#18774=CARTESIAN_POINT('Ctrl Pts',(88.6029538803103,-0.0366660356143475,
4.43467259057519));
#18775=CARTESIAN_POINT('Ctrl Pts',(88.6086452877954,-0.163765631212743,
4.42997402001789));
#18776=CARTESIAN_POINT('Ctrl Pts',(88.6143370466438,-0.29087307340105,4.42527515939078));
#18777=CARTESIAN_POINT('Ctrl Pts',(88.6200288054923,-0.41776841833657,4.41510175678727));
#18778=CARTESIAN_POINT('Ctrl Pts',(88.6257205643407,-0.543949192591837,
4.39950091213523));
#18779=CARTESIAN_POINT('Ctrl Pts',(88.6314139566265,-0.670166178569389,
4.38389559030781));
#18780=CARTESIAN_POINT('Ctrl Pts',(88.6371073489123,-0.795667789915656,
4.36285977682147));
#18781=CARTESIAN_POINT('Ctrl Pts',(88.6428007411982,-0.919959420052621,
4.3364920921704));
#18782=CARTESIAN_POINT('Ctrl Pts',(88.6485001884044,-1.04438323428812,4.31009636549734));
#18783=CARTESIAN_POINT('Ctrl Pts',(88.6541996356106,-1.1675941072211,4.27835752889874));
#18784=CARTESIAN_POINT('Ctrl Pts',(88.6598990828168,-1.2891100236671,4.24142480151199));
#18785=CARTESIAN_POINT('Ctrl Pts',(88.6656019833454,-1.41069956718979,4.20446969640855));
#18786=CARTESIAN_POINT('Ctrl Pts',(88.671304883874,-1.5305917324047,4.16231456350746));
#18787=CARTESIAN_POINT('Ctrl Pts',(88.6770077844026,-1.64832346061325,4.11515719860031));
#18788=CARTESIAN_POINT('Ctrl Pts',(88.6827188546696,-1.76622384640437,4.06793227801138));
#18789=CARTESIAN_POINT('Ctrl Pts',(88.6884299249366,-1.88195725229094,4.01569098048937));
#18790=CARTESIAN_POINT('Ctrl Pts',(88.6941409952036,-1.99508389680263,3.95867771417665));
#18791=CARTESIAN_POINT('Ctrl Pts',(88.6966446921444,-2.04467789942275,3.93368346024911));
#18792=CARTESIAN_POINT('Ctrl Pts',(88.6991483890852,-2.0937712691401,3.90777266002725));
#18793=CARTESIAN_POINT('Ctrl Pts',(88.7016520860259,-2.14232873571998,3.88096851161001));
#18794=CARTESIAN_POINT('Ctrl Pts',(88.707363269979,-2.2530931894419,3.81982555943327));
#18795=CARTESIAN_POINT('Ctrl Pts',(88.713074453932,-2.36140886395185,3.75384261937051));
#18796=CARTESIAN_POINT('Ctrl Pts',(88.718785637885,-2.46682521991997,3.68324073804127));
#18797=CARTESIAN_POINT('Ctrl Pts',(88.7244898544835,-2.572112973285,3.61272498742333));
#18798=CARTESIAN_POINT('Ctrl Pts',(88.730194071082,-2.67450811614117,3.53760172623251));
#18799=CARTESIAN_POINT('Ctrl Pts',(88.7358982876806,-2.77358454238318,3.4581379073503));
#18800=CARTESIAN_POINT('Ctrl Pts',(88.7415969642293,-2.87256474360949,3.37875126532548));
#18801=CARTESIAN_POINT('Ctrl Pts',(88.7472956407781,-2.96823233231395,3.29503270245464));
#18802=CARTESIAN_POINT('Ctrl Pts',(88.7529943173268,-3.06019045529571,3.2072922188845));
#18803=CARTESIAN_POINT('Ctrl Pts',(88.7586888761462,-3.15208213150448,3.11961513452048));
#18804=CARTESIAN_POINT('Ctrl Pts',(88.7643834349655,-3.24026938893768,3.02792218817119));
#18805=CARTESIAN_POINT('Ctrl Pts',(88.7700779937849,-3.32438910454279,2.93256305671288));
#18806=CARTESIAN_POINT('Ctrl Pts',(88.7757704191134,-3.40847730433697,2.83723965196068));
#18807=CARTESIAN_POINT('Ctrl Pts',(88.781462844442,-3.4885007287481,2.73825309203292));
#18808=CARTESIAN_POINT('Ctrl Pts',(88.7871552697705,-3.56413397044426,2.63598900618444));
#18809=CARTESIAN_POINT('Ctrl Pts',(88.7928467632138,-3.6397548305107,2.53374166159966));
#18810=CARTESIAN_POINT('Ctrl Pts',(88.7985382566571,-3.71098670015548,2.42821817914777));
#18811=CARTESIAN_POINT('Ctrl Pts',(88.8042297501004,-3.77754558299305,2.31983584945352));
#18812=CARTESIAN_POINT('Ctrl Pts',(88.8099215937074,-3.84410856080245,2.21144685163973));
#18813=CARTESIAN_POINT('Ctrl Pts',(88.8156134373145,-3.90599777110583,2.10019899691251));
#18814=CARTESIAN_POINT('Ctrl Pts',(88.8213052809215,-3.96297381061829,1.98653657815646));
#18815=CARTESIAN_POINT('Ctrl Pts',(88.8269987566779,-4.01996618814281,1.87284156643705));
#18816=CARTESIAN_POINT('Ctrl Pts',(88.8326922324343,-4.07204241335886,1.75673096999529));
#18817=CARTESIAN_POINT('Ctrl Pts',(88.8383857081907,-4.11901032098851,1.63867110049275));
#18818=CARTESIAN_POINT('Ctrl Pts',(88.8440852364875,-4.16602815860239,1.52048572556064));
#18819=CARTESIAN_POINT('Ctrl Pts',(88.8497847647842,-4.20792668839129,1.40034731138838));
#18820=CARTESIAN_POINT('Ctrl Pts',(88.855484293081,-4.24456283540365,1.2787397453392));
#18821=CARTESIAN_POINT('Ctrl Pts',(88.8611872734499,-4.28122117208105,1.15705852440604));
#18822=CARTESIAN_POINT('Ctrl Pts',(88.8668902538188,-4.31261067806839,1.03390676510222));
#18823=CARTESIAN_POINT('Ctrl Pts',(88.8725932341877,-4.3386392150289,0.909779512746562));
#18824=CARTESIAN_POINT('Ctrl Pts',(88.8783043816994,-4.36470502702142,0.785474499830974));
#18825=CARTESIAN_POINT('Ctrl Pts',(88.884015529211,-4.38539447522944,0.660191597354542));
#18826=CARTESIAN_POINT('Ctrl Pts',(88.8897266767226,-4.40066711891885,0.534432323560671));
#18827=CARTESIAN_POINT('Ctrl Pts',(88.8922294335345,-4.40735994430141,0.479321703758624));
#18828=CARTESIAN_POINT('Ctrl Pts',(88.8947321903464,-4.41301320469446,0.424119621980317));
#18829=CARTESIAN_POINT('Ctrl Pts',(88.8972349471583,-4.41762664990758,0.368868244806094));
#18830=CARTESIAN_POINT('Ctrl Pts',(88.9027593448528,-4.42781002288959,0.246910498362148));
#18831=CARTESIAN_POINT('Ctrl Pts',(88.9082837425472,-4.43294378999581,0.124525430472263));
#18832=CARTESIAN_POINT('Ctrl Pts',(88.9138081402417,-4.43299954096772,0.0020173695596966));
#18833=CARTESIAN_POINT('',(90.1638081402164,-4.43299995951971,0.000599081182435214));
#18834=CARTESIAN_POINT('Ctrl Pts',(88.9138081402808,-4.43299954096812,0.00201736869288152));
#18835=CARTESIAN_POINT('Ctrl Pts',(88.9194545459565,-4.4330565231925,-0.123196319517583));
#18836=CARTESIAN_POINT('Ctrl Pts',(88.9251009516322,-4.42780414529691,-0.248614353895448));
#18837=CARTESIAN_POINT('Ctrl Pts',(88.9307473573079,-4.41721677621254,-0.373744500891365));
#18838=CARTESIAN_POINT('Ctrl Pts',(88.9363873218383,-4.40664148468451,-0.498731905493998));
#18839=CARTESIAN_POINT('Ctrl Pts',(88.9420272863687,-4.39074333915652,-0.623431671623798));
#18840=CARTESIAN_POINT('Ctrl Pts',(88.9476672508991,-4.36954872255428,-0.747350628034997));
#18841=CARTESIAN_POINT('Ctrl Pts',(88.9533022651983,-4.34837270859601,-0.871160820024008));
#18842=CARTESIAN_POINT('Ctrl Pts',(88.9589372794975,-4.32190953918227,-0.994191164384936));
#18843=CARTESIAN_POINT('Ctrl Pts',(88.9645722937967,-4.29023743684232,-1.11595328554407));
#18844=CARTESIAN_POINT('Ctrl Pts',(88.9702041456767,-4.25858310916301,-1.23764707273667));
#18845=CARTESIAN_POINT('Ctrl Pts',(88.9758359975566,-4.22172576483138,-1.35807365737974));
#18846=CARTESIAN_POINT('Ctrl Pts',(88.9814678494366,-4.17979467064512,-1.47675506135806));
#18847=CARTESIAN_POINT('Ctrl Pts',(88.9870981372219,-4.1378752216866,-1.59540350478515));
#18848=CARTESIAN_POINT('Ctrl Pts',(88.9927284250073,-4.09088496036981,-1.71230734581001));
#18849=CARTESIAN_POINT('Ctrl Pts',(88.9983587127926,-4.03900277772549,-1.82700453243165));
#18850=CARTESIAN_POINT('Ctrl Pts',(89.0039887770741,-3.98712265463244,-1.94169716595385));
#18851=CARTESIAN_POINT('Ctrl Pts',(89.0096188413556,-3.93035116527151,-2.05418294677198));
#18852=CARTESIAN_POINT('Ctrl Pts',(89.0152489056372,-3.86891476729876,-2.16402114670296));
#18853=CARTESIAN_POINT('Ctrl Pts',(89.0208800865879,-3.80746618400578,-2.27388113198731));
#18854=CARTESIAN_POINT('Ctrl Pts',(89.0265112675387,-3.74135105259411,-2.38109213569407));
#18855=CARTESIAN_POINT('Ctrl Pts',(89.0321424484895,-3.6708407387347,-2.48523988195218));
#18856=CARTESIAN_POINT('Ctrl Pts',(89.0377792591468,-3.60025993302226,-2.58949174868885));
#18857=CARTESIAN_POINT('Ctrl Pts',(89.0434160698042,-3.52527540145758,-2.69067390452457));
#18858=CARTESIAN_POINT('Ctrl Pts',(89.0490528804616,-3.44620073351959,-2.78840267972347));
#18859=CARTESIAN_POINT('Ctrl Pts',(89.0546927901858,-3.36708259105331,-2.88618518530801));
#18860=CARTESIAN_POINT('Ctrl Pts',(89.0603326999101,-3.28387010488153,-2.98051022352839));
#18861=CARTESIAN_POINT('Ctrl Pts',(89.0659726096343,-3.19691475024118,-3.07102997049693));
#18862=CARTESIAN_POINT('Ctrl Pts',(89.0716207710934,-3.10983217148545,-3.16168215663244));
#18863=CARTESIAN_POINT('Ctrl Pts',(89.0772689325524,-3.01899608510845,-3.24851765287657));
#18864=CARTESIAN_POINT('Ctrl Pts',(89.0829170940115,-2.92479238156857,-3.33122778037144));
#18865=CARTESIAN_POINT('Ctrl Pts',(89.0862173321046,-2.86974886817328,-3.37955556197255));
#18866=CARTESIAN_POINT('Ctrl Pts',(89.0895175701976,-2.8135562087113,-3.42647568460351));
#18867=CARTESIAN_POINT('Ctrl Pts',(89.0928178082907,-2.75629587337804,-3.47193347551464));
#18868=CARTESIAN_POINT('Ctrl Pts',(89.0985282426873,-2.6572177525789,-3.5505895377424));
#18869=CARTESIAN_POINT('Ctrl Pts',(89.104238677084,-2.55461701880162,-3.6251226509496));
#18870=CARTESIAN_POINT('Ctrl Pts',(89.1099491114806,-2.44887108704103,-3.69520221355401));
#18871=CARTESIAN_POINT('Ctrl Pts',(89.115652579348,-2.34325416160057,-3.76519628155511));
#18872=CARTESIAN_POINT('Ctrl Pts',(89.1213560472154,-2.23450000180226,-3.8307473894226));
#18873=CARTESIAN_POINT('Ctrl Pts',(89.1270595150828,-2.12301898023598,-3.89156516193135));
#18874=CARTESIAN_POINT('Ctrl Pts',(89.1327574445841,-2.01164621258168,-3.95232387719699));
#18875=CARTESIAN_POINT('Ctrl Pts',(89.1384553740854,-1.89755220065201,-4.00835821292962));
#18876=CARTESIAN_POINT('Ctrl Pts',(89.1441533035867,-1.78117577892564,-4.05942136819629));
#18877=CARTESIAN_POINT('Ctrl Pts',(89.1498471178977,-1.66488340722561,-4.11044764434706));
#18878=CARTESIAN_POINT('Ctrl Pts',(89.1555409322086,-1.54631227093223,-4.15650972592692));
#18879=CARTESIAN_POINT('Ctrl Pts',(89.1612347465196,-1.42592483029627,-4.19740722093348));
#18880=CARTESIAN_POINT('Ctrl Pts',(89.1669264337978,-1.30558236268251,-4.23828943790156));
#18881=CARTESIAN_POINT('Ctrl Pts',(89.1726181210759,-1.18342531725983,-4.27401077616654));
#18882=CARTESIAN_POINT('Ctrl Pts',(89.1783098083541,-1.05993480737755,-4.30441949676255));
#18883=CARTESIAN_POINT('Ctrl Pts',(89.1840005679819,-0.936464424393002,
-4.33482326124321));
#18884=CARTESIAN_POINT('Ctrl Pts',(89.1896913276098,-0.811661396790677,
-4.35991603489422));
#18885=CARTESIAN_POINT('Ctrl Pts',(89.1953820872377,-0.686020105580647,
-4.37959648994506));
#18886=CARTESIAN_POINT('Ctrl Pts',(89.2010732020358,-0.560370972878362,
-4.39927817328745));
#18887=CARTESIAN_POINT('Ctrl Pts',(89.2067643168339,-0.433883866991581,
-4.41354680440245));
#18888=CARTESIAN_POINT('Ctrl Pts',(89.212455431632,-0.30706090971149,-4.42235260893194));
#18889=CARTESIAN_POINT('Ctrl Pts',(89.2181481843615,-0.180201452148253,
-4.43116094781614));
#18890=CARTESIAN_POINT('Ctrl Pts',(89.2238409370909,-0.0530063490580594,
-4.43450330477294));
#18891=CARTESIAN_POINT('Ctrl Pts',(89.2295336898204,0.0740201563008517,
-4.4323819799811));
#18892=CARTESIAN_POINT('Ctrl Pts',(89.2352325076746,0.20118199716931,-4.43025839510527));
#18893=CARTESIAN_POINT('Ctrl Pts',(89.2409313255287,0.328174482094933,-4.42265951275499));
#18894=CARTESIAN_POINT('Ctrl Pts',(89.2466301433829,0.454496060127244,-4.40963970538737));
#18895=CARTESIAN_POINT('Ctrl Pts',(89.2523324195372,0.580894295799256,-4.39661199701252));
#18896=CARTESIAN_POINT('Ctrl Pts',(89.2580346956914,0.706620419135217,-4.37815686817547));
#18897=CARTESIAN_POINT('Ctrl Pts',(89.2637369718457,0.83118220849259,-4.35437999447515));
#18898=CARTESIAN_POINT('Ctrl Pts',(89.2694474307545,0.955922743761389,-4.33056900100999));
#18899=CARTESIAN_POINT('Ctrl Pts',(89.2751578896633,1.07949522109567,-4.30142110549928));
#18900=CARTESIAN_POINT('Ctrl Pts',(89.2808683485721,1.20142136408789,-4.26709218390149));
#18901=CARTESIAN_POINT('Ctrl Pts',(89.2833791221891,1.2550298302263,-4.25199844940059));
#18902=CARTESIAN_POINT('Ctrl Pts',(89.2858898958061,1.30832027256013,-4.23590376169526));
#18903=CARTESIAN_POINT('Ctrl Pts',(89.2884006694231,1.36125330380707,-4.21882429627904));
#18904=CARTESIAN_POINT('Ctrl Pts',(89.2941122456653,1.48166680570748,-4.17997146293647));
#18905=CARTESIAN_POINT('Ctrl Pts',(89.2998238219076,1.60060131848022,-4.13589934475267));
#18906=CARTESIAN_POINT('Ctrl Pts',(89.3055353981499,1.71757231989815,-4.08673883749864));
#18907=CARTESIAN_POINT('Ctrl Pts',(89.3112400023538,1.83440053650861,-4.03763833976386));
#18908=CARTESIAN_POINT('Ctrl Pts',(89.3169446065577,1.94926964544813,-3.98346196360719));
#18909=CARTESIAN_POINT('Ctrl Pts',(89.3226492107615,2.06171033532708,-3.92439033395067));
#18910=CARTESIAN_POINT('Ctrl Pts',(89.3283482698448,2.17404172802027,-3.8653761244584));
#18911=CARTESIAN_POINT('Ctrl Pts',(89.3340473289281,2.28394904745643,-3.80147631458369));
#18912=CARTESIAN_POINT('Ctrl Pts',(89.3397463880114,2.39098346962001,-3.73291937335966));
#18913=CARTESIAN_POINT('Ctrl Pts',(89.3454413239051,2.4979404538748,-3.66441203212462));
#18914=CARTESIAN_POINT('Ctrl Pts',(89.3511362597987,2.60202834278606,-3.5912544801427));
#18915=CARTESIAN_POINT('Ctrl Pts',(89.3568311956924,2.70282383793958,-3.51372057811454));
#18916=CARTESIAN_POINT('Ctrl Pts',(89.36252398868,2.80358140548796,-3.43621585075551));
#18917=CARTESIAN_POINT('Ctrl Pts',(89.3682167816676,2.90104872678693,-3.35433829062534));
#18918=CARTESIAN_POINT('Ctrl Pts',(89.3739095746552,2.99483265306231,-3.26840425592548));
#18919=CARTESIAN_POINT('Ctrl Pts',(89.3796014297969,3.08860112912376,-3.18248437822748));
#18920=CARTESIAN_POINT('Ctrl Pts',(89.3852932849386,3.178687123026,-3.09250962474938));
#18921=CARTESIAN_POINT('Ctrl Pts',(89.3909851400803,3.26473208148281,-2.99883534661991));
#18922=CARTESIAN_POINT('Ctrl Pts',(89.3966773390632,3.35078223785883,-2.90515540968904));
#18923=CARTESIAN_POINT('Ctrl Pts',(89.4023695380461,3.43279060328041,-2.80777579755594));
#18924=CARTESIAN_POINT('Ctrl Pts',(89.408061737029,3.51043723352108,-2.70708688990747));
#18925=CARTESIAN_POINT('Ctrl Pts',(89.4137555614725,3.58810603648166,-2.60636922960173));
#18926=CARTESIAN_POINT('Ctrl Pts',(89.4194493859159,3.66141038284046,-2.5023407097677));
#18927=CARTESIAN_POINT('Ctrl Pts',(89.4251432103594,3.73007248579902,-2.39542235329913));
#18928=CARTESIAN_POINT('Ctrl Pts',(89.4308430754453,3.79880743315509,-2.2883905659433));
#18929=CARTESIAN_POINT('Ctrl Pts',(89.4365429405311,3.86289008791965,-2.17846315672718));
#18930=CARTESIAN_POINT('Ctrl Pts',(89.442242805617,3.9220874885155,-2.06608778429915));
#18931=CARTESIAN_POINT('Ctrl Pts',(89.4479461164316,3.981320675605,-1.95364447779781));
#18932=CARTESIAN_POINT('Ctrl Pts',(89.4536494272463,4.03566255485428,-1.83875062019934));
#18933=CARTESIAN_POINT('Ctrl Pts',(89.4593527380609,4.08492802804647,-1.72187456154053));
#18934=CARTESIAN_POINT('Ctrl Pts',(89.4650642035028,4.13426394130113,-1.60483139280766));
#18935=CARTESIAN_POINT('Ctrl Pts',(89.4707756689446,4.17850881666604,-1.48580073711594));
#18936=CARTESIAN_POINT('Ctrl Pts',(89.4764871343865,4.21752706231804,-1.36526718213504));
#18937=CARTESIAN_POINT('Ctrl Pts',(89.4789859331095,4.23459776744642,-1.3125330640123));
#18938=CARTESIAN_POINT('Ctrl Pts',(89.4814847318325,4.25066869432302,-1.25951142258196));
#18939=CARTESIAN_POINT('Ctrl Pts',(89.4839835305555,4.26573157368928,-1.20624340049196));
#18940=CARTESIAN_POINT('Ctrl Pts',(89.4896968642443,4.30017182505524,-1.08444968323914));
#18941=CARTESIAN_POINT('Ctrl Pts',(89.4954101979331,4.32944464107065,-0.960992981776088));
#18942=CARTESIAN_POINT('Ctrl Pts',(89.5011235316219,4.35339047025895,-0.836349456542256));
#18943=CARTESIAN_POINT('Ctrl Pts',(89.5068299103414,4.37730714965236,-0.711857662667029));
#18944=CARTESIAN_POINT('Ctrl Pts',(89.512536289061,4.3959096689628,-0.586182307686195));
#18945=CARTESIAN_POINT('Ctrl Pts',(89.5182426677805,4.40908830538804,-0.459814435713356));
#18946=CARTESIAN_POINT('Ctrl Pts',(89.5239435161333,4.4222541696689,-0.333569033824196));
#18947=CARTESIAN_POINT('Ctrl Pts',(89.5296443644861,4.43000656996436,-0.20663284490648));
#18948=CARTESIAN_POINT('Ctrl Pts',(89.5353452128389,4.43228696478374,-0.0795063633183393));
#18949=CARTESIAN_POINT('Ctrl Pts',(89.5410419504645,4.43456571527229,0.0475284508126489));
#18950=CARTESIAN_POINT('Ctrl Pts',(89.5467386880903,4.43138030645747,0.174752887121412));
#18951=CARTESIAN_POINT('Ctrl Pts',(89.5524354257159,4.42272412725664,0.301662550181467));
#18952=CARTESIAN_POINT('Ctrl Pts',(89.5581300321501,4.41407118639619,0.428524735402003));
#18953=CARTESIAN_POINT('Ctrl Pts',(89.5638246385843,4.39995157178336,0.555071984286092));
#18954=CARTESIAN_POINT('Ctrl Pts',(89.5695192450185,4.38041075552766,0.680801448924437));
#18955=CARTESIAN_POINT('Ctrl Pts',(89.5752129203096,4.36087313445245,0.806510355141445));
#18956=CARTESIAN_POINT('Ctrl Pts',(89.5809065956008,4.33591613620271,0.931401349165811));
#18957=CARTESIAN_POINT('Ctrl Pts',(89.5866002708919,4.30563686279154,1.05497877029381));
#18958=CARTESIAN_POINT('Ctrl Pts',(89.5922942947075,4.27535573590846,1.17856375591236));
#18959=CARTESIAN_POINT('Ctrl Pts',(89.5979883185231,4.23975178081076,1.30083462135255));
#18960=CARTESIAN_POINT('Ctrl Pts',(89.6036823423387,4.19897265471482,1.42130842710413));
#18961=CARTESIAN_POINT('Ctrl Pts',(89.6093779942809,4.15818186839686,1.54181668065919));
#18962=CARTESIAN_POINT('Ctrl Pts',(89.6150736462231,4.11221309507761,1.66052647469331));
#18963=CARTESIAN_POINT('Ctrl Pts',(89.6207692981654,4.0612628651163,1.77697297121462));
#18964=CARTESIAN_POINT('Ctrl Pts',(89.6264709847466,4.01025865252979,1.89354284475666));
#18965=CARTESIAN_POINT('Ctrl Pts',(89.6321726713278,3.95426260526756,2.00784426720237));
#18966=CARTESIAN_POINT('Ctrl Pts',(89.637874357909,3.89351827117598,2.11943494168111));
#18967=CARTESIAN_POINT('Ctrl Pts',(89.6435794892293,3.83273723770091,2.23109303494082));
#18968=CARTESIAN_POINT('Ctrl Pts',(89.6492846205497,3.76720240764115,2.3400367764139));
#18969=CARTESIAN_POINT('Ctrl Pts',(89.65498975187,3.69720108618562,2.44585222945047));
#18970=CARTESIAN_POINT('Ctrl Pts',(89.6607030204235,3.62709992179128,2.55181860714937));
#18971=CARTESIAN_POINT('Ctrl Pts',(89.666416288977,3.55251977905433,2.6546474649165));
#18972=CARTESIAN_POINT('Ctrl Pts',(89.6721295575305,3.47378892519854,2.75395706269506));
#18973=CARTESIAN_POINT('Ctrl Pts',(89.6746085022496,3.43962819346187,2.79704675831558));
#18974=CARTESIAN_POINT('Ctrl Pts',(89.6770874469687,3.40468651924392,2.83947436736873));
#18975=CARTESIAN_POINT('Ctrl Pts',(89.6795663916878,3.36899283726742,2.88121090211058));
#18976=CARTESIAN_POINT('Ctrl Pts',(89.6852710062034,3.28685357262487,2.9772561426851));
#18977=CARTESIAN_POINT('Ctrl Pts',(89.6909756207189,3.20047554896026,3.06993611006877));
#18978=CARTESIAN_POINT('Ctrl Pts',(89.6966802352345,3.11016511761852,3.15885452991254));
#18979=CARTESIAN_POINT('Ctrl Pts',(89.7023778793997,3.01996503472333,3.2476643021798));
#18980=CARTESIAN_POINT('Ctrl Pts',(89.7080755235648,2.92584238566442,3.33272139209893));
#18981=CARTESIAN_POINT('Ctrl Pts',(89.71377316773,2.82814359689021,3.41366266572561));
#18982=CARTESIAN_POINT('Ctrl Pts',(89.7194652764114,2.73053972630343,3.49452530174505));
#18983=CARTESIAN_POINT('Ctrl Pts',(89.7251573850928,2.6293669355431,3.57127982403108));
#18984=CARTESIAN_POINT('Ctrl Pts',(89.7308494937743,2.52500794957209,3.64360039721671));
#18985=CARTESIAN_POINT('Ctrl Pts',(89.736537496815,2.4207242363198,3.71586880655547));
#18986=CARTESIAN_POINT('Ctrl Pts',(89.7422254998558,2.31325922946158,3.78370940462262));
#18987=CARTESIAN_POINT('Ctrl Pts',(89.7479135028966,2.20302774130567,3.84683737257473));
#18988=CARTESIAN_POINT('Ctrl Pts',(89.7535994139857,2.09283679443274,3.90994212312448));
#18989=CARTESIAN_POINT('Ctrl Pts',(89.7592853250749,1.97988173575953,3.96833749078323));
#18990=CARTESIAN_POINT('Ctrl Pts',(89.764971236164,1.86460500917239,4.02178283349179));
#18991=CARTESIAN_POINT('Ctrl Pts',(89.7706562430049,1.74934661540412,4.07521967662011));
#18992=CARTESIAN_POINT('Ctrl Pts',(89.7763412498458,1.63176765101383,4.12370789224967));
#18993=CARTESIAN_POINT('Ctrl Pts',(89.7820262566867,1.5123332276658,4.16705378037024));
#18994=CARTESIAN_POINT('Ctrl Pts',(89.7877116480865,1.39289072524838,4.21040260059722));
#18995=CARTESIAN_POINT('Ctrl Pts',(89.7933970394862,1.27159289042968,4.2486082649287));
#18996=CARTESIAN_POINT('Ctrl Pts',(89.799082430886,1.14892228474801,4.28152619793566));
#18997=CARTESIAN_POINT('Ctrl Pts',(89.804769495616,1.02621557452629,4.31445381938285));
#18998=CARTESIAN_POINT('Ctrl Pts',(89.8104565603461,0.902135676053021,4.34209050993948));
#18999=CARTESIAN_POINT('Ctrl Pts',(89.8161436250761,0.777177172513956,4.36434240665455));
#19000=CARTESIAN_POINT('Ctrl Pts',(89.8218368387783,0.652083561253556,4.38661836258108));
#19001=CARTESIAN_POINT('Ctrl Pts',(89.8275300524805,0.526109842569052,4.40349783003496));
#19002=CARTESIAN_POINT('Ctrl Pts',(89.8332232661827,0.399757893981526,4.41493857558624));
#19003=CARTESIAN_POINT('Ctrl Pts',(89.838919978335,0.273328302781571,4.4263863514159));
#19004=CARTESIAN_POINT('Ctrl Pts',(89.8446166904872,0.146520417739216,4.43238872920634));
#19005=CARTESIAN_POINT('Ctrl Pts',(89.8503134026395,0.019836724045662,4.43295561723543));
#19006=CARTESIAN_POINT('Ctrl Pts',(89.8560184073785,-0.107031380496429,
4.43352333047176));
#19007=CARTESIAN_POINT('Ctrl Pts',(89.8617234121176,-0.233774533772461,
4.42863977056217));
#19008=CARTESIAN_POINT('Ctrl Pts',(89.8674284168566,-0.35989438068452,4.41836678363756));
#19009=CARTESIAN_POINT('Ctrl Pts',(89.8700020288445,-0.416788908343833,
4.41373248734688));
#19010=CARTESIAN_POINT('Ctrl Pts',(89.8725756408324,-0.473556712224774,
4.40800211356086));
#19011=CARTESIAN_POINT('Ctrl Pts',(89.8751492528202,-0.530152790862976,
4.40118472894972));
#19012=CARTESIAN_POINT('Ctrl Pts',(89.8808663150511,-0.655876211923623,
4.38604048333019));
#19013=CARTESIAN_POINT('Ctrl Pts',(89.886583377282,-0.781143059404232,4.36548164320263));
#19014=CARTESIAN_POINT('Ctrl Pts',(89.8923004395129,-0.905452013692984,
4.33954440591398));
#19015=CARTESIAN_POINT('Ctrl Pts',(89.8980104951791,-1.02960862072852,4.31363895609293));
#19016=CARTESIAN_POINT('Ctrl Pts',(89.9037205508453,-1.15280928364401,4.2823683039651));
#19017=CARTESIAN_POINT('Ctrl Pts',(89.9094306065115,-1.27455813693656,4.24582036308283));
#19018=CARTESIAN_POINT('Ctrl Pts',(89.915135076565,-1.39618789472747,4.20930817362847));
#19019=CARTESIAN_POINT('Ctrl Pts',(89.9208395466184,-1.51636828961105,4.1675290818621));
#19020=CARTESIAN_POINT('Ctrl Pts',(89.9265440166719,-1.63461443897412,4.12062187489914));
#19021=CARTESIAN_POINT('Ctrl Pts',(89.9322443170708,-1.75277415689164,4.0737489545301));
#19022=CARTESIAN_POINT('Ctrl Pts',(89.9379446174698,-1.86900207437685,4.02175552597497));
#19023=CARTESIAN_POINT('Ctrl Pts',(89.9436449178687,-1.98282969524079,3.96482980715078));
#19024=CARTESIAN_POINT('Ctrl Pts',(89.9493429872033,-2.09661276463729,3.90792636872119));
#19025=CARTESIAN_POINT('Ctrl Pts',(89.9550410565379,-2.20799705008679,3.84609465699794));
#19026=CARTESIAN_POINT('Ctrl Pts',(89.9607391258725,-2.3165355321143,3.77957036294496));
#19027=CARTESIAN_POINT('Ctrl Pts',(89.9664362008577,-2.42505507348567,3.71305767780483));
#19028=CARTESIAN_POINT('Ctrl Pts',(89.9721332758429,-2.53072945987447,3.64185424734687));
#19029=CARTESIAN_POINT('Ctrl Pts',(89.9778303508282,-2.63313816388875,3.56624065506979));
#19030=CARTESIAN_POINT('Ctrl Pts',(89.9835277076911,-2.735551934843,3.49062332161136));
#19031=CARTESIAN_POINT('Ctrl Pts',(89.9892250645541,-2.83469938168904,3.41059562899386));
#19032=CARTESIAN_POINT('Ctrl Pts',(89.9949224214171,-2.93019115869967,3.3264799373329));
#19033=CARTESIAN_POINT('Ctrl Pts',(90.0006213362723,-3.02570904877428,3.24234124349827));
#19034=CARTESIAN_POINT('Ctrl Pts',(90.0063202511275,-3.11756898153019,3.15411258987488));
#19035=CARTESIAN_POINT('Ctrl Pts',(90.0120191659827,-3.20541710812029,3.06215449691386));
#19036=CARTESIAN_POINT('Ctrl Pts',(90.0177239928781,-3.29335636814127,2.97010100685293));
#19037=CARTESIAN_POINT('Ctrl Pts',(90.0234288197736,-3.37727523692711,2.87431064087765));
#19038=CARTESIAN_POINT('Ctrl Pts',(90.0291336466691,-3.45685875146728,2.77517865594344));
#19039=CARTESIAN_POINT('Ctrl Pts',(90.0348418523481,-3.53648940073688,2.67598795835606));
#19040=CARTESIAN_POINT('Ctrl Pts',(90.0405500580272,-3.61177934480988,2.57345201936962));
#19041=CARTESIAN_POINT('Ctrl Pts',(90.0462582637062,-3.68245661183773,2.46799560411533));
#19042=CARTESIAN_POINT('Ctrl Pts',(90.0519744799272,-3.75323306296053,2.36239119786559));
#19043=CARTESIAN_POINT('Ctrl Pts',(90.0576906961483,-3.81938370456455,2.25385847099838));
#19044=CARTESIAN_POINT('Ctrl Pts',(90.0634069123693,-3.88068202871538,2.14284763620876));
#19045=CARTESIAN_POINT('Ctrl Pts',(90.0658486462304,-3.90686616659947,2.09542834628483));
#19046=CARTESIAN_POINT('Ctrl Pts',(90.0682903800915,-3.93216552110533,2.04755715069785));
#19047=CARTESIAN_POINT('Ctrl Pts',(90.0707321139525,-3.95656513489585,1.99927020017969));
#19048=CARTESIAN_POINT('Ctrl Pts',(90.0767804072464,-4.01700416259418,1.87966107993336));
#19049=CARTESIAN_POINT('Ctrl Pts',(90.0828287005402,-4.07208307882196,1.7571757525736));
#19050=CARTESIAN_POINT('Ctrl Pts',(90.0888769938341,-4.12153699335669,1.63230567369972));
#19051=CARTESIAN_POINT('Ctrl Pts',(90.0951212560326,-4.1725932490797,1.50338971751872));
#19052=CARTESIAN_POINT('Ctrl Pts',(90.1013655182312,-4.21765361423013,1.37193212879298));
#19053=CARTESIAN_POINT('Ctrl Pts',(90.1076097804297,-4.25647749947866,1.23850244102784));
#19054=CARTESIAN_POINT('Ctrl Pts',(90.113632853541,-4.29392613502294,1.10979920290736));
#19055=CARTESIAN_POINT('Ctrl Pts',(90.1196559266522,-4.32557242099588,0.979261542044126));
#19056=CARTESIAN_POINT('Ctrl Pts',(90.1256789997635,-4.35124866791305,0.847421990501147));
#19057=CARTESIAN_POINT('Ctrl Pts',(90.1316932308378,-4.37688722139333,0.715775983047038));
#19058=CARTESIAN_POINT('Ctrl Pts',(90.137707461912,-4.39657313467367,0.582832213013575));
#19059=CARTESIAN_POINT('Ctrl Pts',(90.1437216929862,-4.41018873685979,0.449137290007243));
#19060=CARTESIAN_POINT('Ctrl Pts',(90.1497248105176,-4.42377917912487,0.315689418410002));
#19061=CARTESIAN_POINT('Ctrl Pts',(90.1557279280489,-4.43132164108185,0.181493486475357));
#19062=CARTESIAN_POINT('Ctrl Pts',(90.1617310455803,-4.43274972705193,0.0471047483914331));
#19063=CARTESIAN_POINT('Ctrl Pts',(90.162423410459,-4.43291443423355,0.0316051280925057));
#19064=CARTESIAN_POINT('Ctrl Pts',(90.1631157753377,-4.43299786430703,0.0161029527467754));
#19065=CARTESIAN_POINT('Ctrl Pts',(90.1638081402164,-4.43299995951971,0.000599081182447127));
#19066=CARTESIAN_POINT('',(90.4430005297901,-0.73483653948465,-4.3716706486466));
#19067=CARTESIAN_POINT('Ctrl Pts',(90.1638081402416,-4.43299995951978,0.000599080619067216));
#19068=CARTESIAN_POINT('Ctrl Pts',(90.1697491429294,-4.43301793797712,-0.13243560306544));
#19069=CARTESIAN_POINT('Ctrl Pts',(90.1756901456173,-4.42704301383578,-0.265377958426872));
#19070=CARTESIAN_POINT('Ctrl Pts',(90.1816311483051,-4.41512607119674,-0.39768175145319));
#19071=CARTESIAN_POINT('Ctrl Pts',(90.1875786320771,-4.40319612827599,-0.530129875675138));
#19072=CARTESIAN_POINT('Ctrl Pts',(90.1935261158492,-4.38531126751376,-0.661937704319379));
#19073=CARTESIAN_POINT('Ctrl Pts',(90.1994735996212,-4.36157388853184,-0.792566851992466));
#19074=CARTESIAN_POINT('Ctrl Pts',(90.2054333755474,-4.33778744955514,-0.923465981676113));
#19075=CARTESIAN_POINT('Ctrl Pts',(90.2113931514737,-4.30812437494094,-1.05318122000487));
#19076=CARTESIAN_POINT('Ctrl Pts',(90.2173529273999,-4.27273795706517,-1.18118556977917));
#19077=CARTESIAN_POINT('Ctrl Pts',(90.2233190998679,-4.23731355945599,-1.30932730478125));
#19078=CARTESIAN_POINT('Ctrl Pts',(90.229285272336,-4.19615366813219,-1.43575415893636));
#19079=CARTESIAN_POINT('Ctrl Pts',(90.235251444804,-4.14946055740378,-1.55995707714998));
#19080=CARTESIAN_POINT('Ctrl Pts',(90.2412300433691,-4.10267019619687,-1.68441868006116));
#19081=CARTESIAN_POINT('Ctrl Pts',(90.2472086419342,-4.05032370960136,-1.80664676772079));
#19082=CARTESIAN_POINT('Ctrl Pts',(90.2531872404993,-3.99267099489296,-1.92615350544563));
#19083=CARTESIAN_POINT('Ctrl Pts',(90.2575631520279,-3.95047328313869,-2.0136239896494));
#19084=CARTESIAN_POINT('Ctrl Pts',(90.2619390635564,-3.90543389479463,-2.09963708311972));
#19085=CARTESIAN_POINT('Ctrl Pts',(90.266314975085,-3.85766565530893,-2.1840111473731));
#19086=CARTESIAN_POINT('Ctrl Pts',(90.2719042780933,-3.79665181558217,-2.29178119895709));
#19087=CARTESIAN_POINT('Ctrl Pts',(90.2774935811017,-3.73100228864556,-2.39719699742482));
#19088=CARTESIAN_POINT('Ctrl Pts',(90.2830828841101,-3.66092610540627,-2.4998218038002));
#19089=CARTESIAN_POINT('Ctrl Pts',(90.288665249716,-3.59093690021812,-2.60231923300912));
#19090=CARTESIAN_POINT('Ctrl Pts',(90.294247615322,-3.51653219252369,-2.70203221462205));
#19091=CARTESIAN_POINT('Ctrl Pts',(90.2998299809279,-3.4379671796562,-2.79854795771071));
#19092=CARTESIAN_POINT('Ctrl Pts',(90.3054069451015,-3.35947818538567,-2.89497031328366));
#19093=CARTESIAN_POINT('Ctrl Pts',(90.3109839092751,-3.27683715086819,-2.9882012592045));
#19094=CARTESIAN_POINT('Ctrl Pts',(90.3165608734487,-3.19034249513677,-3.07785700832974));
#19095=CARTESIAN_POINT('Ctrl Pts',(90.3221341145495,-3.10390558155529,-3.16745290502057));
#19096=CARTESIAN_POINT('Ctrl Pts',(90.3277073556503,-3.0136204505536,-3.25347805099511));
#19097=CARTESIAN_POINT('Ctrl Pts',(90.3332805967511,-2.91982526417337,-3.33558232197841));
#19098=CARTESIAN_POINT('Ctrl Pts',(90.3388519367764,-2.82606207205449,-3.41765858656176));
#19099=CARTESIAN_POINT('Ctrl Pts',(90.3444232768016,-2.7287915173788,-3.49581635919019));
#19100=CARTESIAN_POINT('Ctrl Pts',(90.3499946168269,-2.62838755126709,-3.56974339138602));
#19101=CARTESIAN_POINT('Ctrl Pts',(90.3555654327219,-2.52799303077463,-3.64366346881079));
#19102=CARTESIAN_POINT('Ctrl Pts',(90.3611362486169,-2.42446602116187,-3.71335334986336));
#19103=CARTESIAN_POINT('Ctrl Pts',(90.366707064512,-2.31821176461007,-3.77854247222702));
#19104=CARTESIAN_POINT('Ctrl Pts',(90.3722787325905,-2.21194125404261,-3.84374156675602));
#19105=CARTESIAN_POINT('Ctrl Pts',(90.3778504006691,-2.10294302376899,-3.90443831706234));
#19106=CARTESIAN_POINT('Ctrl Pts',(90.3834220687476,-1.99164869650006,-3.96040710908988));
#19107=CARTESIAN_POINT('Ctrl Pts',(90.3889990417093,-1.88024840394588,-4.01642918998808));
#19108=CARTESIAN_POINT('Ctrl Pts',(90.394576014671,-1.76654802370243,-4.06771413882168));
#19109=CARTESIAN_POINT('Ctrl Pts',(90.4001529876326,-1.65100105872653,-4.1140836773313));
#19110=CARTESIAN_POINT('Ctrl Pts',(90.4057328907888,-1.53539338427969,-4.16047757883611));
#19111=CARTESIAN_POINT('Ctrl Pts',(90.4113127939449,-1.4179375872935,-4.2019507919376));
#19112=CARTESIAN_POINT('Ctrl Pts',(90.4168926971011,-1.29910262865179,-4.23837484895213));
#19113=CARTESIAN_POINT('Ctrl Pts',(90.4224806058266,-1.18009717574056,-4.27485116409899));
#19114=CARTESIAN_POINT('Ctrl Pts',(90.4280685145522,-1.05970901435191,-4.30626375853715));
#19115=CARTESIAN_POINT('Ctrl Pts',(90.4336564232778,-0.938417771461562,
-4.33253518003087));
#19116=CARTESIAN_POINT('Ctrl Pts',(90.4367711254486,-0.870809992580504,
-4.34717887905574));
#19117=CARTESIAN_POINT('Ctrl Pts',(90.4398858276193,-0.802921749507619,
-4.36022616800192));
#19118=CARTESIAN_POINT('Ctrl Pts',(90.4430005297901,-0.734836539484649,
-4.3716706486466));
#19119=CARTESIAN_POINT('',(90.4430005297901,-3.92880598357857,-2.05328335682078));
#19120=CARTESIAN_POINT('Origin',(90.4430005297901,0.,0.));
#19121=CARTESIAN_POINT('',(90.3471929085019,-4.43299985814068,-0.00112148327145838));
#19122=CARTESIAN_POINT('Ctrl Pts',(90.4430005297901,-3.92880598357866,-2.05328335682061));
#19123=CARTESIAN_POINT('Ctrl Pts',(90.4110646596396,-4.25841379539657,-1.42260316404407));
#19124=CARTESIAN_POINT('Ctrl Pts',(90.379128789489,-4.43043959253044,-0.713287670544325));
#19125=CARTESIAN_POINT('Ctrl Pts',(90.3471929193385,-4.43169289886078,-0.00112139428608522));
#19126=CARTESIAN_POINT('',(89.0971929193785,-4.43299919376221,0.0026735937699673));
#19127=CARTESIAN_POINT('Ctrl Pts',(90.3471929085019,-4.43299985814068,-0.00112148327145838));
#19128=CARTESIAN_POINT('Ctrl Pts',(90.3465316387426,-4.43300358982262,0.0136291117150349));
#19129=CARTESIAN_POINT('Ctrl Pts',(90.3458703689832,-4.43293369846719,0.0283807072529051));
#19130=CARTESIAN_POINT('Ctrl Pts',(90.3452090992239,-4.4327901571182,0.0431326205558783));
#19131=CARTESIAN_POINT('Ctrl Pts',(90.3394423924397,-4.43153838224206,0.171778997204193));
#19132=CARTESIAN_POINT('Ctrl Pts',(90.3336756856555,-4.42468163753682,0.300407073394231));
#19133=CARTESIAN_POINT('Ctrl Pts',(90.3279089788713,-4.41224152195584,0.428501752538767));
#19134=CARTESIAN_POINT('Ctrl Pts',(90.3221427954218,-4.39980253532841,0.556584806956697));
#19135=CARTESIAN_POINT('Ctrl Pts',(90.3163766119723,-4.3817812253595,0.684134176035194));
#19136=CARTESIAN_POINT('Ctrl Pts',(90.3106104285228,-4.35825108459229,0.810639552236455));
#19137=CARTESIAN_POINT('Ctrl Pts',(90.3048414539242,-4.33470955394638,0.937206163978292));
#19138=CARTESIAN_POINT('Ctrl Pts',(90.2990724793256,-4.30565393347754,1.06272739217585));
#19139=CARTESIAN_POINT('Ctrl Pts',(90.2933035047271,-4.27120895910102,1.18670258603206));
#19140=CARTESIAN_POINT('Ctrl Pts',(90.2875331119772,-4.23675551732975,1.31070825594247));
#19141=CARTESIAN_POINT('Ctrl Pts',(90.2817627192273,-4.19691019416052,1.43316676394973));
#19142=CARTESIAN_POINT('Ctrl Pts',(90.2759923264775,-4.15184747744202,1.55359310118779));
#19143=CARTESIAN_POINT('Ctrl Pts',(90.2702164523881,-4.10674195530944,1.67413383231083));
#19144=CARTESIAN_POINT('Ctrl Pts',(90.2644405782986,-4.05640928324267,1.79263817711511));
#19145=CARTESIAN_POINT('Ctrl Pts',(90.2586647042092,-4.0010720782519,1.90864119850564));
#19146=CARTESIAN_POINT('Ctrl Pts',(90.2549156923587,-3.96515373341394,1.98393659019094));
#19147=CARTESIAN_POINT('Ctrl Pts',(90.2511666805082,-3.9271279119575,2.05817860910029));
#19148=CARTESIAN_POINT('Ctrl Pts',(90.2474176686577,-3.88706567518093,2.13124598224377));
#19149=CARTESIAN_POINT('Ctrl Pts',(90.2416408381269,-3.82533400780438,2.24383507206739));
#19150=CARTESIAN_POINT('Ctrl Pts',(90.235864007596,-3.75864455320898,2.35385355122844));
#19151=CARTESIAN_POINT('Ctrl Pts',(90.2300871770651,-3.68723787993225,2.4608465650651));
#19152=CARTESIAN_POINT('Ctrl Pts',(90.2243153194889,-3.61589267672022,2.56774747452018));
#19153=CARTESIAN_POINT('Ctrl Pts',(90.2185434619126,-3.53983855315819,2.67162778396671));
#19154=CARTESIAN_POINT('Ctrl Pts',(90.2127716043364,-3.45936110806888,2.7720587518991));
#19155=CARTESIAN_POINT('Ctrl Pts',(90.2070034129191,-3.37893478050945,2.87242592825613));
#19156=CARTESIAN_POINT('Ctrl Pts',(90.2012352215017,-3.29409096713205,2.96934782523667));
#19157=CARTESIAN_POINT('Ctrl Pts',(90.1954670300844,-3.20515734868601,3.06242638608083));
#19158=CARTESIAN_POINT('Ctrl Pts',(90.1894823541444,-3.1128859852621,3.15899825468006));
#19159=CARTESIAN_POINT('Ctrl Pts',(90.1834976782045,-3.01621208747336,3.25143231607391));
#19160=CARTESIAN_POINT('Ctrl Pts',(90.1775130022645,-2.91554609764722,3.33932327762588));
#19161=CARTESIAN_POINT('Ctrl Pts',(90.1717470295916,-2.81855883346521,3.42400236260755));
#19162=CARTESIAN_POINT('Ctrl Pts',(90.1659810569186,-2.71786644577177,3.50446429911993));
#19163=CARTESIAN_POINT('Ctrl Pts',(90.1602150842457,-2.61387159739403,3.58038605074045));
#19164=CARTESIAN_POINT('Ctrl Pts',(90.1544486145709,-2.50986778511079,3.65631434648711));
#19165=CARTESIAN_POINT('Ctrl Pts',(90.148682144896,-2.40256125726051,3.72770144985256));
#19166=CARTESIAN_POINT('Ctrl Pts',(90.1429156752212,-2.29238516605498,3.79426662880339));
#19167=CARTESIAN_POINT('Ctrl Pts',(90.1371475287528,-2.18217703747118,3.86085116380321));
#19168=CARTESIAN_POINT('Ctrl Pts',(90.1313793822843,-2.06909801481257,3.92261078270365));
#19169=CARTESIAN_POINT('Ctrl Pts',(90.1256112358158,-1.95360712907898,3.97931001370989));
#19170=CARTESIAN_POINT('Ctrl Pts',(90.1198402318251,-1.83805902951072,4.03603733334328));
#19171=CARTESIAN_POINT('Ctrl Pts',(90.1140692278344,-1.72009703434979,4.08769910332605));
#19172=CARTESIAN_POINT('Ctrl Pts',(90.1082982238436,-1.60020115215999,4.13410755455465));
#19173=CARTESIAN_POINT('Ctrl Pts',(90.102519848168,-1.48015211903506,4.18057528636549));
#19174=CARTESIAN_POINT('Ctrl Pts',(90.0967414724924,-1.35816462678385,4.22177616058313));
#19175=CARTESIAN_POINT('Ctrl Pts',(90.0909630968168,-1.23473538928447,4.25757178664653));
#19176=CARTESIAN_POINT('Ctrl Pts',(90.0851803838934,-1.1112135058181,4.29339428090144));
#19177=CARTESIAN_POINT('Ctrl Pts',(90.0793976709699,-0.986248094925947,
4.32380335007161));
#19178=CARTESIAN_POINT('Ctrl Pts',(90.0736149580464,-0.860346192411113,
4.34871169764146));
#19179=CARTESIAN_POINT('Ctrl Pts',(90.0678235788045,-0.734255605799044,
4.37365737434599));
#19180=CARTESIAN_POINT('Ctrl Pts',(90.0620321995627,-0.607226105872629,
4.39308581009496));
#19181=CARTESIAN_POINT('Ctrl Pts',(90.0562408203209,-0.479770447597029,
4.40696146087217));
#19182=CARTESIAN_POINT('Ctrl Pts',(90.054772149389,-0.447448195403114,4.4104802711772));
#19183=CARTESIAN_POINT('Ctrl Pts',(90.0533034784572,-0.415098537276401,
4.41364223814709));
#19184=CARTESIAN_POINT('Ctrl Pts',(90.0518348075254,-0.38272982472858,4.41644731444441));
#19185=CARTESIAN_POINT('Ctrl Pts',(90.0461769990587,-0.258034787916835,
4.42725340046459));
#19186=CARTESIAN_POINT('Ctrl Pts',(90.0405191905921,-0.132649939074645,
4.43279429414113));
#19187=CARTESIAN_POINT('Ctrl Pts',(90.0348613821254,-0.00706243780706909,
4.43299437423196));
#19188=CARTESIAN_POINT('Ctrl Pts',(90.0292112553074,0.118354552376854,4.43319418267257));
#19189=CARTESIAN_POINT('Ctrl Pts',(90.0235611284893,0.243973244670051,4.42806759582563));
#19190=CARTESIAN_POINT('Ctrl Pts',(90.0179110016713,0.369300054675269,4.4175905728821));
#19191=CARTESIAN_POINT('Ctrl Pts',(90.0122670675232,0.494489503590794,4.40712503299865));
#19192=CARTESIAN_POINT('Ctrl Pts',(90.0066231333752,0.619387303110374,4.39132075383049));
#19193=CARTESIAN_POINT('Ctrl Pts',(90.0009791992271,0.74349914601596,4.37020571825555));
#19194=CARTESIAN_POINT('Ctrl Pts',(89.9953399751504,0.867507413008013,4.3491083039571));
#19195=CARTESIAN_POINT('Ctrl Pts',(89.9897007510737,0.990730627962674,4.32270901803345));
#19196=CARTESIAN_POINT('Ctrl Pts',(89.984061526997,1.11267947801103,4.29108766855364));
#19197=CARTESIAN_POINT('Ctrl Pts',(89.9784251344186,1.23456709659216,4.25948219639963));
#19198=CARTESIAN_POINT('Ctrl Pts',(89.9727887418402,1.35518122870269,4.22265997654248));
#19199=CARTESIAN_POINT('Ctrl Pts',(89.9671523492618,1.47404311377501,4.18075183414807));
#19200=CARTESIAN_POINT('Ctrl Pts',(89.961517313954,1.59287637633131,4.13885378343676));
#19201=CARTESIAN_POINT('Ctrl Pts',(89.9558822786462,1.70995784635137,4.09187238064173));
#19202=CARTESIAN_POINT('Ctrl Pts',(89.9502472433383,1.82482485428986,4.03998802611666));
#19203=CARTESIAN_POINT('Ctrl Pts',(89.9446122312962,1.93969138796984,3.98810388580973));
#19204=CARTESIAN_POINT('Ctrl Pts',(89.9389772192541,2.05234310615974,3.93131700221962));
#19205=CARTESIAN_POINT('Ctrl Pts',(89.933342207212,2.16233880620666,3.86985527987453));
#19206=CARTESIAN_POINT('Ctrl Pts',(89.9277058847034,2.27236008662219,3.80837926412058));
#19207=CARTESIAN_POINT('Ctrl Pts',(89.9220695621947,2.37972376492447,3.74222644710263));
#19208=CARTESIAN_POINT('Ctrl Pts',(89.916433239686,2.4840152113769,3.67166956977996));
#19209=CARTESIAN_POINT('Ctrl Pts',(89.9107910563432,2.58841510351825,3.60103932508701));
#19210=CARTESIAN_POINT('Ctrl Pts',(89.9051488730003,2.6897360476216,3.52599610595527));
#19211=CARTESIAN_POINT('Ctrl Pts',(89.8995066896574,2.7875941097298,3.44685480973593));
#19212=CARTESIAN_POINT('Ctrl Pts',(89.8938612494158,2.88550865951021,3.36766782992647));
#19213=CARTESIAN_POINT('Ctrl Pts',(89.8882158091741,2.97995604176652,3.28437833213289));
#19214=CARTESIAN_POINT('Ctrl Pts',(89.8825703689325,3.07058825043254,3.19733901804385));
#19215=CARTESIAN_POINT('Ctrl Pts',(89.8769165617387,3.16135478260924,3.11017070537465));
#19216=CARTESIAN_POINT('Ctrl Pts',(89.8712627545449,3.24829457044237,3.01924177439788));
#19217=CARTESIAN_POINT('Ctrl Pts',(89.8656089473511,3.33109881978181,2.9249392562664));
#19218=CARTESIAN_POINT('Ctrl Pts',(89.8624899470317,3.37677892016065,2.87291597813046));
#19219=CARTESIAN_POINT('Ctrl Pts',(89.8593709467124,3.42120118246359,2.81986655700101));
#19220=CARTESIAN_POINT('Ctrl Pts',(89.856251946393,3.46431945908368,2.76585966480843));
#19221=CARTESIAN_POINT('Ctrl Pts',(89.8505264815675,3.54347051738678,2.66672066835993));
#19222=CARTESIAN_POINT('Ctrl Pts',(89.8448010167419,3.61847966456172,2.56403472814382));
#19223=CARTESIAN_POINT('Ctrl Pts',(89.8390755519164,3.68901516440634,2.45818146538861));
#19224=CARTESIAN_POINT('Ctrl Pts',(89.8333569411806,3.75946622453167,2.35245492208405));
#19225=CARTESIAN_POINT('Ctrl Pts',(89.8276383304447,3.8254540750884,2.2435689281578));
#19226=CARTESIAN_POINT('Ctrl Pts',(89.8219197197089,3.8866872680214,2.13193599355148));
#19227=CARTESIAN_POINT('Ctrl Pts',(89.8162065547643,3.94786214903203,2.0204093661734));
#19228=CARTESIAN_POINT('Ctrl Pts',(89.8104933898197,4.00429119343185,1.90614135001187));
#19229=CARTESIAN_POINT('Ctrl Pts',(89.8047802248751,4.05572656226878,1.78957286862185));
#19230=CARTESIAN_POINT('Ctrl Pts',(89.7987755940578,4.10978598533994,1.66705746735772));
#19231=CARTESIAN_POINT('Ctrl Pts',(89.7927709632405,4.15832853903692,1.54200106594889));
#19232=CARTESIAN_POINT('Ctrl Pts',(89.7867663324233,4.20112131672355,1.41494476293989));
#19233=CARTESIAN_POINT('Ctrl Pts',(89.7810593649033,4.2417927584458,1.29418693176757));
#19234=CARTESIAN_POINT('Ctrl Pts',(89.7753523973833,4.27727062392836,1.17162312913266));
#19235=CARTESIAN_POINT('Ctrl Pts',(89.7696454298633,4.30740471981902,1.04773736197618));
#19236=CARTESIAN_POINT('Ctrl Pts',(89.7639392990392,4.3375343977634,0.923869757656485));
#19237=CARTESIAN_POINT('Ctrl Pts',(89.7582331682152,4.36232177096677,0.798680959789409));
#19238=CARTESIAN_POINT('Ctrl Pts',(89.7525270373911,4.3816671215063,0.672667998577801));
#19239=CARTESIAN_POINT('Ctrl Pts',(89.7468204779354,4.40101392522505,0.54664557155599));
#19240=CARTESIAN_POINT('Ctrl Pts',(89.7411139184796,4.41491783292752,0.419799250219));
#19241=CARTESIAN_POINT('Ctrl Pts',(89.7354073590239,4.42333071143737,0.2926335887334));
#19242=CARTESIAN_POINT('Ctrl Pts',(89.7296991056221,4.43174608724209,0.165430179150732));
#19243=CARTESIAN_POINT('Ctrl Pts',(89.7239908522204,4.4346671647022,0.0379076365427575));
#19244=CARTESIAN_POINT('Ctrl Pts',(89.7182825988186,4.43209789078656,-0.089427548805418));
#19245=CARTESIAN_POINT('Ctrl Pts',(89.7125683489679,4.42952591788072,-0.216896498177392));
#19246=CARTESIAN_POINT('Ctrl Pts',(89.7068540991172,4.42145208632748,-0.344177300343669));
#19247=CARTESIAN_POINT('Ctrl Pts',(89.7011398492665,4.40793240160502,-0.470766335755432));
#19248=CARTESIAN_POINT('Ctrl Pts',(89.6954221188922,4.3944044821041,-0.597432475972821));
#19249=CARTESIAN_POINT('Ctrl Pts',(89.6897043885178,4.37542415965407,-0.72340561826698));
#19250=CARTESIAN_POINT('Ctrl Pts',(89.6839866581435,4.35109871531903,-0.848191587761348));
#19251=CARTESIAN_POINT('Ctrl Pts',(89.6782610095774,4.32673958392263,-0.973150366950498));
#19252=CARTESIAN_POINT('Ctrl Pts',(89.6725353610113,4.29702064340578,-1.0969183058555));
#19253=CARTESIAN_POINT('Ctrl Pts',(89.6668097124451,4.26209932403515,-1.21901532068268));
#19254=CARTESIAN_POINT('Ctrl Pts',(89.664762836717,4.24961521848984,-1.26266407300195));
#19255=CARTESIAN_POINT('Ctrl Pts',(89.6627159609888,4.23646669626051,-1.30609945691691));
#19256=CARTESIAN_POINT('Ctrl Pts',(89.6606690852607,4.22266243405317,-1.34930017714228));
#19257=CARTESIAN_POINT('Ctrl Pts',(89.6549528626141,4.18411185906552,-1.46994498811108));
#19258=CARTESIAN_POINT('Ctrl Pts',(89.6492366399676,4.14032878566903,-1.58911792253836));
#19259=CARTESIAN_POINT('Ctrl Pts',(89.643520417321,4.09144408506085,-1.70633358368772));
#19260=CARTESIAN_POINT('Ctrl Pts',(89.6378110422421,4.04261794432972,-1.8234088300525));
#19261=CARTESIAN_POINT('Ctrl Pts',(89.6321016671633,3.98870248744607,-1.93853110344308));
#19262=CARTESIAN_POINT('Ctrl Pts',(89.6263922920844,3.92987831959161,-2.05123021457949));
#19263=CARTESIAN_POINT('Ctrl Pts',(89.6206883442447,3.87111006903579,-2.16382219577112));
#19264=CARTESIAN_POINT('Ctrl Pts',(89.614984396405,3.80744257623814,-2.27399524723275));
#19265=CARTESIAN_POINT('Ctrl Pts',(89.6092804485654,3.73910429903609,-2.38129965374579));
#19266=CARTESIAN_POINT('Ctrl Pts',(89.6035805124916,3.67081408629359,-2.48852858969508));
#19267=CARTESIAN_POINT('Ctrl Pts',(89.5978805764179,3.59785984110271,-2.59289256170049));
#19268=CARTESIAN_POINT('Ctrl Pts',(89.5921806403441,3.52051542744002,-2.69396735784916));
#19269=CARTESIAN_POINT('Ctrl Pts',(89.5864826996908,3.44319809033185,-2.79500676996558));
#19270=CARTESIAN_POINT('Ctrl Pts',(89.5807847590376,3.36149388194526,-2.89275897963081));
#19271=CARTESIAN_POINT('Ctrl Pts',(89.5750868183844,3.27571919332025,-2.9868298857674));
#19272=CARTESIAN_POINT('Ctrl Pts',(89.5693897252624,3.18995726311767,-3.08088679947362));
#19273=CARTESIAN_POINT('Ctrl Pts',(89.5636926321405,3.10012632529044,-3.17126320461502));
#19274=CARTESIAN_POINT('Ctrl Pts',(89.5579955390185,3.00658179542174,-3.25759956216822));
#19275=CARTESIAN_POINT('Ctrl Pts',(89.552298017245,2.91303022722462,-3.34394241570404));
#19276=CARTESIAN_POINT('Ctrl Pts',(89.5466004954715,2.81576480388216,-3.42624434684018));
#19277=CARTESIAN_POINT('Ctrl Pts',(89.5409029736979,2.71517601201483,-3.50418438781112));
#19278=CARTESIAN_POINT('Ctrl Pts',(89.5352037471007,2.61455712177031,-3.58214775015523));
#19279=CARTESIAN_POINT('Ctrl Pts',(89.5295045205034,2.51061319931515,-3.65574638185656));
#19280=CARTESIAN_POINT('Ctrl Pts',(89.5238052939061,2.40376542905842,-3.72470143260686));
#19281=CARTESIAN_POINT('Ctrl Pts',(89.5180999358819,2.29680270823956,-3.79373066760851));
#19282=CARTESIAN_POINT('Ctrl Pts',(89.5123945778576,2.18693023700328,-3.85810613093712));
#19283=CARTESIAN_POINT('Ctrl Pts',(89.5066892198334,2.07459590672393,-3.91759375430944));
#19284=CARTESIAN_POINT('Ctrl Pts',(89.5009803567025,1.9621925634564,-3.97711792411096));
#19285=CARTESIAN_POINT('Ctrl Pts',(89.4952714935716,1.84732470715158,-4.03174810093616));
#19286=CARTESIAN_POINT('Ctrl Pts',(89.4895626304407,1.73046099961773,-4.08129804459341));
#19287=CARTESIAN_POINT('Ctrl Pts',(89.4838455696813,1.61342948191837,-4.13091913937552));
#19288=CARTESIAN_POINT('Ctrl Pts',(89.4781285089219,1.49439676257133,-4.1754452954221));
#19289=CARTESIAN_POINT('Ctrl Pts',(89.4724114481624,1.37384783026206,-4.21473974751517));
#19290=CARTESIAN_POINT('Ctrl Pts',(89.4699697068177,1.32236170400487,-4.2315223028055));
#19291=CARTESIAN_POINT('Ctrl Pts',(89.467527965473,1.27059914564415,-4.24735116518983));
#19292=CARTESIAN_POINT('Ctrl Pts',(89.4650862241283,1.21859846425015,-4.26221852829336));
#19293=CARTESIAN_POINT('Ctrl Pts',(89.4593811640326,1.09710033218465,-4.29695570475708));
#19294=CARTESIAN_POINT('Ctrl Pts',(89.4536761039369,0.973923986759625,-4.32654844324356));
#19295=CARTESIAN_POINT('Ctrl Pts',(89.4479710438412,0.849543409472067,-4.35083497680877));
#19296=CARTESIAN_POINT('Ctrl Pts',(89.4422730385761,0.725316640187737,-4.37509147784548));
#19297=CARTESIAN_POINT('Ctrl Pts',(89.436575033311,0.599888990771536,-4.39405475140693));
#19298=CARTESIAN_POINT('Ctrl Pts',(89.4308770280459,0.473749623979258,-4.40761276586085));
#19299=CARTESIAN_POINT('Ctrl Pts',(89.4251846424056,0.347734661408601,-4.42115740880135));
#19300=CARTESIAN_POINT('Ctrl Pts',(89.4194922567652,0.221009773679086,-4.4293073572606));
#19301=CARTESIAN_POINT('Ctrl Pts',(89.4137998711249,0.0940738621422794,
-4.43200170447413));
#19302=CARTESIAN_POINT('Ctrl Pts',(89.4081116750029,-0.0327686262916659,
-4.4346940686848));
#19303=CARTESIAN_POINT('Ctrl Pts',(89.4024234788809,-0.159821430762957,
-4.43193881430123));
#19304=CARTESIAN_POINT('Ctrl Pts',(89.3967352827589,-0.286581474138729,
-4.42372694214736));
#19305=CARTESIAN_POINT('Ctrl Pts',(89.3910493038997,-0.413292106360815,
-4.41551827098702));
#19306=CARTESIAN_POINT('Ctrl Pts',(89.3853633250406,-0.539709805735858,
-4.40185723716461));
#19307=CARTESIAN_POINT('Ctrl Pts',(89.3796773461814,-0.665332790061885,
-4.38278693053501));
#19308=CARTESIAN_POINT('Ctrl Pts',(89.3739923495585,-0.790934073384423,
-4.36371991824515));
#19309=CARTESIAN_POINT('Ctrl Pts',(89.3683073529356,-0.915740519226585,
-4.3392455517671));
#19310=CARTESIAN_POINT('Ctrl Pts',(89.3626223563126,-1.03925729366832,-4.3094585828799));
#19311=CARTESIAN_POINT('Ctrl Pts',(89.3569370530937,-1.1627807294588,-4.27967000755997));
#19312=CARTESIAN_POINT('Ctrl Pts',(89.3512517498748,-1.28501396649285,-4.24456835387764));
#19313=CARTESIAN_POINT('Ctrl Pts',(89.3455664466559,-1.40547467608751,-4.20429898257447));
#19314=CARTESIAN_POINT('Ctrl Pts',(89.3398795480991,-1.52596918784376,-4.16401831138937));
#19315=CARTESIAN_POINT('Ctrl Pts',(89.3341926495423,-1.64468980337015,-4.11856716485411));
#19316=CARTESIAN_POINT('Ctrl Pts',(89.3285057509855,-1.76117210416068,-4.06813984758713));
#19317=CARTESIAN_POINT('Ctrl Pts',(89.3228128202523,-1.87777795942903,-4.01765904132816));
#19318=CARTESIAN_POINT('Ctrl Pts',(89.3171198895191,-1.99214039204563,-3.96219168483694));
#19319=CARTESIAN_POINT('Ctrl Pts',(89.3114269587859,-2.10381735312241,-3.90197918301738));
#19320=CARTESIAN_POINT('Ctrl Pts',(89.3057305967038,-2.21556162621179,-3.84173038880016));
#19321=CARTESIAN_POINT('Ctrl Pts',(89.3000342346216,-2.32461686023455,-3.77673095648576));
#19322=CARTESIAN_POINT('Ctrl Pts',(89.2943378725395,-2.43056922637755,-3.70726614040406));
#19323=CARTESIAN_POINT('Ctrl Pts',(89.2886333177804,-2.5366739763561,-3.63770141796354));
#19324=CARTESIAN_POINT('Ctrl Pts',(89.2829287630214,-2.63966662351286,-3.56365872123782));
#19325=CARTESIAN_POINT('Ctrl Pts',(89.2772242082623,-2.73916540771085,-3.48546436923407));
#19326=CARTESIAN_POINT('Ctrl Pts',(89.2746505931735,-2.7840543750618,-3.45018691592227));
#19327=CARTESIAN_POINT('Ctrl Pts',(89.2720769780847,-2.82823269625743,-3.41406495996122));
#19328=CARTESIAN_POINT('Ctrl Pts',(89.2695033629959,-2.87166780824715,-3.37713088272827));
#19329=CARTESIAN_POINT('Ctrl Pts',(89.263865417757,-2.96681987038164,-3.29622045218576));
#19330=CARTESIAN_POINT('Ctrl Pts',(89.2582274725182,-3.05871486481643,-3.21114480803611));
#19331=CARTESIAN_POINT('Ctrl Pts',(89.2525895272793,-3.14696053079779,-3.1221992917815));
#19332=CARTESIAN_POINT('Ctrl Pts',(89.24695849197,-3.23509804189223,-3.03336278815822));
#19333=CARTESIAN_POINT('Ctrl Pts',(89.2413274566606,-3.31959483180976,-2.94066613254748));
#19334=CARTESIAN_POINT('Ctrl Pts',(89.2356964213513,-3.40009127339568,-2.8444451713082));
#19335=CARTESIAN_POINT('Ctrl Pts',(89.2299254421024,-3.48258823327582,-2.7458329019632));
#19336=CARTESIAN_POINT('Ctrl Pts',(89.2241544628535,-3.56088304498919,-2.64351910899112));
#19337=CARTESIAN_POINT('Ctrl Pts',(89.2183834836047,-3.63462789400479,-2.53790643486365));
#19338=CARTESIAN_POINT('Ctrl Pts',(89.2127618304416,-3.70646456952343,-2.43502652523977));
#19339=CARTESIAN_POINT('Ctrl Pts',(89.2071401772786,-3.77398360099277,-2.32901671612977));
#19340=CARTESIAN_POINT('Ctrl Pts',(89.2015185241156,-3.8369041825518,-2.22028270585448));
#19341=CARTESIAN_POINT('Ctrl Pts',(89.1958988209634,-3.89980293853472,-2.11158641268794));
#19342=CARTESIAN_POINT('Ctrl Pts',(89.1902791178113,-3.95810621063216,-2.00016815211306));
#19343=CARTESIAN_POINT('Ctrl Pts',(89.1846594146592,-4.01157734340261,-1.88646129509695));
#19344=CARTESIAN_POINT('Ctrl Pts',(89.1790403124819,-4.06504275793361,-1.77276659796978));
#19345=CARTESIAN_POINT('Ctrl Pts',(89.1734212103047,-4.11367688690895,-1.6567841630041));
#19346=CARTESIAN_POINT('Ctrl Pts',(89.1678021081274,-4.15729003725138,-1.5389699627252));
#19347=CARTESIAN_POINT('Ctrl Pts',(89.161918009065,-4.20295998396949,-1.41559964420594));
#19348=CARTESIAN_POINT('Ctrl Pts',(89.1560339100026,-4.24312361768197,-1.29022102191266));
#19349=CARTESIAN_POINT('Ctrl Pts',(89.1501498109402,-4.27762101250791,-1.16337761425551));
#19350=CARTESIAN_POINT('Ctrl Pts',(89.1445252559786,-4.31059674781946,-1.04212919367123));
#19351=CARTESIAN_POINT('Ctrl Pts',(89.1389007010171,-4.33839540505862,-0.919542878203412));
#19352=CARTESIAN_POINT('Ctrl Pts',(89.1332761460555,-4.36092954124719,-0.796104601341791));
#19353=CARTESIAN_POINT('Ctrl Pts',(89.1276487188446,-4.38347518477421,-0.672603289180431));
#19354=CARTESIAN_POINT('Ctrl Pts',(89.1220212916337,-4.40075089815923,-0.548249555326521));
#19355=CARTESIAN_POINT('Ctrl Pts',(89.1163938644229,-4.41272106872279,-0.42353485057315));
#19356=CARTESIAN_POINT('Ctrl Pts',(89.1107598757896,-4.42470519616957,-0.298674731971114));
#19357=CARTESIAN_POINT('Ctrl Pts',(89.1051258871564,-4.43137141745617,-0.173453211240283));
#19358=CARTESIAN_POINT('Ctrl Pts',(89.0994918985232,-4.43273618773755,-0.048362071109586));
#19359=CARTESIAN_POINT('Ctrl Pts',(89.0987255721416,-4.43292182167107,-0.0313473685561952));
#19360=CARTESIAN_POINT('Ctrl Pts',(89.0979592457601,-4.43300945188702,-0.0143350705708257));
#19361=CARTESIAN_POINT('Ctrl Pts',(89.0971929193785,-4.4329991937622,0.00267359376999083));
#19362=CARTESIAN_POINT('',(87.8471929193744,-4.43299846679216,-0.00368692533081282));
#19363=CARTESIAN_POINT('Ctrl Pts',(89.0971929193385,-4.43299919376167,0.00267359465718153));
#19364=CARTESIAN_POINT('Ctrl Pts',(89.0894354468469,-4.43289535139194,0.174851205810205));
#19365=CARTESIAN_POINT('Ctrl Pts',(89.0816779743552,-4.42276034109812,0.34671858518774));
#19366=CARTESIAN_POINT('Ctrl Pts',(89.0739205018635,-4.40270237763495,0.517398080753629));
#19367=CARTESIAN_POINT('Ctrl Pts',(89.0682090089903,-4.38793456305444,0.643062041994788));
#19368=CARTESIAN_POINT('Ctrl Pts',(89.0624975161171,-4.36775959624138,0.76828670624058));
#19369=CARTESIAN_POINT('Ctrl Pts',(89.0567860232439,-4.34221203575391,0.892571362163206));
#19370=CARTESIAN_POINT('Ctrl Pts',(89.0510814865924,-4.31669559051027,1.01670464757139));
#19371=CARTESIAN_POINT('Ctrl Pts',(89.0453769499408,-4.28581964941365,1.13989981476734));
#19372=CARTESIAN_POINT('Ctrl Pts',(89.0396724132893,-4.24967050494999,1.26166144403248));
#19373=CARTESIAN_POINT('Ctrl Pts',(89.0339734060043,-4.21355639959348,1.38330505062134));
#19374=CARTESIAN_POINT('Ctrl Pts',(89.0282743987194,-4.17217937456742,1.50351750378311));
#19375=CARTESIAN_POINT('Ctrl Pts',(89.0225753914344,-4.12567662877393,1.62181421710028));
#19376=CARTESIAN_POINT('Ctrl Pts',(89.0168804916338,-4.07920739922103,1.74002566962182));
#19377=CARTESIAN_POINT('Ctrl Pts',(89.0111855918331,-4.02761994720952,1.85632376023667));
#19378=CARTESIAN_POINT('Ctrl Pts',(89.0054906920325,-3.97110094773782,1.97024015360459));
#19379=CARTESIAN_POINT('Ctrl Pts',(88.9997979116885,-3.91460298280093,2.08411415099301));
#19380=CARTESIAN_POINT('Ctrl Pts',(88.9941051313445,-3.85317729676634,2.19560785661257));
#19381=CARTESIAN_POINT('Ctrl Pts',(88.9884123510005,-3.78705809782464,2.30427428135212));
#19382=CARTESIAN_POINT('Ctrl Pts',(88.9827204938992,-3.72094962195105,2.41292308280687));
#19383=CARTESIAN_POINT('Ctrl Pts',(88.977028636798,-3.65014935461175,2.51874517459598));
#19384=CARTESIAN_POINT('Ctrl Pts',(88.9713367796967,-3.57493645903895,2.62131995640251));
#19385=CARTESIAN_POINT('Ctrl Pts',(88.9656445641558,-3.49971882699983,2.72390119776622));
#19386=CARTESIAN_POINT('Ctrl Pts',(88.9599523486148,-3.42008825004789,2.82323440055596));
#19387=CARTESIAN_POINT('Ctrl Pts',(88.9542601330738,-3.33636573433397,2.9189300585595));
#19388=CARTESIAN_POINT('Ctrl Pts',(88.9485662774683,-3.25261909614423,3.01465328878989));
#19389=CARTESIAN_POINT('Ctrl Pts',(88.9428724218627,-3.16477843645335,3.10673658900602));
#19390=CARTESIAN_POINT('Ctrl Pts',(88.9371785662572,-3.07320298910899,3.19482587752941));
#19391=CARTESIAN_POINT('Ctrl Pts',(88.931478648168,-2.98153003759703,3.28300895836287));
#19392=CARTESIAN_POINT('Ctrl Pts',(88.9257787300788,-2.88611464662167,3.36718925980919));
#19393=CARTESIAN_POINT('Ctrl Pts',(88.9200788119897,-2.7873508641998,3.44705151685388));
#19394=CARTESIAN_POINT('Ctrl Pts',(88.9143754356075,-2.68852715914599,3.52696222846882));
#19395=CARTESIAN_POINT('Ctrl Pts',(88.9086720592254,-2.58635133585645,3.60254943961233));
#19396=CARTESIAN_POINT('Ctrl Pts',(88.9029686828432,-2.48124701120323,3.67354083540595));
#19397=CARTESIAN_POINT('Ctrl Pts',(88.897257133184,-2.37599206581049,3.74463396608602));
#19398=CARTESIAN_POINT('Ctrl Pts',(88.8915455835248,-2.26780057847517,3.81111792209363));
#19399=CARTESIAN_POINT('Ctrl Pts',(88.8858340338655,-2.15712168492817,3.87276581223454));
#19400=CARTESIAN_POINT('Ctrl Pts',(88.8833352361541,-2.10869977101671,3.89973670734887));
#19401=CARTESIAN_POINT('Ctrl Pts',(88.8808364384426,-2.05980202699204,3.92578256936849));
#19402=CARTESIAN_POINT('Ctrl Pts',(88.8783376407312,-2.01046721161541,3.95088731692253));
#19403=CARTESIAN_POINT('Ctrl Pts',(88.8726271506174,-1.89772260080482,4.00825907297089));
#19404=CARTESIAN_POINT('Ctrl Pts',(88.8669166605037,-1.78234588133867,4.06088971102955));
#19405=CARTESIAN_POINT('Ctrl Pts',(88.86120617039,-1.66477265814443,4.1085302720918));
#19406=CARTESIAN_POINT('Ctrl Pts',(88.8555026574601,-1.54734308811755,4.15611262502378));
#19407=CARTESIAN_POINT('Ctrl Pts',(88.8497991445302,-1.42772272042424,4.19871688203682));
#19408=CARTESIAN_POINT('Ctrl Pts',(88.8440956316003,-1.30637146279836,4.2361400592032));
#19409=CARTESIAN_POINT('Ctrl Pts',(88.8383976676482,-1.18513826845135,4.27352682716304));
#19410=CARTESIAN_POINT('Ctrl Pts',(88.8326997036961,-1.06217791443523,4.30574242848771));
#19411=CARTESIAN_POINT('Ctrl Pts',(88.827001739744,-0.937969539779162,4.33263224177248));
#19412=CARTESIAN_POINT('Ctrl Pts',(88.8213079015606,-0.813851101637493,
4.35950258474307));
#19413=CARTESIAN_POINT('Ctrl Pts',(88.8156140633771,-0.68848683030407,4.38105473060733));
#19414=CARTESIAN_POINT('Ctrl Pts',(88.8099202251937,-0.562369793009557,
4.39718423720344));
#19415=CARTESIAN_POINT('Ctrl Pts',(88.8042285298373,-0.436300218778932,
4.41330767359826));
#19416=CARTESIAN_POINT('Ctrl Pts',(88.798536834481,-0.309478837278903,4.42401247789389));
#19417=CARTESIAN_POINT('Ctrl Pts',(88.7928451391247,-0.182407323016303,
4.42924559812504));
#19418=CARTESIAN_POINT('Ctrl Pts',(88.7871543812534,-0.0553567388350208,
4.43447785640351));
#19419=CARTESIAN_POINT('Ctrl Pts',(88.7814636233821,0.0719434973714359,
4.43424020684309));
#19420=CARTESIAN_POINT('Ctrl Pts',(88.7757728655108,0.198988729714833,4.42853163988319));
#19421=CARTESIAN_POINT('Ctrl Pts',(88.7700817623004,0.326041671696574,4.42282272650346));
#19422=CARTESIAN_POINT('Ctrl Pts',(88.7643906590901,0.452839180153901,4.41164225334748));
#19423=CARTESIAN_POINT('Ctrl Pts',(88.7586995558797,0.578879261437488,4.39504127405848));
#19424=CARTESIAN_POINT('Ctrl Pts',(88.7530068245723,0.704955399961066,4.37843554560169));
#19425=CARTESIAN_POINT('Ctrl Pts',(88.747314093265,0.830273284559471,4.35640627830354));
#19426=CARTESIAN_POINT('Ctrl Pts',(88.7416213619577,0.954339194576103,4.32905598273987));
#19427=CARTESIAN_POINT('Ctrl Pts',(88.7359225802343,1.07853696578984,4.30167661841175));
#19428=CARTESIAN_POINT('Ctrl Pts',(88.730223798511,1.20147971540065,4.26896502030362));
#19429=CARTESIAN_POINT('Ctrl Pts',(88.7245250167877,1.32268671422558,4.23107419646727));
#19430=CARTESIAN_POINT('Ctrl Pts',(88.7188227852243,1.44396708746282,4.19316043487189));
#19431=CARTESIAN_POINT('Ctrl Pts',(88.7131205536609,1.56350924169432,4.15006133685358));
#19432=CARTESIAN_POINT('Ctrl Pts',(88.7074183220975,1.68085178923926,4.10197833521963));
#19433=CARTESIAN_POINT('Ctrl Pts',(88.7017079203398,1.79836246594738,4.05382643994908));
#19434=CARTESIAN_POINT('Ctrl Pts',(88.695997518582,1.91366688115736,4.00067654901692));
#19435=CARTESIAN_POINT('Ctrl Pts',(88.6902871168243,2.02632729424893,3.94277652125781));
#19436=CARTESIAN_POINT('Ctrl Pts',(88.6877763377491,2.07586240925397,3.91731873661866));
#19437=CARTESIAN_POINT('Ctrl Pts',(88.6852655586739,2.12488674171948,3.89094321429857));
#19438=CARTESIAN_POINT('Ctrl Pts',(88.6827547795987,2.17336490489364,3.86367363919064));
#19439=CARTESIAN_POINT('Ctrl Pts',(88.6770433142055,2.28364197149242,3.80164140543018));
#19440=CARTESIAN_POINT('Ctrl Pts',(88.6713318488124,2.3914310796582,3.73478852734399));
#19441=CARTESIAN_POINT('Ctrl Pts',(88.6656203834193,2.49628345568051,3.66333972065051));
#19442=CARTESIAN_POINT('Ctrl Pts',(88.6599158814639,2.60100799533493,3.59197802458137));
#19443=CARTESIAN_POINT('Ctrl Pts',(88.6542113795085,2.7028025991565,3.5160317705608));
#19444=CARTESIAN_POINT('Ctrl Pts',(88.6485068775531,2.80124329905826,3.43577138056088));
#19445=CARTESIAN_POINT('Ctrl Pts',(88.6428079121074,2.89958845724684,3.35558888735738));
#19446=CARTESIAN_POINT('Ctrl Pts',(88.6371089466617,2.9945858811983,3.27110084068346));
#19447=CARTESIAN_POINT('Ctrl Pts',(88.631409981216,3.08584120419349,3.18262047101154));
#19448=CARTESIAN_POINT('Ctrl Pts',(88.6257151303313,3.17703064231818,3.09420398273859));
#19449=CARTESIAN_POINT('Ctrl Pts',(88.6200202794467,3.26448307121504,3.00180118519211));
#19450=CARTESIAN_POINT('Ctrl Pts',(88.6143254285621,3.34783817477462,2.90576471097055));
#19451=CARTESIAN_POINT('Ctrl Pts',(88.6086327075492,3.43116210356169,2.80976415434861));
#19452=CARTESIAN_POINT('Ctrl Pts',(88.6029399865364,3.51039149274652,2.7101329241084));
#19453=CARTESIAN_POINT('Ctrl Pts',(88.5972472655235,3.58520403149405,2.6072592990646));
#19454=CARTESIAN_POINT('Ctrl Pts',(88.5915554742348,3.660004352003,2.50440247514151));
#19455=CARTESIAN_POINT('Ctrl Pts',(88.5858636829461,3.73038902225902,2.39830463238631));
#19456=CARTESIAN_POINT('Ctrl Pts',(88.5801718916574,3.79607739688818,2.28938537534306));
#19457=CARTESIAN_POINT('Ctrl Pts',(88.5744797483686,3.86176983391376,2.18045938235599));
#19458=CARTESIAN_POINT('Ctrl Pts',(88.5687876050798,3.9227651915419,2.06871196982378));
#19459=CARTESIAN_POINT('Ctrl Pts',(88.563095461791,3.97882763391271,1.95458938388926));
#19460=CARTESIAN_POINT('Ctrl Pts',(88.55740168484,4.03490616637246,1.84043404443062));
#19461=CARTESIAN_POINT('Ctrl Pts',(88.5517079078891,4.0860487912224,1.72390253354171));
#19462=CARTESIAN_POINT('Ctrl Pts',(88.5460141309381,4.13206708644723,1.60546273488346));
#19463=CARTESIAN_POINT('Ctrl Pts',(88.5403143008061,4.17813430474638,1.486897020238));
#19464=CARTESIAN_POINT('Ctrl Pts',(88.5346144706741,4.2190661716257,1.36641933955194));
#19465=CARTESIAN_POINT('Ctrl Pts',(88.528914640542,4.25472349518734,1.24451475664246));
#19466=CARTESIAN_POINT('Ctrl Pts',(88.5232113575629,4.29040241926731,1.12253632628974));
#19467=CARTESIAN_POINT('Ctrl Pts',(88.5175080745838,4.32080033946052,0.999129658631843));
#19468=CARTESIAN_POINT('Ctrl Pts',(88.5118047916047,4.34582908841368,0.874790565962802));
#19469=CARTESIAN_POINT('Ctrl Pts',(88.5060933429315,4.37089367236019,0.750273450390316));
#19470=CARTESIAN_POINT('Ctrl Pts',(88.5003818942583,4.39057367356081,0.62482163752853));
#19471=CARTESIAN_POINT('Ctrl Pts',(88.4946704455851,4.40483267249706,0.498936997327742));
#19472=CARTESIAN_POINT('Ctrl Pts',(88.4921709365455,4.41107285756669,0.443845931272622));
#19473=CARTESIAN_POINT('Ctrl Pts',(88.489671427506,4.41627547989079,0.388671984248708));
#19474=CARTESIAN_POINT('Ctrl Pts',(88.4871719184664,4.42044062562448,0.333457156661257));
#19475=CARTESIAN_POINT('Ctrl Pts',(88.4814607422868,4.42995764705641,0.207295737323731));
#19476=CARTESIAN_POINT('Ctrl Pts',(88.4757495661071,4.43408399449798,0.0805319756985775));
#19477=CARTESIAN_POINT('Ctrl Pts',(88.4700383899275,4.43275782838372,-0.0463361079808987));
#19478=CARTESIAN_POINT('Ctrl Pts',(88.4643341796299,4.43143327978509,-0.173049451537361));
#19479=CARTESIAN_POINT('Ctrl Pts',(88.4586299693323,4.42466945260335,-0.299866468287363));
#19480=CARTESIAN_POINT('Ctrl Pts',(88.4529257590347,4.4124562977987,-0.426284435578654));
#19481=CARTESIAN_POINT('Ctrl Pts',(88.4472270873202,4.40025500152826,-0.552579655568815));
#19482=CARTESIAN_POINT('Ctrl Pts',(88.4415284156057,4.38261494433749,-0.678476202027556));
#19483=CARTESIAN_POINT('Ctrl Pts',(88.4358297438912,4.3595781156314,-0.803472248249908));
#19484=CARTESIAN_POINT('Ctrl Pts',(88.4301351884441,4.3365579268985,-0.928378007268043));
#19485=CARTESIAN_POINT('Ctrl Pts',(88.4244406329968,4.30814879734629,-1.05238416943556));
#19486=CARTESIAN_POINT('Ctrl Pts',(88.4187460775497,4.27444438719986,-1.1749953960487));
#19487=CARTESIAN_POINT('Ctrl Pts',(88.41305365341,4.24075259164037,-1.29756073282213));
#19488=CARTESIAN_POINT('Ctrl Pts',(88.4073612292704,4.20176956173012,-1.41873178786164));
#19489=CARTESIAN_POINT('Ctrl Pts',(88.4016688051308,4.15763969562153,-1.53802508477336));
#19490=CARTESIAN_POINT('Ctrl Pts',(88.3959773115169,4.11351704330688,-1.65729888112146));
#19491=CARTESIAN_POINT('Ctrl Pts',(88.390285817903,4.06424936672886,-1.77469515566863));
#19492=CARTESIAN_POINT('Ctrl Pts',(88.3845943242891,4.01003023584544,-1.88974773649959));
#19493=CARTESIAN_POINT('Ctrl Pts',(88.3789024791523,3.95580775623424,-2.0048074233053));
#19494=CARTESIAN_POINT('Ctrl Pts',(88.3732106340156,3.89663338424477,-2.11752276741075));
#19495=CARTESIAN_POINT('Ctrl Pts',(88.3675187888788,3.83274770655572,-2.22745011569101));
#19496=CARTESIAN_POINT('Ctrl Pts',(88.361825310233,3.7688436942437,-2.3374090121454));
#19497=CARTESIAN_POINT('Ctrl Pts',(88.3561318315872,3.70022588691505,-2.44457797606595));
#19498=CARTESIAN_POINT('Ctrl Pts',(88.3504383529414,3.62717916722803,-2.54854081560939));
#19499=CARTESIAN_POINT('Ctrl Pts',(88.3447388197215,3.55405476800685,-2.65261421158823));
#19500=CARTESIAN_POINT('Ctrl Pts',(88.3390392865017,3.47649228245226,-2.75347434892433));
#19501=CARTESIAN_POINT('Ctrl Pts',(88.3333397532819,3.39481818658066,-2.85073648029087));
#19502=CARTESIAN_POINT('Ctrl Pts',(88.3276367668201,3.31309460588234,-2.94805754098703));
#19503=CARTESIAN_POINT('Ctrl Pts',(88.3219337803584,3.22725472136438,-3.04177595910031));
#19504=CARTESIAN_POINT('Ctrl Pts',(88.3162307938966,3.13766224411753,-3.13154349192844));
#19505=CARTESIAN_POINT('Ctrl Pts',(88.3105196385554,3.04794143583697,-3.22143960653748));
#19506=CARTESIAN_POINT('Ctrl Pts',(88.3048084832142,2.95445759510588,-3.30737326625973));
#19507=CARTESIAN_POINT('Ctrl Pts',(88.2990973278729,2.8576081652666,-3.38903593574953));
#19508=CARTESIAN_POINT('Ctrl Pts',(88.2965945710266,2.81516656473057,-3.42482235599943));
#19509=CARTESIAN_POINT('Ctrl Pts',(88.2940918141803,2.77207902670282,-3.45978913373035));
#19510=CARTESIAN_POINT('Ctrl Pts',(88.291589057334,2.72838069256191,-3.49391296349171));
#19511=CARTESIAN_POINT('Ctrl Pts',(88.2858779581601,2.62866444550436,-3.57178092587354));
#19512=CARTESIAN_POINT('Ctrl Pts',(88.2801668589862,2.52545816082209,-3.64549679102386));
#19513=CARTESIAN_POINT('Ctrl Pts',(88.2744557598124,2.4191419936789,-3.71473296677154));
#19514=CARTESIAN_POINT('Ctrl Pts',(88.2687516284963,2.31295553815734,-3.78388467054404));
#19515=CARTESIAN_POINT('Ctrl Pts',(88.2630474971802,2.2036670803463,-3.84856734239221));
#19516=CARTESIAN_POINT('Ctrl Pts',(88.2573433658642,2.09168940537722,-3.90849388274214));
#19517=CARTESIAN_POINT('Ctrl Pts',(88.2516447750012,1.97982049491967,-3.96836221612455));
#19518=CARTESIAN_POINT('Ctrl Pts',(88.2459461841382,1.86526791486414,-4.02348342317211));
#19519=CARTESIAN_POINT('Ctrl Pts',(88.2402475932753,1.74847255868385,-4.073614207498));
#19520=CARTESIAN_POINT('Ctrl Pts',(88.234553120446,1.63176160358075,-4.12370876527913));
#19521=CARTESIAN_POINT('Ctrl Pts',(88.2288586476166,1.51281146363334,-4.16881992102407));
#19522=CARTESIAN_POINT('Ctrl Pts',(88.2231641747873,1.3920862829569,-4.20875097633529));
#19523=CARTESIAN_POINT('Ctrl Pts',(88.2174718355986,1.27140633634445,-4.24866707002954));
#19524=CARTESIAN_POINT('Ctrl Pts',(88.2117794964099,1.14895304977384,-4.28340679732801));
#19525=CARTESIAN_POINT('Ctrl Pts',(88.2060871572212,1.02520882789455,-4.31282226149039));
#19526=CARTESIAN_POINT('Ctrl Pts',(88.2003957499874,0.901484865528564,-4.342232909727));
#19527=CARTESIAN_POINT('Ctrl Pts',(88.1947043427534,0.776470776461303,-4.36632093641831));
#19528=CARTESIAN_POINT('Ctrl Pts',(88.1890129355195,0.650661828547268,-4.3849889606328));
#19529=CARTESIAN_POINT('Ctrl Pts',(88.1833211781036,0.52484513983484,-4.40365813345726));
#19530=CARTESIAN_POINT('Ctrl Pts',(88.1776294206876,0.398233889867758,-4.41690658195273));
#19531=CARTESIAN_POINT('Ctrl Pts',(88.1719376632717,0.271330675230027,-4.4246885387199));
#19532=CARTESIAN_POINT('Ctrl Pts',(88.1662442736,0.144391067878774,-4.43247272716043));
#19533=CARTESIAN_POINT('Ctrl Pts',(88.1605508839284,0.0171597275565208,
-4.43478728084396));
#19534=CARTESIAN_POINT('Ctrl Pts',(88.1548574942567,-0.109859042330854,
-4.43163852212905));
#19535=CARTESIAN_POINT('Ctrl Pts',(88.1491580514315,-0.23701285727201,-4.42848641568616));
#19536=CARTESIAN_POINT('Ctrl Pts',(88.1434586086063,-0.363953251139066,
-4.41985940935115));
#19537=CARTESIAN_POINT('Ctrl Pts',(88.1377591657811,-0.490179027338487,
-4.40581587463179));
#19538=CARTESIAN_POINT('Ctrl Pts',(88.13205627065,-0.616481261888762,-4.39176383336538));
#19539=CARTESIAN_POINT('Ctrl Pts',(88.1263533755188,-0.742067622648898,
-4.37228878877165));
#19540=CARTESIAN_POINT('Ctrl Pts',(88.1206504803877,-0.866446647464566,
-4.3475003400917));
#19541=CARTESIAN_POINT('Ctrl Pts',(88.1149394170264,-0.991003819777342,
-4.32267638703232));
#19542=CARTESIAN_POINT('Ctrl Pts',(88.1092283536652,-1.11434981633043,-4.2925239283635));
#19543=CARTESIAN_POINT('Ctrl Pts',(88.1035172903039,-1.23600751705262,-4.25720265171737));
#19544=CARTESIAN_POINT('Ctrl Pts',(88.1010135922699,-1.28934156832493,-4.24171800283394));
#19545=CARTESIAN_POINT('Ctrl Pts',(88.0985098942358,-1.34235139342916,-4.22524059022021));
#19546=CARTESIAN_POINT('Ctrl Pts',(88.0960061962017,-1.39499806833746,-4.2077867566376));
#19547=CARTESIAN_POINT('Ctrl Pts',(88.0902949857889,-1.51509092052739,-4.16797264377605));
#19548=CARTESIAN_POINT('Ctrl Pts',(88.0845837753762,-1.6336631609298,-4.12295174897156));
#19549=CARTESIAN_POINT('Ctrl Pts',(88.0788725649634,-1.75023137394233,-4.07285884087184));
#19550=CARTESIAN_POINT('Ctrl Pts',(88.073168320749,-1.86665740390753,-4.02282703315394));
#19551=CARTESIAN_POINT('Ctrl Pts',(88.0674640765346,-1.98108390597914,-3.96773567640255));
#19552=CARTESIAN_POINT('Ctrl Pts',(88.0617598323203,-2.09304307445528,-3.90776914472628));
#19553=CARTESIAN_POINT('Ctrl Pts',(88.056061127046,-2.20489352824358,-3.84786084180306));
#19554=CARTESIAN_POINT('Ctrl Pts',(88.0503624217718,-2.31428106592543,-3.78308697113222));
#19555=CARTESIAN_POINT('Ctrl Pts',(88.0446637164975,-2.42075875350021,-3.71367958463733));
#19556=CARTESIAN_POINT('Ctrl Pts',(88.0389691278883,-2.5271595230825,-3.64432233706784));
#19557=CARTESIAN_POINT('Ctrl Pts',(88.033274539279,-2.63065429300325,-3.57033845281576));
#19558=CARTESIAN_POINT('Ctrl Pts',(88.0275799506697,-2.73082201984094,-3.49200516837416));
#19559=CARTESIAN_POINT('Ctrl Pts',(88.0218874940895,-2.83095224432101,-3.41370121157071));
#19560=CARTESIAN_POINT('Ctrl Pts',(88.0161950375092,-2.92775758853443,-3.33105133786086));
#19561=CARTESIAN_POINT('Ctrl Pts',(88.010502580929,-3.02084749990109,-3.2443750372516));
#19562=CARTESIAN_POINT('Ctrl Pts',(88.004811055335,-3.11392218665838,-3.1577129123226));
#19563=CARTESIAN_POINT('Ctrl Pts',(87.999119529741,-3.20328235721564,-3.06702594223288));
#19564=CARTESIAN_POINT('Ctrl Pts',(87.993428004147,-3.28857236869048,-2.97267232904763));
#19565=CARTESIAN_POINT('Ctrl Pts',(87.9877361275281,-3.37386764042707,-2.87831289660297));
#19566=CARTESIAN_POINT('Ctrl Pts',(87.9820442509093,-3.45509198614297,-2.78028666741058));
#19567=CARTESIAN_POINT('Ctrl Pts',(87.9763523742904,-3.53192865445068,-2.67898655835938));
#19568=CARTESIAN_POINT('Ctrl Pts',(87.9706588646982,-3.60878736684661,-2.57765738677085));
#19569=CARTESIAN_POINT('Ctrl Pts',(87.964965355106,-3.68125565651211,-2.47305278469922));
#19570=CARTESIAN_POINT('Ctrl Pts',(87.9592718455138,-3.74905917663427,-2.36559596932662));
#19571=CARTESIAN_POINT('Ctrl Pts',(87.9535722823306,-3.8169347884554,-2.25802490111918));
#19572=CARTESIAN_POINT('Ctrl Pts',(87.9478727191474,-3.88013551477021,-2.14759590255314));
#19573=CARTESIAN_POINT('Ctrl Pts',(87.9421731559642,-3.93843204822112,-2.03475846270382));
#19574=CARTESIAN_POINT('Ctrl Pts',(87.9364701400612,-3.99676389693887,-1.92185266742987));
#19575=CARTESIAN_POINT('Ctrl Pts',(87.9307671241582,-4.05018546690914,-1.80653588594852));
#19576=CARTESIAN_POINT('Ctrl Pts',(87.9250641082552,-4.09851548105195,-1.6892779083317));
#19577=CARTESIAN_POINT('Ctrl Pts',(87.9193529245336,-4.14691471309565,-1.57185199467724));
#19578=CARTESIAN_POINT('Ctrl Pts',(87.913641740812,-4.19020769294354,-1.4524797079483));
#19579=CARTESIAN_POINT('Ctrl Pts',(87.9079305570904,-4.22826278018989,-1.33164667298082));
#19580=CARTESIAN_POINT('Ctrl Pts',(87.90542814975,-4.24493696444051,-1.2787025744542));
#19581=CARTESIAN_POINT('Ctrl Pts',(87.9029257424097,-4.26060622023336,-1.22547817995853));
#19582=CARTESIAN_POINT('Ctrl Pts',(87.9004233350693,-4.27526257954052,-1.17201487873684));
#19583=CARTESIAN_POINT('Ctrl Pts',(87.8932731563333,-4.31714048925394,-1.01925311473932));
#19584=CARTESIAN_POINT('Ctrl Pts',(87.8861229775972,-4.35084897738077,-0.864164255937209));
#19585=CARTESIAN_POINT('Ctrl Pts',(87.8789727988612,-4.37617406990347,-0.70752350484245));
#19586=CARTESIAN_POINT('Ctrl Pts',(87.8719271935475,-4.40112877565772,-0.553173669824393));
#19587=CARTESIAN_POINT('Ctrl Pts',(87.8648815882338,-4.41794351585947,-0.397316902218557));
#19588=CARTESIAN_POINT('Ctrl Pts',(87.85783598292,-4.42645967010616,-0.240715161391253));
#19589=CARTESIAN_POINT('Ctrl Pts',(87.8542882950715,-4.43074782642376,-0.161861171101559));
#19590=CARTESIAN_POINT('Ctrl Pts',(87.850740607223,-4.43293265294547,-0.0828186286532786));
#19591=CARTESIAN_POINT('Ctrl Pts',(87.8471929193744,-4.43299846679216,-0.00368692533081282));
#19592=CARTESIAN_POINT('',(86.5971929193007,-4.43299889626788,0.00312820839395853));
#19593=CARTESIAN_POINT('Ctrl Pts',(87.8471929193385,-4.43299846679282,-0.00368692453002637));
#19594=CARTESIAN_POINT('Ctrl Pts',(87.8412615674468,-4.43310850043048,0.128612758598833));
#19595=CARTESIAN_POINT('Ctrl Pts',(87.8353302155551,-4.42729075618896,0.261038035339765));
#19596=CARTESIAN_POINT('Ctrl Pts',(87.8293988636633,-4.41554413589774,0.393012702007276));
#19597=CARTESIAN_POINT('Ctrl Pts',(87.8237577098415,-4.40437223223067,0.518530359507987));
#19598=CARTESIAN_POINT('Ctrl Pts',(87.8181165560196,-4.38783787641083,0.64363999588161));
#19599=CARTESIAN_POINT('Ctrl Pts',(87.8124754021977,-4.36599350192544,0.767847472578289));
#19600=CARTESIAN_POINT('Ctrl Pts',(87.8068353578439,-4.34415342365963,0.89203052089888));
#19601=CARTESIAN_POINT('Ctrl Pts',(87.80119531349,-4.3170054737535,1.0153113613675));
#19602=CARTESIAN_POINT('Ctrl Pts',(87.7955552691362,-4.28465359414585,1.13720384196198));
#19603=CARTESIAN_POINT('Ctrl Pts',(87.7899150029168,-4.25230044189391,1.25910111751025));
#19604=CARTESIAN_POINT('Ctrl Pts',(87.7842747366973,-4.2147430577544,1.37960953098333));
#19605=CARTESIAN_POINT('Ctrl Pts',(87.7786344704778,-4.17213570277715,1.49825654599346));
#19606=CARTESIAN_POINT('Ctrl Pts',(87.7729926511568,-4.12951661545433,1.6169362316019));
#19607=CARTESIAN_POINT('Ctrl Pts',(87.7673508318357,-4.0818449301354,1.73375311648484));
#19608=CARTESIAN_POINT('Ctrl Pts',(87.7617090125146,-4.02932340739154,1.84825373762551));
#19609=CARTESIAN_POINT('Ctrl Pts',(87.7560612407086,-3.97674647103854,1.96287516433947));
#19610=CARTESIAN_POINT('Ctrl Pts',(87.7504134689026,-3.91930965343418,2.07517507880274));
#19611=CARTESIAN_POINT('Ctrl Pts',(87.7447656970966,-3.85726220666753,2.184723613873));
#19612=CARTESIAN_POINT('Ctrl Pts',(87.7391144537161,-3.79517662055247,2.29433948627888));
#19613=CARTESIAN_POINT('Ctrl Pts',(87.7334632103356,-3.72847497780001,2.40120026736829));
#19614=CARTESIAN_POINT('Ctrl Pts',(87.7278119669551,-3.65744957676044,2.50490550589337));
#19615=CARTESIAN_POINT('Ctrl Pts',(87.7221526948006,-3.5863232692746,2.60875807941303));
#19616=CARTESIAN_POINT('Ctrl Pts',(87.7164934226462,-3.51086118639162,2.70944583774612));
#19617=CARTESIAN_POINT('Ctrl Pts',(87.7108341504918,-3.43139567019841,2.80660163802125));
#19618=CARTESIAN_POINT('Ctrl Pts',(87.7088362583068,-3.40334196833646,2.84090053879793));
#19619=CARTESIAN_POINT('Ctrl Pts',(87.7068383661219,-3.3747896503618,2.87475959036286));
#19620=CARTESIAN_POINT('Ctrl Pts',(87.7048404739369,-3.34575438665027,2.90816378221903));
#19621=CARTESIAN_POINT('Ctrl Pts',(87.6991293093837,-3.26275432781231,3.00365283708149));
#19622=CARTESIAN_POINT('Ctrl Pts',(87.6934181448304,-3.175535045002,3.09573308792214));
#19623=CARTESIAN_POINT('Ctrl Pts',(87.6877069802772,-3.08440710509131,3.18401033447792));
#19624=CARTESIAN_POINT('Ctrl Pts',(87.6820027825159,-2.99339032804251,3.27217989560401));
#19625=CARTESIAN_POINT('Ctrl Pts',(87.6762985847546,-2.89847466397116,3.35655540652586));
#19626=CARTESIAN_POINT('Ctrl Pts',(87.6705943869933,-2.80001044521793,3.43677617930969));
#19627=CARTESIAN_POINT('Ctrl Pts',(87.6648957287057,-2.70164184726516,3.51691904791061));
#19628=CARTESIAN_POINT('Ctrl Pts',(87.6591970704182,-2.59973185954931,3.59291495626663));
#19629=CARTESIAN_POINT('Ctrl Pts',(87.6534984121306,-2.49466677417512,3.66444084217861));
#19630=CARTESIAN_POINT('Ctrl Pts',(87.6478038709826,-2.38967759572394,3.73591505240884));
#19631=CARTESIAN_POINT('Ctrl Pts',(87.6421093298346,-2.28153818529909,3.80292544397902));
#19632=CARTESIAN_POINT('Ctrl Pts',(87.6364147886866,-2.17066656065766,3.86519025177838));
#19633=CARTESIAN_POINT('Ctrl Pts',(87.6307223800985,-2.05983645655062,3.9274317419065));
#19634=CARTESIAN_POINT('Ctrl Pts',(87.6250299715105,-1.94627652014265,3.98493098676285));
#19635=CARTESIAN_POINT('Ctrl Pts',(87.6193375629225,-1.83043201790219,4.03745063472465));
#19636=CARTESIAN_POINT('Ctrl Pts',(87.6136460856369,-1.71460646831836,4.08996169024715));
#19637=CARTESIAN_POINT('Ctrl Pts',(87.6079546083513,-1.59649745976387,4.13749460459382));
#19638=CARTESIAN_POINT('Ctrl Pts',(87.6022631310657,-1.47657253710115,4.17985915344987));
#19639=CARTESIAN_POINT('Ctrl Pts',(87.5965713030196,-1.35664022357751,4.22222631319348));
#19640=CARTESIAN_POINT('Ctrl Pts',(87.5908794749736,-1.23489214974176,4.25942434098187));
#19641=CARTESIAN_POINT('Ctrl Pts',(87.5851876469276,-1.1118129162237,4.29131227473813));
#19642=CARTESIAN_POINT('Ctrl Pts',(87.5794941861211,-0.988698376139835,
4.32320935588181));
#19643=CARTESIAN_POINT('Ctrl Pts',(87.5738007253147,-0.864252302975927,
4.34979321263873));
#19644=CARTESIAN_POINT('Ctrl Pts',(87.5681072645082,-0.738970925940442,
4.37097368679048));
#19645=CARTESIAN_POINT('Ctrl Pts',(87.5624077501686,-0.613556344340249,
4.39217668093606));
#19646=CARTESIAN_POINT('Ctrl Pts',(87.556708235829,-0.487305079536574,4.40796475512485));
#19647=CARTESIAN_POINT('Ctrl Pts',(87.5510087214894,-0.360720256752866,
4.41829943489213));
#19648=CARTESIAN_POINT('Ctrl Pts',(87.5453057545294,-0.234058752112526,
4.42864037514479));
#19649=CARTESIAN_POINT('Ctrl Pts',(87.5396027875694,-0.107063685173065,
4.43352132465323));
#19650=CARTESIAN_POINT('Ctrl Pts',(87.5338998206094,0.0197615851498626,
4.43295595283242));
#19651=CARTESIAN_POINT('Ctrl Pts',(87.5281886855587,0.146768501327744,4.4323897712562));
#19652=CARTESIAN_POINT('Ctrl Pts',(87.522477550508,0.273604737472531,4.42636171148116));
#19653=CARTESIAN_POINT('Ctrl Pts',(87.5167664154573,0.399771441374032,4.41493734889429));
#19654=CARTESIAN_POINT('Ctrl Pts',(87.5142634812398,0.455064646229623,4.40993056341661));
#19655=CARTESIAN_POINT('Ctrl Pts',(87.5117605470222,0.510229377559847,4.40388798793471));
#19656=CARTESIAN_POINT('Ctrl Pts',(87.5092576128046,0.565224344161995,4.3968182178442));
#19657=CARTESIAN_POINT('Ctrl Pts',(87.5035464360579,0.690711451347686,4.38068646885081));
#19658=CARTESIAN_POINT('Ctrl Pts',(87.4978352593113,0.815700963541726,4.35915337948087));
#19659=CARTESIAN_POINT('Ctrl Pts',(87.4921240825646,0.939692625398773,4.3322588530432));
#19660=CARTESIAN_POINT('Ctrl Pts',(87.486419872417,1.06353303993185,4.30539713304664));
#19661=CARTESIAN_POINT('Ctrl Pts',(87.4807156622695,1.1863776389725,4.27318707104068));
#19662=CARTESIAN_POINT('Ctrl Pts',(87.4750114521219,1.30773200965324,4.23572024464887));
#19663=CARTESIAN_POINT('Ctrl Pts',(87.4693127812714,1.42896853441169,4.19828980188863));
#19664=CARTESIAN_POINT('Ctrl Pts',(87.4636141104209,1.54871733117747,4.15561286962637));
#19665=CARTESIAN_POINT('Ctrl Pts',(87.4579154395704,1.66649536283774,4.10783181321245));
#19666=CARTESIAN_POINT('Ctrl Pts',(87.4522208856985,1.78418830629793,4.06008527600412));
#19667=CARTESIAN_POINT('Ctrl Pts',(87.4465263318267,1.89991294977084,4.00724210333145));
#19668=CARTESIAN_POINT('Ctrl Pts',(87.4408317779548,2.01320303481319,3.94949396006868));
#19669=CARTESIAN_POINT('Ctrl Pts',(87.4351393564502,2.12645069755636,3.89176744101962));
#19670=CARTESIAN_POINT('Ctrl Pts',(87.4294469349457,2.23726525946651,3.82913978433716));
#19671=CARTESIAN_POINT('Ctrl Pts',(87.4237545134411,2.34520231646116,3.76184995645297));
#19672=CARTESIAN_POINT('Ctrl Pts',(87.4180630231227,2.45312171673464,3.6945711360741));
#19673=CARTESIAN_POINT('Ctrl Pts',(87.4123715328043,2.55816420977772,3.62263187257006));
#19674=CARTESIAN_POINT('Ctrl Pts',(87.4066800424859,2.65991226009746,3.54631580215062));
#19675=CARTESIAN_POINT('Ctrl Pts',(87.4009882013048,2.76166658286984,3.46999502708146));
#19676=CARTESIAN_POINT('Ctrl Pts',(87.3952963601237,2.86012573966043,3.38929714797341));
#19677=CARTESIAN_POINT('Ctrl Pts',(87.3896045189425,2.95490373590428,3.30454730811029));
#19678=CARTESIAN_POINT('Ctrl Pts',(87.3839110449123,3.04970892162158,3.21977315560485));
#19679=CARTESIAN_POINT('Ctrl Pts',(87.378217570882,3.14083054854304,3.13094499587316));
#19680=CARTESIAN_POINT('Ctrl Pts',(87.3725240968518,3.22791845502371,3.03842581737934));
#19681=CARTESIAN_POINT('Ctrl Pts',(87.3668245692257,3.31509895786811,2.94580826771265));
#19682=CARTESIAN_POINT('Ctrl Pts',(87.3611250415996,3.39823690325468,2.84949215452158));
#19683=CARTESIAN_POINT('Ctrl Pts',(87.3554255139734,3.47702131862471,2.74987486075808));
#19684=CARTESIAN_POINT('Ctrl Pts',(87.349722533673,3.55585346021824,2.65019722057703));
#19685=CARTESIAN_POINT('Ctrl Pts',(87.3440195533725,3.6303265844766,2.54721473890253));
#19686=CARTESIAN_POINT('Ctrl Pts',(87.3383165730721,3.70017298468677,2.44135390375796));
#19687=CARTESIAN_POINT('Ctrl Pts',(87.3326054247137,3.77011942196735,2.33534145009349));
#19688=CARTESIAN_POINT('Ctrl Pts',(87.3268942763553,3.83542569861879,2.22644275284825));
#19689=CARTESIAN_POINT('Ctrl Pts',(87.3211831279969,3.8958698040357,2.11510932814426));
#19690=CARTESIAN_POINT('Ctrl Pts',(87.3186803358887,3.92235817739518,2.06631976792811));
#19691=CARTESIAN_POINT('Ctrl Pts',(87.3161775437804,3.94791341649992,2.01706289789703));
#19692=CARTESIAN_POINT('Ctrl Pts',(87.3136747516722,3.97251978385321,1.96737784039946));
#19693=CARTESIAN_POINT('Ctrl Pts',(87.3079635806114,4.02866954262647,1.85400052008763));
#19694=CARTESIAN_POINT('Ctrl Pts',(87.3022524095507,4.08004830297613,1.73804259426207));
#19695=CARTESIAN_POINT('Ctrl Pts',(87.2965412384899,4.12641191158218,1.61994251007642));
#19696=CARTESIAN_POINT('Ctrl Pts',(87.2908370340932,4.17271896441743,1.50198648804413));
#19697=CARTESIAN_POINT('Ctrl Pts',(87.2851328296964,4.2140228918231,1.38189387467903));
#19698=CARTESIAN_POINT('Ctrl Pts',(87.2794286252996,4.25012578432657,1.26012690527679));
#19699=CARTESIAN_POINT('Ctrl Pts',(87.2737299602574,4.28619361730083,1.13847818381328));
#19700=CARTESIAN_POINT('Ctrl Pts',(87.2680312952151,4.31707035277037,1.01515872228983));
#19701=CARTESIAN_POINT('Ctrl Pts',(87.2623326301728,4.34260665515484,0.890649447653165));
#19702=CARTESIAN_POINT('Ctrl Pts',(87.2566380821594,4.36812450871079,0.766230125360507));
#19703=CARTESIAN_POINT('Ctrl Pts',(87.2509435341461,4.38830952828994,0.640623090475924));
#19704=CARTESIAN_POINT('Ctrl Pts',(87.2452489861327,4.40306270929082,0.514322640034989));
#19705=CARTESIAN_POINT('Ctrl Pts',(87.2395565705395,4.41781036571238,0.388069484943883));
#19706=CARTESIAN_POINT('Ctrl Pts',(87.2338641549464,4.42713018167997,0.26112382640866));
#19707=CARTESIAN_POINT('Ctrl Pts',(87.2281717393533,4.430974634992,0.133987999677086));
#19708=CARTESIAN_POINT('Ctrl Pts',(87.2224802549776,4.4348184593932,0.00687297098711359));
#19709=CARTESIAN_POINT('Ctrl Pts',(87.2167887706019,4.43318869072357,-0.120431765188496));
#19710=CARTESIAN_POINT('Ctrl Pts',(87.2110972862262,4.42608987904782,-0.247421467521375));
#19711=CARTESIAN_POINT('Ctrl Pts',(87.2054054510125,4.41899062978273,-0.374418997832107));
#19712=CARTESIAN_POINT('Ctrl Pts',(87.1997136157988,4.40642168928279,-0.501101057126508));
#19713=CARTESIAN_POINT('Ctrl Pts',(87.1940217805851,4.38843963833758,-0.626966139968921));
#19714=CARTESIAN_POINT('Ctrl Pts',(87.1883283125408,4.37045242883763,-0.752867330034119));
#19715=CARTESIAN_POINT('Ctrl Pts',(87.1826348444964,4.3470490761229,-0.877950682418883));
#19716=CARTESIAN_POINT('Ctrl Pts',(87.1769413764521,4.31833752384674,-1.00172352979112));
#19717=CARTESIAN_POINT('Ctrl Pts',(87.1712418548072,4.28959544390871,-1.1256279790913));
#19718=CARTESIAN_POINT('Ctrl Pts',(87.1655423331624,4.25553398588382,-1.24821875212503));
#19719=CARTESIAN_POINT('Ctrl Pts',(87.1598428115176,4.21631144533384,-1.36901672595584));
#19720=CARTESIAN_POINT('Ctrl Pts',(87.1541398372039,4.17706514446639,-1.48988787705074));
#19721=CARTESIAN_POINT('Ctrl Pts',(87.1484368628902,4.13265167199479,-1.60896369203366));
#19722=CARTESIAN_POINT('Ctrl Pts',(87.1427338885766,4.08327753372543,-1.72578491781947));
#19723=CARTESIAN_POINT('Ctrl Pts',(87.1370227461614,4.03383267920321,-1.84277346114501));
#19724=CARTESIAN_POINT('Ctrl Pts',(87.1313116037462,3.97941314270378,-1.95750060760015));
#19725=CARTESIAN_POINT('Ctrl Pts',(87.125600461331,3.92027159475806,-2.06953125691136));
#19726=CARTESIAN_POINT('Ctrl Pts',(87.1230976044006,3.89435334191318,-2.11862768397628));
#19727=CARTESIAN_POINT('Ctrl Pts',(87.1205947474702,3.86752876863485,-2.16720660325151));
#19728=CARTESIAN_POINT('Ctrl Pts',(87.1180918905398,3.83982170988911,-2.21523322389863));
#19729=CARTESIAN_POINT('Ctrl Pts',(87.1123807193201,3.77659805752225,-2.32482328887132));
#19730=CARTESIAN_POINT('Ctrl Pts',(87.1066695481004,3.70858153221895,-2.43187360557027));
#19731=CARTESIAN_POINT('Ctrl Pts',(87.1009583768807,3.63600165180871,-2.53593789120403));
#19732=CARTESIAN_POINT('Ctrl Pts',(87.095254172336,3.56351030673041,-2.63987523578994));
#19733=CARTESIAN_POINT('Ctrl Pts',(87.0895499677914,3.48646690744268,-2.74083347132593));
#19734=CARTESIAN_POINT('Ctrl Pts',(87.0838457632467,3.40514640826533,-2.83839161115547));
#19735=CARTESIAN_POINT('Ctrl Pts',(87.0781470980677,3.32390487960515,-2.93585501205897));
#19736=CARTESIAN_POINT('Ctrl Pts',(87.0724484328887,3.23839477006315,-3.02992458256673));
#19737=CARTESIAN_POINT('Ctrl Pts',(87.0667497677097,3.14893352089849,-3.12020939697352));
#19738=CARTESIAN_POINT('Ctrl Pts',(87.061055219571,3.05953690363478,-3.21042898448892));
#19739=CARTESIAN_POINT('Ctrl Pts',(87.0553606714323,2.96619510811612,-3.29686897546491));
#19740=CARTESIAN_POINT('Ctrl Pts',(87.0496661232935,2.86926460800952,-3.37917291792296));
#19741=CARTESIAN_POINT('Ctrl Pts',(87.0439737075925,2.77237040547232,-3.46144604001941));
#19742=CARTESIAN_POINT('Ctrl Pts',(87.0382812918915,2.67189047416994,-3.53958593524632));
#19743=CARTESIAN_POINT('Ctrl Pts',(87.0325888761905,2.5682165212555,-3.6132745397977));
#19744=CARTESIAN_POINT('Ctrl Pts',(87.0268973917179,2.46455952847356,-3.6869510895517));
#19745=CARTESIAN_POINT('Ctrl Pts',(87.0212059072452,2.35770987863441,-3.75617756590147));
#19746=CARTESIAN_POINT('Ctrl Pts',(87.0155144227726,2.24809015223047,-3.82067790679146));
#19747=CARTESIAN_POINT('Ctrl Pts',(87.009822587473,2.13846366879342,-3.88518222352552));
#19748=CARTESIAN_POINT('Ctrl Pts',(87.0041307521735,2.02606711322478,-3.94495962296032));
#19749=CARTESIAN_POINT('Ctrl Pts',(86.9984389168739,1.91134922094013,-3.99977913835396));
#19750=CARTESIAN_POINT('Ctrl Pts',(86.992745448755,1.79659841948137,-4.054614379847));
#19751=CARTESIAN_POINT('Ctrl Pts',(86.987051980636,1.67952531656237,-4.10448873587591));
#19752=CARTESIAN_POINT('Ctrl Pts',(86.9813585125171,1.56059976994032,-4.14921888529181));
#19753=CARTESIAN_POINT('Ctrl Pts',(86.9756589908152,1.44154777566845,-4.19399659406254));
#19754=CARTESIAN_POINT('Ctrl Pts',(86.9699594691133,1.32063977907843,-4.23361903494679));
#19755=CARTESIAN_POINT('Ctrl Pts',(86.9642599474114,1.19836228306582,-4.26795230040417));
#19756=CARTESIAN_POINT('Ctrl Pts',(86.9585569730506,1.07601071373488,-4.30230636428306));
#19757=CARTESIAN_POINT('Ctrl Pts',(86.9528539986898,0.952288380234433,-4.33136477871307));
#19758=CARTESIAN_POINT('Ctrl Pts',(86.947151024329,0.827691978982203,-4.3550447745033));
#19759=CARTESIAN_POINT('Ctrl Pts',(86.9414398818824,0.702917124518957,-4.37875868597042));
#19760=CARTESIAN_POINT('Ctrl Pts',(86.9357287394359,0.577266096688827,-4.39707873978299));
#19761=CARTESIAN_POINT('Ctrl Pts',(86.9300175969893,0.45124108693146,-4.40997397741358));
#19762=CARTESIAN_POINT('Ctrl Pts',(86.9275147411287,0.39601178084987,-4.41562519717913));
#19763=CARTESIAN_POINT('Ctrl Pts',(86.9250118852681,0.340710657020514,-4.42023522939293));
#19764=CARTESIAN_POINT('Ctrl Pts',(86.9225090294075,0.285379884210033,-4.42380462065045));
#19765=CARTESIAN_POINT('Ctrl Pts',(86.9167978569,0.159122678004703,-4.43194948010454));
#19766=CARTESIAN_POINT('Ctrl Pts',(86.9110866843924,0.0323217523639859,
-4.43469745605847));
#19767=CARTESIAN_POINT('Ctrl Pts',(86.9053755118849,-0.0945242314710083,
-4.43199212202197));
#19768=CARTESIAN_POINT('Ctrl Pts',(86.8996713060308,-0.221215484905607,
-4.42929008803019));
#19769=CARTESIAN_POINT('Ctrl Pts',(86.8939671001767,-0.347951291536879,
-4.42114798672762));
#19770=CARTESIAN_POINT('Ctrl Pts',(86.8882628943226,-0.474228850403496,
-4.40756123014133));
#19771=CARTESIAN_POINT('Ctrl Pts',(86.8825642278143,-0.600383781320188,
-4.3939876676342));
#19772=CARTESIAN_POINT('Ctrl Pts',(86.876865561306,-0.726080955335841,-4.37498001326702));
#19773=CARTESIAN_POINT('Ctrl Pts',(86.8711668947977,-0.850819032508404,
-4.35058570469787));
#19774=CARTESIAN_POINT('Ctrl Pts',(86.8654723453115,-0.975466992210403,
-4.32620901988431));
#19775=CARTESIAN_POINT('Ctrl Pts',(86.8597777958253,-1.09915684375608,-4.29645350269457));
#19776=CARTESIAN_POINT('Ctrl Pts',(86.854083246339,-1.22139429596614,-4.26141818808966));
#19777=CARTESIAN_POINT('Ctrl Pts',(86.8483908292684,-1.34358597439709,-4.22639599302155));
#19778=CARTESIAN_POINT('Ctrl Pts',(86.8426984121977,-1.46432595181099,-4.18609804148277));
#19779=CARTESIAN_POINT('Ctrl Pts',(86.8370059951271,-1.583132349755,-4.14067397450695));
#19780=CARTESIAN_POINT('Ctrl Pts',(86.8313145092714,-1.7019193123181,-4.09525733839395));
#19781=CARTESIAN_POINT('Ctrl Pts',(86.8256230234157,-1.81877295188167,-4.0447163973388));
#19782=CARTESIAN_POINT('Ctrl Pts',(86.81993153756,-1.93322922746241,-3.98924977333898));
#19783=CARTESIAN_POINT('Ctrl Pts',(86.8142397008655,-2.04769255844206,-3.93377973022424));
#19784=CARTESIAN_POINT('Ctrl Pts',(86.808547864171,-2.15975787230553,-3.87338357435075));
#19785=CARTESIAN_POINT('Ctrl Pts',(86.8028560274765,-2.26898415615019,-3.80830669709511));
#19786=CARTESIAN_POINT('Ctrl Pts',(86.7971625579521,-2.37824177398204,-3.74321115109082));
#19787=CARTESIAN_POINT('Ctrl Pts',(86.7914690884278,-2.48465839882089,-3.67343241669553));
#19788=CARTESIAN_POINT('Ctrl Pts',(86.7857756189034,-2.58782095850807,-3.59925988040685));
#19789=CARTESIAN_POINT('Ctrl Pts',(86.7800760957878,-2.69109320596399,-3.52500848004161));
#19790=CARTESIAN_POINT('Ctrl Pts',(86.7743765726722,-2.79110415583821,-3.44635418339532));
#19791=CARTESIAN_POINT('Ctrl Pts',(86.7686770495566,-2.88747263043725,-3.36362762630999));
#19792=CARTESIAN_POINT('Ctrl Pts',(86.7629740737754,-2.98389948327371,-3.28085095500826));
#19793=CARTESIAN_POINT('Ctrl Pts',(86.7572710979942,-3.07667917421548,-3.19399738124988));
#19794=CARTESIAN_POINT('Ctrl Pts',(86.7515681222131,-3.16546743243455,-3.1034343772982));
#19795=CARTESIAN_POINT('Ctrl Pts',(86.7458569783482,-3.25438285758336,-3.01274166453825));
#19796=CARTESIAN_POINT('Ctrl Pts',(86.7401458344834,-3.33929516872905,-2.91832920924054));
#19797=CARTESIAN_POINT('Ctrl Pts',(86.7344346906186,-3.41990016645889,-2.82059778264369));
#19798=CARTESIAN_POINT('Ctrl Pts',(86.7319318498374,-3.45522434673863,-2.77776814888233));
#19799=CARTESIAN_POINT('Ctrl Pts',(86.7294290090563,-3.48972185442209,-2.73430147873475));
#19800=CARTESIAN_POINT('Ctrl Pts',(86.7269261682751,-3.52336976477716,-2.69023316845476));
#19801=CARTESIAN_POINT('Ctrl Pts',(86.7212150154459,-3.60014986196306,-2.58967509187851));
#19802=CARTESIAN_POINT('Ctrl Pts',(86.7155038626168,-3.6727441616283,-2.4856668996596));
#19803=CARTESIAN_POINT('Ctrl Pts',(86.7097927097876,-3.74082788013809,-2.3785911315696));
#19804=CARTESIAN_POINT('Ctrl Pts',(86.7040883844099,-3.8088302073252,-2.27164336821527));
#19805=CARTESIAN_POINT('Ctrl Pts',(86.6983840590322,-3.87233246567081,-2.16163565522594));
#19806=CARTESIAN_POINT('Ctrl Pts',(86.6926797336545,-3.93105046747928,-2.04898297263079));
#19807=CARTESIAN_POINT('Ctrl Pts',(86.6869809465631,-3.98971146042517,-1.93643966367071));
#19808=CARTESIAN_POINT('Ctrl Pts',(86.6812821594716,-4.04359725380571,-1.8212568445637));
#19809=CARTESIAN_POINT('Ctrl Pts',(86.6755833723802,-4.09246757400438,-1.70387738869988));
#19810=CARTESIAN_POINT('Ctrl Pts',(86.6698888386931,-4.14130141885656,-1.58658554135397));
#19811=CARTESIAN_POINT('Ctrl Pts',(86.664194305006,-4.18512708647871,-1.46710068603454));
#19812=CARTESIAN_POINT('Ctrl Pts',(86.6584997713189,-4.22375101126631,-1.34588870075753));
#19813=CARTESIAN_POINT('Ctrl Pts',(86.6528079022886,-4.26235686266863,-1.22473343449401));
#19814=CARTESIAN_POINT('Ctrl Pts',(86.6471160332582,-4.29576569288201,-1.10185302511737));
#19815=CARTESIAN_POINT('Ctrl Pts',(86.6414241642279,-4.32383285685581,-0.977731264701169));
#19816=CARTESIAN_POINT('Ctrl Pts',(86.6357339027777,-4.3518920936943,-0.853644560551788));
#19817=CARTESIAN_POINT('Ctrl Pts',(86.6300436413275,-4.37461258142881,-0.728317592141152));
#19818=CARTESIAN_POINT('Ctrl Pts',(86.6243533798773,-4.39190027218435,-0.602246626546801));
#19819=CARTESIAN_POINT('Ctrl Pts',(86.6186622188746,-4.4091906958874,-0.476155730856733));
#19820=CARTESIAN_POINT('Ctrl Pts',(86.6129710578719,-4.42104654978381,-0.349320997581811));
#19821=CARTESIAN_POINT('Ctrl Pts',(86.6072798968692,-4.42742540679828,-0.222245961126497));
#19822=CARTESIAN_POINT('Ctrl Pts',(86.6039175710256,-4.43119402198628,-0.147170299246186));
#19823=CARTESIAN_POINT('Ctrl Pts',(86.6005552451821,-4.43305191920432,-0.0720108656635592));
#19824=CARTESIAN_POINT('Ctrl Pts',(86.5971929193385,-4.43299889626848,0.00312820754919921));
#19825=CARTESIAN_POINT('',(85.3471929193076,-4.43299979596283,-0.00134498828473521));
#19826=CARTESIAN_POINT('Ctrl Pts',(86.5971929193007,-4.43299889626788,0.00312820839396158));
#19827=CARTESIAN_POINT('Ctrl Pts',(86.5906144593768,-4.4328951557713,0.150139356284962));
#19828=CARTESIAN_POINT('Ctrl Pts',(86.5840359994529,-4.42547447811461,0.296863596691938));
#19829=CARTESIAN_POINT('Ctrl Pts',(86.577457539529,-4.41084607268977,0.442635203115662));
#19830=CARTESIAN_POINT('Ctrl Pts',(86.5708439092666,-4.39613945960291,0.589186146466117));
#19831=CARTESIAN_POINT('Ctrl Pts',(86.5642302790042,-4.37414795009144,0.734774121502404));
#19832=CARTESIAN_POINT('Ctrl Pts',(86.5576166487418,-4.34503195291692,0.878741331752945));
#19833=CARTESIAN_POINT('Ctrl Pts',(86.5509627105994,-4.3157385034094,1.02358597433674));
#19834=CARTESIAN_POINT('Ctrl Pts',(86.544308772457,-4.27923354022666,1.1667899182295));
#19835=CARTESIAN_POINT('Ctrl Pts',(86.5376548343146,-4.23572891997995,1.30770391008265));
#19836=CARTESIAN_POINT('Ctrl Pts',(86.535550991924,-4.22197362765444,1.35225810087213));
#19837=CARTESIAN_POINT('Ctrl Pts',(86.5334471495333,-4.20751893789606,1.39658352669599));
#19838=CARTESIAN_POINT('Ctrl Pts',(86.5313433071426,-4.19237252860606,1.44066012001071));
#19839=CARTESIAN_POINT('Ctrl Pts',(86.5256321353073,-4.15125550076794,1.56031214311604));
#19840=CARTESIAN_POINT('Ctrl Pts',(86.519920963472,-4.10494859877901,1.67838708878222));
#19841=CARTESIAN_POINT('Ctrl Pts',(86.5142097916366,-4.05359183096115,1.79440303944377));
#19842=CARTESIAN_POINT('Ctrl Pts',(86.5085055864642,-4.00229770970667,1.91027747028398));
#19843=CARTESIAN_POINT('Ctrl Pts',(86.5028013812917,-3.94596613798181,2.0240975410831));
#19844=CARTESIAN_POINT('Ctrl Pts',(86.4970971761193,-3.88478655715426,2.13539748181774));
#19845=CARTESIAN_POINT('Ctrl Pts',(86.4913985103012,-3.82366638782589,2.24658933916493));
#19846=CARTESIAN_POINT('Ctrl Pts',(86.4856998444832,-3.757707768639,2.35526558839802));
#19847=CARTESIAN_POINT('Ctrl Pts',(86.4800011786651,-3.68714758931704,2.46098184767656));
#19848=CARTESIAN_POINT('Ctrl Pts',(86.4743066298768,-3.61663838655049,2.56662173171341));
#19849=CARTESIAN_POINT('Ctrl Pts',(86.4686120810885,-3.54153446108794,2.66930555111145));
#19850=CARTESIAN_POINT('Ctrl Pts',(86.4629175323001,-3.46211760337245,2.76861530379694));
#19851=CARTESIAN_POINT('Ctrl Pts',(86.4572251159363,-3.38273048470374,2.86788786818934));
#19852=CARTESIAN_POINT('Ctrl Pts',(86.4515326995725,-3.299033893937,2.96378856685644));
#19853=CARTESIAN_POINT('Ctrl Pts',(86.4458402832086,-3.21135154132985,3.05593034573735));
#19854=CARTESIAN_POINT('Ctrl Pts',(86.4401487980651,-3.12368353264651,3.14805705117855));
#19855=CARTESIAN_POINT('Ctrl Pts',(86.4344573129216,-3.0320313341295,3.23642577091044));
#19856=CARTESIAN_POINT('Ctrl Pts',(86.428765827778,-2.93675698656896,3.32068477905362));
#19857=CARTESIAN_POINT('Ctrl Pts',(86.4230739918002,-2.84147676611137,3.4049489810868));
#19858=CARTESIAN_POINT('Ctrl Pts',(86.4173821558224,-2.74257425155059,3.48510270324141));
#19859=CARTESIAN_POINT('Ctrl Pts',(86.4116903198446,-2.64044577389125,3.56083348601698));
#19860=CARTESIAN_POINT('Ctrl Pts',(86.4059968510407,-2.53828799847291,3.63658599380279));
#19861=CARTESIAN_POINT('Ctrl Pts',(86.4003033822368,-2.43290273943988,3.70791280043777));
#19862=CARTESIAN_POINT('Ctrl Pts',(86.394609913433,-2.3247161655013,3.77454417775934));
#19863=CARTESIAN_POINT('Ctrl Pts',(86.3889103910398,-2.2164145620233,3.84124640099427));
#19864=CARTESIAN_POINT('Ctrl Pts',(86.3832108686465,-2.10530603689519,3.90324301747818));
#19865=CARTESIAN_POINT('Ctrl Pts',(86.3775113462533,-1.9918425396822,3.96030962136956));
#19866=CARTESIAN_POINT('Ctrl Pts',(86.3718083711966,-1.87831030841598,4.01741079513661));
#19867=CARTESIAN_POINT('Ctrl Pts',(86.3661053961398,-1.76242062649897,4.06957584326114));
#19868=CARTESIAN_POINT('Ctrl Pts',(86.3604024210831,-1.64464522120501,4.11662860801986));
#19869=CARTESIAN_POINT('Ctrl Pts',(86.3546912779396,-1.52670113207099,4.16374876410723));
#19870=CARTESIAN_POINT('Ctrl Pts',(86.348980134796,-1.40686630250328,4.2057418846751));
#19871=CARTESIAN_POINT('Ctrl Pts',(86.3432689916525,-1.28562775403868,4.2424816178795));
#19872=CARTESIAN_POINT('Ctrl Pts',(86.3407661431051,-1.23249623250552,4.25858242039317));
#19873=CARTESIAN_POINT('Ctrl Pts',(86.3382632945578,-1.17909525768112,4.27367495140329));
#19874=CARTESIAN_POINT('Ctrl Pts',(86.3357604460104,-1.12546632534492,4.28775168946554));
#19875=CARTESIAN_POINT('Ctrl Pts',(86.3300492739532,-1.00309213688677,4.31987295911356));
#19876=CARTESIAN_POINT('Ctrl Pts',(86.324338101896,-0.879152957298337,4.34680069676259));
#19877=CARTESIAN_POINT('Ctrl Pts',(86.3186269298387,-0.754127476099715,
4.3683842264379));
#19878=CARTESIAN_POINT('Ctrl Pts',(86.3129227244419,-0.629254504764249,
4.38994142787095));
#19879=CARTESIAN_POINT('Ctrl Pts',(86.3072185190451,-0.503298258058655,
4.40616732349194));
#19880=CARTESIAN_POINT('Ctrl Pts',(86.3015143136482,-0.376751394775666,
4.41696132952674));
#19881=CARTESIAN_POINT('Ctrl Pts',(86.2958156476036,-0.2503274211148,4.42774485350541));
#19882=CARTESIAN_POINT('Ctrl Pts',(86.290116981559,-0.123314367625963,4.4331069504743));
#19883=CARTESIAN_POINT('Ctrl Pts',(86.2844183155143,0.00378659940249116,
4.43299838277265));
#19884=CARTESIAN_POINT('Ctrl Pts',(86.2787237664975,0.130795741746123,4.43288989350625));
#19885=CARTESIAN_POINT('Ctrl Pts',(86.2730292174807,0.25789227342292,4.42731860619702));
#19886=CARTESIAN_POINT('Ctrl Pts',(86.2673346684638,0.384572087274374,4.41628727662608));
#19887=CARTESIAN_POINT('Ctrl Pts',(86.2616422518694,0.511204463677064,4.40526007792743));
#19888=CARTESIAN_POINT('Ctrl Pts',(86.255949835275,0.637420035520863,4.3887769369016));
#19889=CARTESIAN_POINT('Ctrl Pts',(86.2502574186806,0.762717209312201,4.36689265480834));
#19890=CARTESIAN_POINT('Ctrl Pts',(86.2445659333053,0.887993885812354,4.34501195275195));
#19891=CARTESIAN_POINT('Ctrl Pts',(86.23887444793,1.01235207003775,4.31773193577678));
#19892=CARTESIAN_POINT('Ctrl Pts',(86.2331829625547,1.13529831748097,4.28515889207447));
#19893=CARTESIAN_POINT('Ctrl Pts',(86.2274911263441,1.25825214359147,4.2525838405007));
#19894=CARTESIAN_POINT('Ctrl Pts',(86.2217992901336,1.37979347395702,4.21471521550547));
#19895=CARTESIAN_POINT('Ctrl Pts',(86.216107453923,1.49944253063066,4.17170961325641));
#19896=CARTESIAN_POINT('Ctrl Pts',(86.2104139848857,1.61912591123335,4.12869167391685));
#19897=CARTESIAN_POINT('Ctrl Pts',(86.2047205158484,1.7369155627658,4.08053396067619));
#19898=CARTESIAN_POINT('Ctrl Pts',(86.1990270468111,1.85235072611109,4.02744159330408));
#19899=CARTESIAN_POINT('Ctrl Pts',(86.1933275241846,1.96790862606085,3.97429277539554));
#19900=CARTESIAN_POINT('Ctrl Pts',(86.1876280015581,2.08110667651898,3.91619899451292));
#19901=CARTESIAN_POINT('Ctrl Pts',(86.1819284789316,2.19150754275433,3.85341195436601));
#19902=CARTESIAN_POINT('Ctrl Pts',(86.1762255036414,2.30197528776012,3.79058687900988));
#19903=CARTESIAN_POINT('Ctrl Pts',(86.1705225283512,2.40964213533218,3.72306309234928));
#19904=CARTESIAN_POINT('Ctrl Pts',(86.164819553061,2.51409993842635,3.65113550825009));
#19905=CARTESIAN_POINT('Ctrl Pts',(86.1591084096857,2.61870735118599,3.57910490588441));
#19906=CARTESIAN_POINT('Ctrl Pts',(86.1533972663104,2.72009622403066,3.50265815158753));
#19907=CARTESIAN_POINT('Ctrl Pts',(86.1476861229351,2.81789137980966,3.42213050183572));
#19908=CARTESIAN_POINT('Ctrl Pts',(86.145183276916,2.8607490354903,3.38684014150711));
#19909=CARTESIAN_POINT('Ctrl Pts',(86.142680430897,2.90291698057388,3.35076651150491));
#19910=CARTESIAN_POINT('Ctrl Pts',(86.140177584878,2.94436594871412,3.31393997532436));
#19911=CARTESIAN_POINT('Ctrl Pts',(86.1344664130515,3.03894714838806,3.2299065692331));
#19912=CARTESIAN_POINT('Ctrl Pts',(86.128755241225,3.1300738605265,3.14169123977798));
#19913=CARTESIAN_POINT('Ctrl Pts',(86.1230440693985,3.21735528449407,3.04960882300305));
#19914=CARTESIAN_POINT('Ctrl Pts',(86.1173398642333,3.30453023992418,2.95763873116275));
#19915=CARTESIAN_POINT('Ctrl Pts',(86.111635659068,3.38786896680283,2.86181122398429));
#19916=CARTESIAN_POINT('Ctrl Pts',(86.1059314539028,3.46701460729642,2.7624805361836));
#19917=CARTESIAN_POINT('Ctrl Pts',(86.1002327880902,3.54608338947103,2.66324630839815));
#19918=CARTESIAN_POINT('Ctrl Pts',(86.0945341222777,3.6209669404316,2.56051597977903));
#19919=CARTESIAN_POINT('Ctrl Pts',(86.0888354564652,3.69134641690937,2.45467933351189));
#19920=CARTESIAN_POINT('Ctrl Pts',(86.0831409076808,3.76167504740151,2.34891914943038));
#19921=CARTESIAN_POINT('Ctrl Pts',(86.0774463588963,3.82750585956527,2.24005744552949));
#19922=CARTESIAN_POINT('Ctrl Pts',(86.0717518101118,3.88856164977795,2.12851527969056));
#19923=CARTESIAN_POINT('Ctrl Pts',(86.0660593937494,3.94959457659708,2.01701488273918));
#19924=CARTESIAN_POINT('Ctrl Pts',(86.0603669773869,4.005855845439,1.90283636919786));
#19925=CARTESIAN_POINT('Ctrl Pts',(86.0546745610245,4.05711295984482,1.78642756110042));
#19926=CARTESIAN_POINT('Ctrl Pts',(86.0489830758808,4.10836168913209,1.67003779624543));
#19927=CARTESIAN_POINT('Ctrl Pts',(86.0432915907371,4.15460773150647,1.55141882773757));
#19928=CARTESIAN_POINT('Ctrl Pts',(86.0376001055934,4.19566595728358,1.43104024223349));
#19929=CARTESIAN_POINT('Ctrl Pts',(86.0319082696138,4.23672671398111,1.31065423632547));
#19930=CARTESIAN_POINT('Ctrl Pts',(86.0262164336343,4.27259888919706,1.18850877549396));
#19931=CARTESIAN_POINT('Ctrl Pts',(86.0205245976548,4.30314679802921,1.06508996550101));
#19932=CARTESIAN_POINT('Ctrl Pts',(86.0148311288477,4.33370347019691,0.941635750124001));
#19933=CARTESIAN_POINT('Ctrl Pts',(86.0091376600406,4.35893274162317,0.816907846213275));
#19934=CARTESIAN_POINT('Ctrl Pts',(86.0034441912335,4.3787498547006,0.691403435021481));
#19935=CARTESIAN_POINT('Ctrl Pts',(85.9977446688347,4.3985880383617,0.565765581022593));
#19936=CARTESIAN_POINT('Ctrl Pts',(85.9920451464359,4.41300251188449,0.439349965915013));
#19937=CARTESIAN_POINT('Ctrl Pts',(85.9863456240371,4.42196027333882,0.312660104607597));
#19938=CARTESIAN_POINT('Ctrl Pts',(85.9806426489735,4.4309234612387,0.18589349693477));
#19939=CARTESIAN_POINT('Ctrl Pts',(85.9749396739098,4.43442334099854,0.058852710456793));
#19940=CARTESIAN_POINT('Ctrl Pts',(85.9692366988462,4.43247905402526,-0.0679590731790049));
#19941=CARTESIAN_POINT('Ctrl Pts',(85.9635255556938,4.43053198234603,-0.194952483052602));
#19942=CARTESIAN_POINT('Ctrl Pts',(85.9578144125414,4.4231251975759,-0.321715837576687));
#19943=CARTESIAN_POINT('Ctrl Pts',(85.952103269389,4.41032969502454,-0.447751025889136));
#19944=CARTESIAN_POINT('Ctrl Pts',(85.9496004208412,4.40472220032081,-0.50298462442174));
#19945=CARTESIAN_POINT('Ctrl Pts',(85.9470975722934,4.39808044483649,-0.558078504930061));
#19946=CARTESIAN_POINT('Ctrl Pts',(85.9445947237456,4.3904134714002,-0.612991476407032));
#19947=CARTESIAN_POINT('Ctrl Pts',(85.9388835519819,4.37291844468733,-0.738295667279145));
#19948=CARTESIAN_POINT('Ctrl Pts',(85.9331723802182,4.35002781647401,-0.863043575908686));
#19949=CARTESIAN_POINT('Ctrl Pts',(85.9274612084545,4.32178692539746,-0.986735411072074));
#19950=CARTESIAN_POINT('Ctrl Pts',(85.9217570033536,4.29358048342722,-1.11027636313593));
#19951=CARTESIAN_POINT('Ctrl Pts',(85.9160527982526,4.26003685086349,-1.23276341883413));
#19952=CARTESIAN_POINT('Ctrl Pts',(85.9103485931516,4.22125297409735,-1.35370319076018));
#19953=CARTESIAN_POINT('Ctrl Pts',(85.9046499274048,4.18250676035782,-1.47452551806159));
#19954=CARTESIAN_POINT('Ctrl Pts',(85.898951261658,4.13853054960645,-1.59380317353583));
#19955=CARTESIAN_POINT('Ctrl Pts',(85.8932525959112,4.08947194930563,-1.7110546969172));
#19956=CARTESIAN_POINT('Ctrl Pts',(85.8875580471937,4.04044879163431,-1.82822151135302));
#19957=CARTESIAN_POINT('Ctrl Pts',(85.8818634984763,3.98635070594406,-1.94336474011074));
#19958=CARTESIAN_POINT('Ctrl Pts',(85.8761689497589,3.92737441392121,-2.05602023649501));
#19959=CARTESIAN_POINT('Ctrl Pts',(85.8704765334651,3.86842020660578,-2.16863354705188));
#19960=CARTESIAN_POINT('Ctrl Pts',(85.8647841171714,3.80459160993615,-2.27876062446177));
#19961=CARTESIAN_POINT('Ctrl Pts',(85.8590917008776,3.73613240679481,-2.38595968928598));
#19962=CARTESIAN_POINT('Ctrl Pts',(85.8534002158037,3.66768440286324,-2.49314121746413));
#19963=CARTESIAN_POINT('Ctrl Pts',(85.8477087307297,3.59460751399057,-2.59739534952529));
#19964=CARTESIAN_POINT('Ctrl Pts',(85.8420172456557,3.51718989812161,-2.69830765861702));
#19965=CARTESIAN_POINT('Ctrl Pts',(85.8363254097469,3.43976751007137,-2.79922618815132));
#19966=CARTESIAN_POINT('Ctrl Pts',(85.8306335738381,3.35800410582481,-2.89680216830276));
#19967=CARTESIAN_POINT('Ctrl Pts',(85.8249417379292,3.27222900507449,-2.99065316249631));
#19968=CARTESIAN_POINT('Ctrl Pts',(85.8192482691937,3.18642929787401,-3.08453107988542));
#19969=CARTESIAN_POINT('Ctrl Pts',(85.8135548004581,3.09661587392479,-3.17468159099211));
#19970=CARTESIAN_POINT('Ctrl Pts',(85.8078613317226,3.00315550632496,-3.26075850145792));
#19971=CARTESIAN_POINT('Ctrl Pts',(85.8021618093963,2.90959576682281,-3.34692693335209));
#19972=CARTESIAN_POINT('Ctrl Pts',(85.7964622870699,2.8123816354345,-3.42901284610396));
#19973=CARTESIAN_POINT('Ctrl Pts',(85.7907627647436,2.7119138516841,-3.50670960603297));
#19974=CARTESIAN_POINT('Ctrl Pts',(85.7850597897531,2.61138520642603,-3.58445343320856));
#19975=CARTESIAN_POINT('Ctrl Pts',(85.7793568147625,2.50759930776965,-3.6578025807879));
#19976=CARTESIAN_POINT('Ctrl Pts',(85.773653839772,2.40098552823103,-3.72649399479258));
#19977=CARTESIAN_POINT('Ctrl Pts',(85.767942696693,2.29421905105937,-3.79528379210543));
#19978=CARTESIAN_POINT('Ctrl Pts',(85.762231553614,2.18461694940847,-3.85940233424258));
#19979=CARTESIAN_POINT('Ctrl Pts',(85.756520410535,2.07263312563219,-3.91863253272518));
#19980=CARTESIAN_POINT('Ctrl Pts',(85.7540175612277,2.02355737461579,-3.94458955379628));
#19981=CARTESIAN_POINT('Ctrl Pts',(85.7515147119205,1.97402446467942,-3.96960837257711));
#19982=CARTESIAN_POINT('Ctrl Pts',(85.7490118626132,1.92407368970206,-3.99367367677885));
#19983=CARTESIAN_POINT('Ctrl Pts',(85.7433006900686,1.81009259870891,-4.04858753205416));
#19984=CARTESIAN_POINT('Ctrl Pts',(85.7375895175239,1.6935829226719,-4.09870261257304));
#19985=CARTESIAN_POINT('Ctrl Pts',(85.7318783449793,1.57498573745547,-4.1437795461163));
#19986=CARTESIAN_POINT('Ctrl Pts',(85.7261741390951,1.45653322066087,-4.18880149345712));
#19987=CARTESIAN_POINT('Ctrl Pts',(85.7204699332109,1.33599863063617,-4.22879737994613));
#19988=CARTESIAN_POINT('Ctrl Pts',(85.7147657273267,1.21384632721907,-4.26357433310324));
#19989=CARTESIAN_POINT('Ctrl Pts',(85.7090670607953,1.09181264587102,-4.29831751437048));
#19990=CARTESIAN_POINT('Ctrl Pts',(85.7033683942639,0.968164758856482,-4.32785173842749));
#19991=CARTESIAN_POINT('Ctrl Pts',(85.6976697277325,0.843385188467329,-4.35203290703022));
#19992=CARTESIAN_POINT('Ctrl Pts',(85.6919751782301,0.718695765677514,-4.37619660583167));
#19993=CARTESIAN_POINT('Ctrl Pts',(85.6862806287277,0.59287667729466,-4.39501487067645));
#19994=CARTESIAN_POINT('Ctrl Pts',(85.6805860792253,0.466423267717234,-4.4083940766828));
#19995=CARTESIAN_POINT('Ctrl Pts',(85.6748936621488,0.34001721088171,-4.42176827260605));
#19996=CARTESIAN_POINT('Ctrl Pts',(85.6692012450724,0.212977701444396,-4.42970741750697));
#19997=CARTESIAN_POINT('Ctrl Pts',(85.6635088279959,0.0858075618328727,
-4.43216945325112));
#19998=CARTESIAN_POINT('Ctrl Pts',(85.6578173421409,-0.0413417740395733,
-4.4346310862313));
#19999=CARTESIAN_POINT('Ctrl Pts',(85.6521258562858,-0.168621298641298,
-4.4316173845517));
#20000=CARTESIAN_POINT('Ctrl Pts',(85.6464343704308,-0.295526349723232,
-4.42313838542491));
#20001=CARTESIAN_POINT('Ctrl Pts',(85.6407425337434,-0.422439223437343,
-4.41465886363893));
#20002=CARTESIAN_POINT('Ctrl Pts',(85.635050697056,-0.54897717943748,-4.4007134009788));
#20003=CARTESIAN_POINT('Ctrl Pts',(85.6293588603686,-0.674639356838034,
-4.3813640271273));
#20004=CARTESIAN_POINT('Ctrl Pts',(85.6236653908578,-0.800337583084492,
-4.36200910249982));
#20005=CARTESIAN_POINT('Ctrl Pts',(85.617971921347,-0.925159136584635,-4.33724724346669));
#20006=CARTESIAN_POINT('Ctrl Pts',(85.6122784518362,-1.04861255243217,-4.30719174345439));
#20007=CARTESIAN_POINT('Ctrl Pts',(85.6065789287439,-1.17219723012678,-4.27710428693106));
#20008=CARTESIAN_POINT('Ctrl Pts',(85.6008794056515,-1.29441047758078,-4.24171204607327));
#20009=CARTESIAN_POINT('Ctrl Pts',(85.5951798825591,-1.41477492088964,-4.20117851599069));
#20010=CARTESIAN_POINT('Ctrl Pts',(85.5894769068067,-1.53521227863213,-4.16062043148565));
#20011=CARTESIAN_POINT('Ctrl Pts',(85.5837739310544,-1.65379822927678,-4.11491499663148));
#20012=CARTESIAN_POINT('Ctrl Pts',(85.578070955302,-1.77007579171369,-4.06427369791814));
#20013=CARTESIAN_POINT('Ctrl Pts',(85.5723598114742,-1.88651989245249,-4.01355986830789));
#20014=CARTESIAN_POINT('Ctrl Pts',(85.5666486676464,-2.0006486453519,-3.95789623353993));
#20015=CARTESIAN_POINT('Ctrl Pts',(85.5609375238187,-2.1120297225665,-3.89754017952293));
#20016=CARTESIAN_POINT('Ctrl Pts',(85.5584346830394,-2.16084115342805,-3.87108985751671));
#20017=CARTESIAN_POINT('Ctrl Pts',(85.5559318422602,-2.20912526059895,-3.84373890644368));
#20018=CARTESIAN_POINT('Ctrl Pts',(85.5534290014809,-2.25684751509205,-3.8155115376084));
#20019=CARTESIAN_POINT('Ctrl Pts',(85.5477178303485,-2.3657437599082,-3.75110019535618));
#20020=CARTESIAN_POINT('Ctrl Pts',(85.5420066592161,-2.47204829966788,-3.68192387470062));
#20021=CARTESIAN_POINT('Ctrl Pts',(85.5362954880837,-2.57531737322834,-3.60821693183049));
#20022=CARTESIAN_POINT('Ctrl Pts',(85.5305912836099,-2.67846047606241,-3.53459989890933));
#20023=CARTESIAN_POINT('Ctrl Pts',(85.5248870791361,-2.77857515714656,-3.45646346872346));
#20024=CARTESIAN_POINT('Ctrl Pts',(85.5191828746622,-2.87524344395868,-3.37408715625021));
#20025=CARTESIAN_POINT('Ctrl Pts',(85.5134842095377,-2.97181785625936,-3.29179083936127));
#20026=CARTESIAN_POINT('Ctrl Pts',(85.5077855444132,-3.06495223182522,-3.20526309055057));
#20027=CARTESIAN_POINT('Ctrl Pts',(85.5020868792887,-3.15425911922232,-3.11482558240471));
#20028=CARTESIAN_POINT('Ctrl Pts',(85.4963923311881,-3.24350148649438,-3.02445341120546));
#20029=CARTESIAN_POINT('Ctrl Pts',(85.4906977830874,-3.32892158964286,-2.93017738557085));
#20030=CARTESIAN_POINT('Ctrl Pts',(85.4850032349868,-3.41016687327916,-2.83235783339419));
#20031=CARTESIAN_POINT('Ctrl Pts',(85.4793108192995,-3.49138173333796,-2.73457491129122));
#20032=CARTESIAN_POINT('Ctrl Pts',(85.4736184036121,-3.56842462768289,-2.63325140758664));
#20033=CARTESIAN_POINT('Ctrl Pts',(85.4679259879248,-3.6409817698824,-2.5287824642274));
#20034=CARTESIAN_POINT('Ctrl Pts',(85.4622345034506,-3.71352704257538,-2.42433061077508));
#20035=CARTESIAN_POINT('Ctrl Pts',(85.4565430189765,-3.78158779513353,-2.31673466889177));
#20036=CARTESIAN_POINT('Ctrl Pts',(85.4508515345023,-3.84489257604527,-2.20642019540068));
#20037=CARTESIAN_POINT('Ctrl Pts',(85.445159699186,-3.90820125927502,-2.09609892175721));
#20038=CARTESIAN_POINT('Ctrl Pts',(85.4394678638698,-3.96675318908799,-1.98305912942441));
#20039=CARTESIAN_POINT('Ctrl Pts',(85.4337760285535,-4.02032229097474,-1.86775203833154));
#20040=CARTESIAN_POINT('Ctrl Pts',(85.4280825604026,-4.07390676039728,-1.75241186873282));
#20041=CARTESIAN_POINT('Ctrl Pts',(85.4223890922517,-4.12250539013308,-1.63480346830541));
#20042=CARTESIAN_POINT('Ctrl Pts',(85.4166956241009,-4.16593997808967,-1.51539866007405));
#20043=CARTESIAN_POINT('Ctrl Pts',(85.4109961023443,-4.20942074806791,-1.39586689414151));
#20044=CARTESIAN_POINT('Ctrl Pts',(85.4052965805877,-4.2477263769179,-1.2745352822411));
#20045=CARTESIAN_POINT('Ctrl Pts',(85.3995970588311,-4.28072825419882,-1.15189175433453));
#20046=CARTESIAN_POINT('Ctrl Pts',(85.3938940844026,-4.31375012344783,-1.02917393109399));
#20047=CARTESIAN_POINT('Ctrl Pts',(85.388191109974,-4.34146175371432,-0.905142997552945));
#20048=CARTESIAN_POINT('Ctrl Pts',(85.3824881355455,-4.36378578070761,-0.78029652062154));
#20049=CARTESIAN_POINT('Ctrl Pts',(85.3767769930118,-4.386141781367,-0.655271231884875));
#20050=CARTESIAN_POINT('Ctrl Pts',(85.371065850478,-4.40309471772306,-0.529428462110429));
#20051=CARTESIAN_POINT('Ctrl Pts',(85.3653547079443,-4.41461909282753,-0.403270709626425));
#20052=CARTESIAN_POINT('Ctrl Pts',(85.362851852079,-4.41966954458104,-0.347983231001733));
#20053=CARTESIAN_POINT('Ctrl Pts',(85.3603489962138,-4.42367808959139,-0.292635258380975));
#20054=CARTESIAN_POINT('Ctrl Pts',(85.3578461403485,-4.42664573287411,-0.237268952093333));
#20055=CARTESIAN_POINT('Ctrl Pts',(85.3542950666785,-4.43085625097439,-0.15871475518988));
#20056=CARTESIAN_POINT('Ctrl Pts',(85.3507439930085,-4.4329759173203,-0.0800475054487878));
#20057=CARTESIAN_POINT('Ctrl Pts',(85.3471929193385,-4.43299979596262,-0.00134498896944356));
#20058=CARTESIAN_POINT('',(84.0971929193621,-4.43299983598826,-0.00120587233263061));
#20059=CARTESIAN_POINT('Ctrl Pts',(85.3471929193076,-4.43299979596283,-0.00134498828473226));
#20060=CARTESIAN_POINT('Ctrl Pts',(85.3415282140113,-4.43303788737273,0.124201988030421));
#20061=CARTESIAN_POINT('Ctrl Pts',(85.3358635087149,-4.42773831151435,0.249954571554026));
#20062=CARTESIAN_POINT('Ctrl Pts',(85.3301988034186,-4.41707483986748,0.375418245440573));
#20063=CARTESIAN_POINT('Ctrl Pts',(85.3245408265264,-4.4064240340422,0.500732896517129));
#20064=CARTESIAN_POINT('Ctrl Pts',(85.3188828496342,-4.39042203787962,0.625758919050579));
#20065=CARTESIAN_POINT('Ctrl Pts',(85.313224872742,-4.36909462571147,0.750000767719023));
#20066=CARTESIAN_POINT('Ctrl Pts',(85.3075721479842,-4.34778701115638,0.874127286312468));
#20067=CARTESIAN_POINT('Ctrl Pts',(85.3019194232265,-4.32116388290341,0.997470680771747));
#20068=CARTESIAN_POINT('Ctrl Pts',(85.2962666984688,-4.28930285940635,1.11954007533831));
#20069=CARTESIAN_POINT('Ctrl Pts',(85.2906175557129,-4.25746202550785,1.24153211733417));
#20070=CARTESIAN_POINT('Ctrl Pts',(85.284968412957,-4.2203900012271,1.36225137334623));
#20071=CARTESIAN_POINT('Ctrl Pts',(85.2793192702011,-4.17821546973224,1.4812172320393));
#20072=CARTESIAN_POINT('Ctrl Pts',(85.2736719911722,-4.13605485217438,1.6001438423186));
#20073=CARTESIAN_POINT('Ctrl Pts',(85.2680247121434,-4.0887952099321,1.71731782282565));
#20074=CARTESIAN_POINT('Ctrl Pts',(85.2623774331146,-4.03661490893153,1.83227429087233));
#20075=CARTESIAN_POINT('Ctrl Pts',(85.2567306908283,-3.98443956737916,1.94721983294431));
#20076=CARTESIAN_POINT('Ctrl Pts',(85.251083948542,-3.92734466520962,2.0599479117584));
#20077=CARTESIAN_POINT('Ctrl Pts',(85.2454372062557,-3.86555623384926,2.1700147471732));
#20078=CARTESIAN_POINT('Ctrl Pts',(85.239789674387,-3.8037591626301,2.28009697320231));
#20079=CARTESIAN_POINT('Ctrl Pts',(85.2341421425184,-3.73726745645285,2.3875168617243));
#20080=CARTESIAN_POINT('Ctrl Pts',(85.2284946106497,-3.66635220006584,2.49185684682576));
#20081=CARTESIAN_POINT('Ctrl Pts',(85.2228415718791,-3.5953677942917,2.59629857372989));
#20082=CARTESIAN_POINT('Ctrl Pts',(85.2171885331084,-3.51995145158518,2.69765406196533));
#20083=CARTESIAN_POINT('Ctrl Pts',(85.2115354943378,-3.44041671265339,2.79553605651854));
#20084=CARTESIAN_POINT('Ctrl Pts',(85.2058796766761,-3.36084287645444,2.89346616738599));
#20085=CARTESIAN_POINT('Ctrl Pts',(85.2002238590145,-3.2771468807361,2.98791907923903));
#20086=CARTESIAN_POINT('Ctrl Pts',(85.1945680413529,-3.18968041661611,3.07854313594201));
#20087=CARTESIAN_POINT('Ctrl Pts',(85.1889034265582,-3.10207790600888,3.16930815049322));
#20088=CARTESIAN_POINT('Ctrl Pts',(85.1832388117635,-3.01069350446996,3.25623213115127));
#20089=CARTESIAN_POINT('Ctrl Pts',(85.1775741969688,-2.91591382201898,3.33900218367084));
#20090=CARTESIAN_POINT('Ctrl Pts',(85.1724705577179,-2.83052031776918,3.41357539017258));
#20091=CARTESIAN_POINT('Ctrl Pts',(85.167366918467,-2.74237132042908,3.48477708333452));
#20092=CARTESIAN_POINT('Ctrl Pts',(85.1622632792161,-2.65176930431954,3.55240883861481));
#20093=CARTESIAN_POINT('Ctrl Pts',(85.1565521021975,-2.55038201442544,3.62809148534929));
#20094=CARTESIAN_POINT('Ctrl Pts',(85.1508409251788,-2.44559573299975,3.69954696648941));
#20095=CARTESIAN_POINT('Ctrl Pts',(85.1451297481602,-2.33779766712063,3.76645603553332));
#20096=CARTESIAN_POINT('Ctrl Pts',(85.1394255377919,-2.23013109627913,3.83328348705951));
#20097=CARTESIAN_POINT('Ctrl Pts',(85.1337213274237,-2.11946038629147,3.89557535113553));
#20098=CARTESIAN_POINT('Ctrl Pts',(85.1280171170554,-2.00620448474273,3.95305357482012));
#20099=CARTESIAN_POINT('Ctrl Pts',(85.1223184460353,-1.8930585657898,4.01047598150836));
#20100=CARTESIAN_POINT('Ctrl Pts',(85.1166197750152,-1.77733280469662,4.06309386980102));
#20101=CARTESIAN_POINT('Ctrl Pts',(85.110921103995,-1.65947329705126,4.11067359156305));
#20102=CARTESIAN_POINT('Ctrl Pts',(85.1052265500045,-1.54169893751839,4.15821893914871));
#20103=CARTESIAN_POINT('Ctrl Pts',(85.0995319960139,-1.4217942684245,4.20073321568559));
#20104=CARTESIAN_POINT('Ctrl Pts',(85.0938374420234,-1.30022761611469,4.23802986613978));
#20105=CARTESIAN_POINT('Ctrl Pts',(85.0881450204762,-1.17870648694803,4.27531255009307));
#20106=CARTESIAN_POINT('Ctrl Pts',(85.082452598929,-1.05552499301529,4.30738137598142));
#20107=CARTESIAN_POINT('Ctrl Pts',(85.0767601773817,-0.931168654758774,
4.33409897630346));
#20108=CARTESIAN_POINT('Ctrl Pts',(85.0710686870681,-0.806832660181519,
4.36081220584474));
#20109=CARTESIAN_POINT('Ctrl Pts',(85.0653771967545,-0.681322593683535,
4.3821758672857));
#20110=CARTESIAN_POINT('Ctrl Pts',(85.0596857064408,-0.55513573651598,4.39810337691633));
#20111=CARTESIAN_POINT('Ctrl Pts',(85.0539938653117,-0.428941101368054,
4.41403186829625));
#20112=CARTESIAN_POINT('Ctrl Pts',(85.0483020241826,-0.302069988610285,
4.42452349144645));
#20113=CARTESIAN_POINT('Ctrl Pts',(85.0426101830535,-0.175025883421164,
4.42954342343911));
#20114=CARTESIAN_POINT('Ctrl Pts',(85.0369167091228,-0.0479453334641138,
4.43456479548485));
#20115=CARTESIAN_POINT('Ctrl Pts',(85.031223235192,0.0793079089593364,4.43411133804602));
#20116=CARTESIAN_POINT('Ctrl Pts',(85.0255297612612,0.206229785507273,4.42820034275434));
#20117=CARTESIAN_POINT('Ctrl Pts',(85.0198302338054,0.333286610378385,4.42228306266034));
#20118=CARTESIAN_POINT('Ctrl Pts',(85.0141307063495,0.46001096684867,4.41089667762191));
#20119=CARTESIAN_POINT('Ctrl Pts',(85.0084311788937,0.585903034864924,4.39411044851356));
#20120=CARTESIAN_POINT('Ctrl Pts',(85.0027281988043,0.71187136520028,4.3773140507204));
#20121=CARTESIAN_POINT('Ctrl Pts',(84.9970252187149,0.837006010321613,4.35511136207105));
#20122=CARTESIAN_POINT('Ctrl Pts',(84.9913222386254,0.960817996480046,4.32762264732498));
#20123=CARTESIAN_POINT('Ctrl Pts',(84.9856110905386,1.08480731027524,4.3000945623291));
#20124=CARTESIAN_POINT('Ctrl Pts',(84.9798999424518,1.20746979779887,4.26726543705814));
#20125=CARTESIAN_POINT('Ctrl Pts',(84.974188794365,1.32833191332227,4.22930530087975));
#20126=CARTESIAN_POINT('Ctrl Pts',(84.9716860022713,1.3812972265245,4.2126700591981));
#20127=CARTESIAN_POINT('Ctrl Pts',(84.9691832101775,1.43391704778814,4.19505005678398));
#20128=CARTESIAN_POINT('Ctrl Pts',(84.9666804180838,1.486152860131,4.1764624595852));
#20129=CARTESIAN_POINT('Ctrl Pts',(84.960969254316,1.6053506471065,4.13404710598173));
#20130=CARTESIAN_POINT('Ctrl Pts',(84.9552580905483,1.72291503430886,4.0864593429778));
#20131=CARTESIAN_POINT('Ctrl Pts',(84.9495469267805,1.83836565569993,4.03384440899038));
#20132=CARTESIAN_POINT('Ctrl Pts',(84.9438427296566,1.95367544706221,3.98129365623108));
#20133=CARTESIAN_POINT('Ctrl Pts',(84.9381385325326,2.06687624225092,3.92372809667851));
#20134=CARTESIAN_POINT('Ctrl Pts',(84.9324343354087,2.177504359174,3.86134222334388));
#20135=CARTESIAN_POINT('Ctrl Pts',(84.926735677611,2.28802504551298,3.79901693271641));
#20136=CARTESIAN_POINT('Ctrl Pts',(84.9210370198133,2.39597767915769,3.73188083776983));
#20137=CARTESIAN_POINT('Ctrl Pts',(84.9153383620155,2.50092048073354,3.66017564456236));
#20138=CARTESIAN_POINT('Ctrl Pts',(84.9096438212103,2.60578746643538,3.58852225473552));
#20139=CARTESIAN_POINT('Ctrl Pts',(84.903949280405,2.7076486194383,3.51230656094385));
#20140=CARTESIAN_POINT('Ctrl Pts',(84.8982547395997,2.80608902669326,3.43181488053649));
#20141=CARTESIAN_POINT('Ctrl Pts',(84.8925623311348,2.90449257259949,3.35135334051542));
#20142=CARTESIAN_POINT('Ctrl Pts',(84.8868699226699,2.99947761112639,3.26661924977286));
#20143=CARTESIAN_POINT('Ctrl Pts',(84.881177514205,3.09066063112659,3.17794050655518));
#20144=CARTESIAN_POINT('Ctrl Pts',(84.8754860369058,3.18182873538483,3.08927626942922));
#20145=CARTESIAN_POINT('Ctrl Pts',(84.8697945596065,3.26919577215273,2.99666894151143));
#20146=CARTESIAN_POINT('Ctrl Pts',(84.8641030823072,3.35241397309439,2.90048436523997));
#20147=CARTESIAN_POINT('Ctrl Pts',(84.8584112541108,3.43563730469505,2.80429385889244));
#20148=CARTESIAN_POINT('Ctrl Pts',(84.8527194259144,3.51471103055647,2.70452596741517));
#20149=CARTESIAN_POINT('Ctrl Pts',(84.847027597718,3.58932701920446,2.60158039453114));
#20150=CARTESIAN_POINT('Ctrl Pts',(84.8413341366245,3.66396441402169,2.49860528815978));
#20151=CARTESIAN_POINT('Ctrl Pts',(84.8356406755309,3.7341412933782,2.39245100990343));
#20152=CARTESIAN_POINT('Ctrl Pts',(84.8299472144373,3.79959257901694,2.28354663483787));
#20153=CARTESIAN_POINT('Ctrl Pts',(84.8242476996059,3.86511345763529,2.17452646403387));
#20154=CARTESIAN_POINT('Ctrl Pts',(84.8185481847745,3.92589850451247,2.06275070051456));
#20155=CARTESIAN_POINT('Ctrl Pts',(84.8128486699432,3.98172824133116,1.94867370593075));
#20156=CARTESIAN_POINT('Ctrl Pts',(84.8071457023737,4.03759179953024,1.83452760406385));
#20157=CARTESIAN_POINT('Ctrl Pts',(84.8014427348042,4.08849390791508,1.7180778591149));
#20158=CARTESIAN_POINT('Ctrl Pts',(84.7957397672347,4.13426354847867,1.59979808467211));
#20159=CARTESIAN_POINT('Ctrl Pts',(84.7900286313998,4.18009874413595,1.48134890007885));
#20160=CARTESIAN_POINT('Ctrl Pts',(84.7843174955649,4.22078666584669,1.36106482950147));
#20161=CARTESIAN_POINT('Ctrl Pts',(84.77860635973,4.25620626483195,1.23943423835443));
#20162=CARTESIAN_POINT('Ctrl Pts',(84.7761034254704,4.27172908381607,1.18612901459703));
#20163=CARTESIAN_POINT('Ctrl Pts',(84.7736004912109,4.28624069249104,1.13256529713689));
#20164=CARTESIAN_POINT('Ctrl Pts',(84.7710975569514,4.29973402033953,1.07878466541515));
#20165=CARTESIAN_POINT('Ctrl Pts',(84.765386387843,4.33052295412135,0.956068584740487));
#20166=CARTESIAN_POINT('Ctrl Pts',(84.7596752187347,4.35610165707599,0.831844066722693));
#20167=CARTESIAN_POINT('Ctrl Pts',(84.7539640496263,4.37632466568423,0.706591409885409));
#20168=CARTESIAN_POINT('Ctrl Pts',(84.7482598472653,4.39652300533454,0.58149154201145));
#20169=CARTESIAN_POINT('Ctrl Pts',(84.7425556449042,4.41137858508747,0.455366421148501));
#20170=CARTESIAN_POINT('Ctrl Pts',(84.7368514425432,4.42079618250531,0.328709769776476));
#20171=CARTESIAN_POINT('Ctrl Pts',(84.7311527796165,4.43020463435658,0.202176116530777));
#20172=CARTESIAN_POINT('Ctrl Pts',(84.7254541166898,4.43418558268488,0.0751123557100857));
#20173=CARTESIAN_POINT('Ctrl Pts',(84.719755453763,4.43269524060635,-0.0519798413408479));
#20174=CARTESIAN_POINT('Ctrl Pts',(84.7140609079416,4.43120597525325,-0.178980218263863));
#20175=CARTESIAN_POINT('Ctrl Pts',(84.7083663621202,4.42425329149755,-0.30600859275918));
#20176=CARTESIAN_POINT('Ctrl Pts',(84.7026718162988,4.41184542479171,-0.432560917957741));
#20177=CARTESIAN_POINT('Ctrl Pts',(84.6969794030022,4.39944220465206,-0.559065851145361));
#20178=CARTESIAN_POINT('Ctrl Pts',(84.6912869897057,4.38158790239047,-0.685094692894899));
#20179=CARTESIAN_POINT('Ctrl Pts',(84.6855945764091,4.35834276853733,-0.810146475606956));
#20180=CARTESIAN_POINT('Ctrl Pts',(84.6799030943942,4.33510143759976,-0.935177799784545));
#20181=CARTESIAN_POINT('Ctrl Pts',(84.6742116123793,4.30647110225273,-1.05923199058084));
#20182=CARTESIAN_POINT('Ctrl Pts',(84.6685201303644,4.27256340833325,-1.18181678858092));
#20183=CARTESIAN_POINT('Ctrl Pts',(84.6628282975729,4.23865362461961,-1.30440914170987));
#20184=CARTESIAN_POINT('Ctrl Pts',(84.6571364647814,4.19946594185683,-1.42553153719938));
#20185=CARTESIAN_POINT('Ctrl Pts',(84.6514446319899,4.15516216232301,-1.54470592825922));
#20186=CARTESIAN_POINT('Ctrl Pts',(84.6457511664263,4.11084567370657,-1.66391450595501));
#20187=CARTESIAN_POINT('Ctrl Pts',(84.6400577008628,4.06141030775849,-1.78117359356347));
#20188=CARTESIAN_POINT('Ctrl Pts',(84.6343642352992,4.00706618074523,-1.89602468948266));
#20189=CARTESIAN_POINT('Ctrl Pts',(84.6286647162093,3.95266427282489,-2.01099789980257));
#20190=CARTESIAN_POINT('Ctrl Pts',(84.6229651971194,3.89334335400322,-2.12355764543186));
#20191=CARTESIAN_POINT('Ctrl Pts',(84.6172656780295,3.82935986709181,-2.23326935417709));
#20192=CARTESIAN_POINT('Ctrl Pts',(84.6115627063165,3.76533762061858,-2.34304752347276));
#20193=CARTESIAN_POINT('Ctrl Pts',(84.6058597346035,3.696647394774,-2.44997388366463));
#20194=CARTESIAN_POINT('Ctrl Pts',(84.6001567628905,3.62358852267693,-2.55364351825466));
#20195=CARTESIAN_POINT('Ctrl Pts',(84.594445623123,3.55042501235113,-2.65746163319519));
#20196=CARTESIAN_POINT('Ctrl Pts',(84.5887344833553,3.47288060528993,-2.75801339338908));
#20197=CARTESIAN_POINT('Ctrl Pts',(84.5830233435877,3.39129461642376,-2.85492728884909));
#20198=CARTESIAN_POINT('Ctrl Pts',(84.5805204609982,3.35553990556104,-2.89739938925394));
#20199=CARTESIAN_POINT('Ctrl Pts',(84.5780175784086,3.31900944650053,-2.93917328425464));
#20200=CARTESIAN_POINT('Ctrl Pts',(84.575514695819,3.28173392048605,-2.98022003803935));
#20201=CARTESIAN_POINT('Ctrl Pts',(84.569803483592,3.19667661862605,-3.07388273043659));
#20202=CARTESIAN_POINT('Ctrl Pts',(84.5640922713649,3.10747515059021,-3.16404561091582));
#20203=CARTESIAN_POINT('Ctrl Pts',(84.5583810591379,3.0144485895958,-3.2503213226824));
#20204=CARTESIAN_POINT('Ctrl Pts',(84.5526768134514,2.92153550246336,-3.33649179527748));
#20205=CARTESIAN_POINT('Ctrl Pts',(84.546972567765,2.82480689515587,-3.41878426333201));
#20206=CARTESIAN_POINT('Ctrl Pts',(84.5412683220785,2.72462086789934,-3.49684573954978));
#20207=CARTESIAN_POINT('Ctrl Pts',(84.5355696156728,2.62453212932434,-3.57483141180259));
#20208=CARTESIAN_POINT('Ctrl Pts',(84.5298709092672,2.52099296469723,-3.64859402386817));
#20209=CARTESIAN_POINT('Ctrl Pts',(84.5241722028615,2.41439660703346,-3.71781898751745));
#20210=CARTESIAN_POINT('Ctrl Pts',(84.5184776134606,2.30787725942763,-3.7869939399039));
#20211=CARTESIAN_POINT('Ctrl Pts',(84.5127830240597,2.19830544829266,-3.85163755184132));
#20212=CARTESIAN_POINT('Ctrl Pts',(84.5070884346589,2.08610522654049,-3.91147721248641));
#20213=CARTESIAN_POINT('Ctrl Pts',(84.5013959777942,1.97394702204781,-3.97129446409781));
#20214=CARTESIAN_POINT('Ctrl Pts',(84.4957035209296,1.85916271567687,-4.02631115391453));
#20215=CARTESIAN_POINT('Ctrl Pts',(84.4900110640649,1.74220263664386,-4.07629966671627));
#20216=CARTESIAN_POINT('Ctrl Pts',(84.4843195385025,1.62526169261295,-4.12628000125492));
#20217=CARTESIAN_POINT('Ctrl Pts',(84.47862801294,1.50614605086188,-4.17123363823749));
#20218=CARTESIAN_POINT('Ctrl Pts',(84.4729364873775,1.38532728884591,-4.21098056309678));
#20219=CARTESIAN_POINT('Ctrl Pts',(84.467244611106,1.26450108203617,-4.25072993714237));
#20220=CARTESIAN_POINT('Ctrl Pts',(84.4615527348344,1.14197192541054,-4.28527183621726));
#20221=CARTESIAN_POINT('Ctrl Pts',(84.4558608585629,1.01822737694168,-4.31447586722263));
#20222=CARTESIAN_POINT('Ctrl Pts',(84.450167349634,0.89444733359516,-4.34368827511022));
#20223=CARTESIAN_POINT('Ctrl Pts',(84.444473840705,0.76945159319912,-4.36755967736608));
#20224=CARTESIAN_POINT('Ctrl Pts',(84.4387803317761,0.643738234916988,-4.38601072558036));
#20225=CARTESIAN_POINT('Ctrl Pts',(84.4330807697288,0.517891223056601,-4.40448139023517));
#20226=CARTESIAN_POINT('Ctrl Pts',(84.4273812076814,0.391325465276577,-4.41752013693667));
#20227=CARTESIAN_POINT('Ctrl Pts',(84.4216816456341,0.264544811393503,-4.42509943874313));
#20228=CARTESIAN_POINT('Ctrl Pts',(84.4159786311388,0.137687361502868,-4.43268333162955));
#20229=CARTESIAN_POINT('Ctrl Pts',(84.4102756166435,0.0106151546344382,
-4.43480118504154));
#20230=CARTESIAN_POINT('Ctrl Pts',(84.4045726021483,-0.116168859317712,
-4.43147760866788));
#20231=CARTESIAN_POINT('Ctrl Pts',(84.398861420238,-0.243134443500064,-4.42814927252596));
#20232=CARTESIAN_POINT('Ctrl Pts',(84.3931502383277,-0.369810613339101,
-4.41936397378047));
#20233=CARTESIAN_POINT('Ctrl Pts',(84.3874390564175,-0.49570005297812,-4.4051981178464));
#20234=CARTESIAN_POINT('Ctrl Pts',(84.3849366491739,-0.550859676782646,
-4.39899121688288));
#20235=CARTESIAN_POINT('Ctrl Pts',(84.3824342419302,-0.605868397615598,
-4.39175199917643));
#20236=CARTESIAN_POINT('Ctrl Pts',(84.3799318346866,-0.660685147178269,
-4.38348994937801));
#20237=CARTESIAN_POINT('Ctrl Pts',(84.3742207423032,-0.785790092308468,
-4.3646339738789));
#20238=CARTESIAN_POINT('Ctrl Pts',(84.3685096499199,-0.910280175299019,
-4.34038890063126));
#20239=CARTESIAN_POINT('Ctrl Pts',(84.3627985575365,-1.03365613806391,-4.31080549181273));
#20240=CARTESIAN_POINT('Ctrl Pts',(84.3570944317305,-1.15688160279174,-4.28125816980444));
#20241=CARTESIAN_POINT('Ctrl Pts',(84.3513903059246,-1.27899526623601,-4.24638555975464));
#20242=CARTESIAN_POINT('Ctrl Pts',(84.3456861801186,-1.39950483410601,-4.20628995901541));
#20243=CARTESIAN_POINT('Ctrl Pts',(84.3399875934903,-1.51989737722392,-4.16623329441893));
#20244=CARTESIAN_POINT('Ctrl Pts',(84.3342890068621,-1.63868854776384,-4.1209638569014));
#20245=CARTESIAN_POINT('Ctrl Pts',(84.3285904202338,-1.75539852810498,-4.07063447235525));
#20246=CARTESIAN_POINT('Ctrl Pts',(84.3228959503677,-1.87202419504252,-4.02034144666803));
#20247=CARTESIAN_POINT('Ctrl Pts',(84.3172014805016,-1.98657129888928,-3.96499590682139));
#20248=CARTESIAN_POINT('Ctrl Pts',(84.3115070106355,-2.09857786815734,-3.90479960193608));
#20249=CARTESIAN_POINT('Ctrl Pts',(84.3058146725113,-2.21054250742934,-3.84462583171854));
#20250=CARTESIAN_POINT('Ctrl Pts',(84.3001223343871,-2.31996815210041,-3.7796050957292));
#20251=CARTESIAN_POINT('Ctrl Pts',(84.2944299962629,-2.4264157079711,-3.70998595847897));
#20252=CARTESIAN_POINT('Ctrl Pts',(84.2887385889112,-2.53284585826152,-3.64037820487651));
#20253=CARTESIAN_POINT('Ctrl Pts',(84.2830471815594,-2.63629855440457,-3.56617376401281));
#20254=CARTESIAN_POINT('Ctrl Pts',(84.2773557742077,-2.73636253555055,-3.48766527551532));
#20255=CARTESIAN_POINT('Ctrl Pts',(84.2716640154919,-2.83643269423456,-3.40915194022712));
#20256=CARTESIAN_POINT('Ctrl Pts',(84.265972256776,-2.93311340777536,-3.32633427523276));
#20257=CARTESIAN_POINT('Ctrl Pts',(84.2602804980602,-3.02602585128815,-3.23954573163211));
#20258=CARTESIAN_POINT('Ctrl Pts',(84.2545871059062,-3.11896495909711,-3.15273228119075));
#20259=CARTESIAN_POINT('Ctrl Pts',(84.2488937137521,-3.20813335395086,-3.06194595750582));
#20260=CARTESIAN_POINT('Ctrl Pts',(84.243200321598,-3.29318885840884,-2.96755726867265));
#20261=CARTESIAN_POINT('Ctrl Pts',(84.2375008745215,-3.37833481939359,-2.87306819747137));
#20262=CARTESIAN_POINT('Ctrl Pts',(84.231801427445,-3.45935888923631,-2.77496940867005));
#20263=CARTESIAN_POINT('Ctrl Pts',(84.2261019803686,-3.53595881828426,-2.67366494449057));
#20264=CARTESIAN_POINT('Ctrl Pts',(84.2203990799687,-3.61260515961086,-2.57229909943154));
#20265=CARTESIAN_POINT('Ctrl Pts',(84.2146961795688,-3.68482179360344,-2.46772403755889));
#20266=CARTESIAN_POINT('Ctrl Pts',(84.208993279169,-3.75235035936997,-2.36037195808967));
#20267=CARTESIAN_POINT('Ctrl Pts',(84.2032822090281,-3.81997566378722,-2.25286609043907));
#20268=CARTESIAN_POINT('Ctrl Pts',(84.1975711388873,-3.88289929247917,-2.14257560752219));
#20269=CARTESIAN_POINT('Ctrl Pts',(84.1918600687465,-3.94090911427975,-2.02995673672785));
#20270=CARTESIAN_POINT('Ctrl Pts',(84.1893563703491,-3.96634026716265,-1.98058530906659));
#20271=CARTESIAN_POINT('Ctrl Pts',(84.1868526719517,-3.99082766603068,-1.93076664398898));
#20272=CARTESIAN_POINT('Ctrl Pts',(84.1843489735543,-4.01435641213992,-1.88054024054554));
#20273=CARTESIAN_POINT('Ctrl Pts',(84.1781915115531,-4.07222175257094,-1.75701610881383));
#20274=CARTESIAN_POINT('Ctrl Pts',(84.1720340495519,-4.1244421435033,-1.63069055220892));
#20275=CARTESIAN_POINT('Ctrl Pts',(84.1658765875508,-4.17076017586692,-1.50208140771481));
#20276=CARTESIAN_POINT('Ctrl Pts',(84.1597384307519,-4.21693298947263,-1.37387548544901));
#20277=CARTESIAN_POINT('Ctrl Pts',(84.153600273953,-4.25724025001845,-1.24340053497881));
#20278=CARTESIAN_POINT('Ctrl Pts',(84.1474621171541,-4.29147259395242,-1.11119394137804));
#20279=CARTESIAN_POINT('Ctrl Pts',(84.1413358900107,-4.3256384065015,-0.979244294476043));
#20280=CARTESIAN_POINT('Ctrl Pts',(84.1352096628674,-4.35375275848106,-0.845569999491432));
#20281=CARTESIAN_POINT('Ctrl Pts',(84.1290834357241,-4.37565515223945,-0.710725677515822));
#20282=CARTESIAN_POINT('Ctrl Pts',(84.1229755449203,-4.39749199019677,-0.576284956518449));
#20283=CARTESIAN_POINT('Ctrl Pts',(84.1168676541165,-4.41315389735394,-0.440681485826579));
#20284=CARTESIAN_POINT('Ctrl Pts',(84.1107597633126,-4.42253098370653,-0.304481030863648));
#20285=CARTESIAN_POINT('Ctrl Pts',(84.1062374819958,-4.42947377685407,-0.203638237073225));
#20286=CARTESIAN_POINT('Ctrl Pts',(84.101715200679,-4.43297229034197,-0.102468536838374));
#20287=CARTESIAN_POINT('Ctrl Pts',(84.0971929193621,-4.43299983598826,-0.00120587233263017));
#20288=CARTESIAN_POINT('Ctrl Pts',(84.0971929193385,-4.4329998359884,-0.00120587180341138));
#20289=CARTESIAN_POINT('Ctrl Pts',(84.0913529328301,-4.43303540788692,0.12956277196029));
#20290=CARTESIAN_POINT('Ctrl Pts',(84.0855129463217,-4.42728033452424,0.26028024094117));
#20291=CARTESIAN_POINT('Ctrl Pts',(84.0796729598133,-4.415774401046,0.390417006631218));
#20292=CARTESIAN_POINT('Ctrl Pts',(84.0738291793772,-4.40426099277658,0.5206383152355));
#20293=CARTESIAN_POINT('Ctrl Pts',(84.0679853989411,-4.38698931100753,0.650277801680128));
#20294=CARTESIAN_POINT('Ctrl Pts',(84.062141618505,-4.36405081751758,0.778812854365017));
#20295=CARTESIAN_POINT('Ctrl Pts',(84.0560269929981,-4.34004918040645,0.913305195457647));
#20296=CARTESIAN_POINT('Ctrl Pts',(84.0499123674912,-4.30984296405206,1.04658782571554));
#20297=CARTESIAN_POINT('Ctrl Pts',(84.0437977419842,-4.2735958871232,1.17807775361548));
#20298=CARTESIAN_POINT('Ctrl Pts',(84.0379393301313,-4.23886762700767,1.30405802031789));
#20299=CARTESIAN_POINT('Ctrl Pts',(84.0320809182784,-4.1985946681494,1.42839244942262));
#20300=CARTESIAN_POINT('Ctrl Pts',(84.0262225064255,-4.15297088683791,1.55058757027029));
#20301=CARTESIAN_POINT('Ctrl Pts',(84.0203584203072,-4.10730291582958,1.67290104530059));
#20302=CARTESIAN_POINT('Ctrl Pts',(84.0144943341889,-4.05627393146945,1.79307074206799));
#20303=CARTESIAN_POINT('Ctrl Pts',(84.0086302480705,-4.00012480179417,1.91062570119612));
#20304=CARTESIAN_POINT('Ctrl Pts',(84.0027563569163,-3.94388178805554,2.02837721790747));
#20305=CARTESIAN_POINT('Ctrl Pts',(83.9968824657621,-3.88250170262343,2.14350494074438));
#20306=CARTESIAN_POINT('Ctrl Pts',(83.9910085746079,-3.81627026328809,2.25556429248715));
#20307=CARTESIAN_POINT('Ctrl Pts',(83.9902610872125,-3.80784192085246,2.26982450786342));
#20308=CARTESIAN_POINT('Ctrl Pts',(83.9895135998172,-3.79933507053889,2.28403507546932));
#20309=CARTESIAN_POINT('Ctrl Pts',(83.9887661124219,-3.7907503488902,2.29819511625728));
#20310=CARTESIAN_POINT('Ctrl Pts',(83.983054636412,-3.7251553541719,2.4063905637869));
#20311=CARTESIAN_POINT('Ctrl Pts',(83.9773431604021,-3.65482340222278,2.51194223722398));
#20312=CARTESIAN_POINT('Ctrl Pts',(83.9716316843921,-3.57999371167098,2.61440892447915));
#20313=CARTESIAN_POINT('Ctrl Pts',(83.965927173822,-3.50525527978894,2.71675064832067));
#20314=CARTESIAN_POINT('Ctrl Pts',(83.9602226632518,-3.42603025544912,2.81601455147138));
#20315=CARTESIAN_POINT('Ctrl Pts',(83.9545181526817,-3.34260273108345,2.91178570333626));
#20316=CARTESIAN_POINT('Ctrl Pts',(83.9488191806154,-3.25925620642181,3.00746387108092));
#20317=CARTESIAN_POINT('Ctrl Pts',(83.9431202085492,-3.17171556145002,3.09965573613323));
#20318=CARTESIAN_POINT('Ctrl Pts',(83.9374212364829,-3.08030670995789,3.18797734819249));
#20319=CARTESIAN_POINT('Ctrl Pts',(83.9317263809658,-2.98896388599269,3.27623516273625));
#20320=CARTESIAN_POINT('Ctrl Pts',(83.9260315254487,-2.8937587027215,3.36062801202631));
#20321=CARTESIAN_POINT('Ctrl Pts',(83.9203366699316,-2.79505534578238,3.44080726196823));
#20322=CARTESIAN_POINT('Ctrl Pts',(83.9146439472549,-2.69638895527797,3.52095648313404));
#20323=CARTESIAN_POINT('Ctrl Pts',(83.9089512245782,-2.59422730538682,3.59689499148059));
#20324=CARTESIAN_POINT('Ctrl Pts',(83.9032585019015,-2.48896897063816,3.66831329948799));
#20325=CARTESIAN_POINT('Ctrl Pts',(83.8975667107976,-2.38372786065409,3.73971992040622));
#20326=CARTESIAN_POINT('Ctrl Pts',(83.8918749196937,-2.27539140392943,3.80660758831022));
#20327=CARTESIAN_POINT('Ctrl Pts',(83.8861831285899,-2.16438812667184,3.86870947954508));
#20328=CARTESIAN_POINT('Ctrl Pts',(83.8804909873342,-2.05337802063171,3.93081519121048));
#20329=CARTESIAN_POINT('Ctrl Pts',(83.8747988460785,-1.93970111607934,3.98813434577702));
#20330=CARTESIAN_POINT('Ctrl Pts',(83.8691067048227,-1.82381110683975,4.04044577324928));
#20331=CARTESIAN_POINT('Ctrl Pts',(83.8634129317538,-1.70788787445219,4.09277219727134));
#20332=CARTESIAN_POINT('Ctrl Pts',(83.8577191586848,-1.58975063885866,4.14008787413932));
#20333=CARTESIAN_POINT('Ctrl Pts',(83.8520253856159,-1.46987317524154,4.18221972745399));
#20334=CARTESIAN_POINT('Ctrl Pts',(83.8463255621315,-1.34986832536405,4.22439635164614));
#20335=CARTESIAN_POINT('Ctrl Pts',(83.840625738647,-1.22811993212665,4.26137802144207));
#20336=CARTESIAN_POINT('Ctrl Pts',(83.8349259151626,-1.10511733767614,4.2930414242082));
#20337=CARTESIAN_POINT('Ctrl Pts',(83.829222640422,-0.982040264870982,4.32472399923774));
#20338=CARTESIAN_POINT('Ctrl Pts',(83.8235193656813,-0.857707867782099,
4.35108180951428));
#20339=CARTESIAN_POINT('Ctrl Pts',(83.8178160909406,-0.732618569098261,
4.37204289002434));
#20340=CARTESIAN_POINT('Ctrl Pts',(83.8121046528678,-0.607350224946806,
4.39303397299266));
#20341=CARTESIAN_POINT('Ctrl Pts',(83.806393214795,-0.481323211148197,4.40861285320017));
#20342=CARTESIAN_POINT('Ctrl Pts',(83.8006817767222,-0.35504031884819,4.41875948338356));
#20343=CARTESIAN_POINT('Ctrl Pts',(83.7981822682446,-0.29977487504039,4.42319997417393));
#20344=CARTESIAN_POINT('Ctrl Pts',(83.795682759767,-0.244460417594769,4.42660074476098));
#20345=CARTESIAN_POINT('Ctrl Pts',(83.7931832512895,-0.189138922143068,
4.42896324980582));
#20346=CARTESIAN_POINT('Ctrl Pts',(83.7874728176785,-0.0627501821680352,
4.43436068227514));
#20347=CARTESIAN_POINT('Ctrl Pts',(83.7817623840675,0.0640650031860301,
4.43435204042131));
#20348=CARTESIAN_POINT('Ctrl Pts',(83.7760519504566,0.190806976161237,4.42889170084889));
#20349=CARTESIAN_POINT('Ctrl Pts',(83.7703484833763,0.317394328331168,4.42343802270111));
#20350=CARTESIAN_POINT('Ctrl Pts',(83.764645016296,0.443908250334559,4.41254589560693));
#20351=CARTESIAN_POINT('Ctrl Pts',(83.7589415492157,0.569846065609721,4.39622161196511));
#20352=CARTESIAN_POINT('Ctrl Pts',(83.7532436205021,0.695661588640037,4.3799131800616));
#20353=CARTESIAN_POINT('Ctrl Pts',(83.7475456917884,0.820901724396628,4.35818313890482));
#20354=CARTESIAN_POINT('Ctrl Pts',(83.7418477630747,0.945066382485209,4.33108976271519));
#20355=CARTESIAN_POINT('Ctrl Pts',(83.736153949551,1.06914136568023,4.30401595405519));
#20356=CARTESIAN_POINT('Ctrl Pts',(83.7304601360273,1.19214202838096,4.27158660466542));
#20357=CARTESIAN_POINT('Ctrl Pts',(83.7247663225036,1.31357644502133,4.23391142126109));
#20358=CARTESIAN_POINT('Ctrl Pts',(83.7190746360093,1.43496549758774,4.19625031211885));
#20359=CARTESIAN_POINT('Ctrl Pts',(83.713382949515,1.55478908672782,4.15334738351648));
#20360=CARTESIAN_POINT('Ctrl Pts',(83.7076912630207,1.67256879373474,4.10536266731999));
#20361=CARTESIAN_POINT('Ctrl Pts',(83.7020005041744,1.79032930465516,4.05738577181509));
#20362=CARTESIAN_POINT('Ctrl Pts',(83.696309745328,1.90604622640667,4.00432888674341));
#20363=CARTESIAN_POINT('Ctrl Pts',(83.6906189864817,2.01926003747436,3.94640062602101));
#20364=CARTESIAN_POINT('Ctrl Pts',(83.684927872462,2.13248091447746,3.88846874986208));
#20365=CARTESIAN_POINT('Ctrl Pts',(83.6792367584422,2.24319801462135,3.82566507523673));
#20366=CARTESIAN_POINT('Ctrl Pts',(83.6735456444225,2.35097585630249,3.75824447356512));
#20367=CARTESIAN_POINT('Ctrl Pts',(83.6678528924675,2.45878471706596,3.69080446785683));
#20368=CARTESIAN_POINT('Ctrl Pts',(83.6621601405124,2.56365229815003,3.61874510337618));
#20369=CARTESIAN_POINT('Ctrl Pts',(83.6564673885573,2.66517201029379,3.54236462769526));
#20370=CARTESIAN_POINT('Ctrl Pts',(83.6507685714675,2.76679988290871,3.46590277522492));
#20371=CARTESIAN_POINT('Ctrl Pts',(83.6450697543777,2.86507244561426,3.3851108598858));
#20372=CARTESIAN_POINT('Ctrl Pts',(83.6393709372879,2.95961589459052,3.30032767410861));
#20373=CARTESIAN_POINT('Ctrl Pts',(83.6336686618933,3.05421671688846,3.21549303798723));
#20374=CARTESIAN_POINT('Ctrl Pts',(83.6279663864987,3.14508363230125,3.12666258503787));
#20375=CARTESIAN_POINT('Ctrl Pts',(83.622264111104,3.23188053981087,3.0342111291721));
#20376=CARTESIAN_POINT('Ctrl Pts',(83.6165536529411,3.31880200093002,2.94162700541682));
#20377=CARTESIAN_POINT('Ctrl Pts',(83.6108431947782,3.4016415322164,2.84541180519697));
#20378=CARTESIAN_POINT('Ctrl Pts',(83.6051327366153,3.4801038216176,2.74597275856164));
#20379=CARTESIAN_POINT('Ctrl Pts',(83.6026219544625,3.51460222967349,2.70225126083712));
#20380=CARTESIAN_POINT('Ctrl Pts',(83.6001111723098,3.54825499981515,2.65790690039704));
#20381=CARTESIAN_POINT('Ctrl Pts',(83.5976003901571,3.5810397745534,2.61297591513327));
#20382=CARTESIAN_POINT('Ctrl Pts',(83.5918888133932,3.65561922677717,2.51076602363333));
#20383=CARTESIAN_POINT('Ctrl Pts',(83.5861772366293,3.72593433224448,2.40520296959203));
#20384=CARTESIAN_POINT('Ctrl Pts',(83.5804656598655,3.79167004282015,2.29667744500186));
#20385=CARTESIAN_POINT('Ctrl Pts',(83.574761055143,3.85732551073857,2.188284395993));
#20386=CARTESIAN_POINT('Ctrl Pts',(83.5690564504205,3.91841250000079,2.07693640934517));
#20387=CARTESIAN_POINT('Ctrl Pts',(83.5633518456981,3.97465749836092,1.96305546807096));
#20388=CARTESIAN_POINT('Ctrl Pts',(83.5576527860998,4.03084782413389,1.84928522402975));
#20389=CARTESIAN_POINT('Ctrl Pts',(83.5519537265015,4.0822053488005,1.73298728050214));
#20390=CARTESIAN_POINT('Ctrl Pts',(83.5462546669032,4.12850125681246,1.61461028502172));
#20391=CARTESIAN_POINT('Ctrl Pts',(83.5405597304986,4.17476367035164,1.49631893372075));
#20392=CARTESIAN_POINT('Ctrl Pts',(83.534864794094,4.21597161089721,1.37595189463706));
#20393=CARTESIAN_POINT('Ctrl Pts',(83.5291698576894,4.25194359409921,1.25397953436198));
#20394=CARTESIAN_POINT('Ctrl Pts',(83.5234770641988,4.28790204161613,1.13205307034589));
#20395=CARTESIAN_POINT('Ctrl Pts',(83.5177842707082,4.31862833657742,1.00852286840435));
#20396=CARTESIAN_POINT('Ctrl Pts',(83.5120914772176,4.34399036560862,0.88387595481463));
#20397=CARTESIAN_POINT('Ctrl Pts',(83.5063996215779,4.36934821640941,0.759249575998512));
#20398=CARTESIAN_POINT('Ctrl Pts',(83.5007077659382,4.3893434795575,0.633507242415827));
#20399=CARTESIAN_POINT('Ctrl Pts',(83.4950159102986,4.40389494948329,0.507147191568224));
#20400=CARTESIAN_POINT('Ctrl Pts',(83.4893237108232,4.41844729843957,0.380779507516781));
#20401=CARTESIAN_POINT('Ctrl Pts',(83.4836315113479,4.42755515447289,0.253794428480396));
#20402=CARTESIAN_POINT('Ctrl Pts',(83.4779393118725,4.43118913666873,0.126695836825879));
#20403=CARTESIAN_POINT('Ctrl Pts',(83.4722454869427,4.43482415657815,-0.000439048879321308));
#20404=CARTESIAN_POINT('Ctrl Pts',(83.4665516620128,4.43298218168202,-0.127687112904415));
#20405=CARTESIAN_POINT('Ctrl Pts',(83.460857837083,4.42568594876661,-0.254544461518653));
#20406=CARTESIAN_POINT('Ctrl Pts',(83.4551579715224,4.41838197521124,-0.381536394249353));
#20407=CARTESIAN_POINT('Ctrl Pts',(83.4494581059619,4.40561221322122,-0.508136385150158));
#20408=CARTESIAN_POINT('Ctrl Pts',(83.4437582404013,4.38745132005257,-0.633845339313109));
#20409=CARTESIAN_POINT('Ctrl Pts',(83.438054929118,4.36927944813329,-0.759630287935535));
#20410=CARTESIAN_POINT('Ctrl Pts',(83.4323516178347,4.34571002640231,-0.884522735206173));
#20411=CARTESIAN_POINT('Ctrl Pts',(83.4266483065514,4.31686859648169,-1.00803497990406));
#20412=CARTESIAN_POINT('Ctrl Pts',(83.4209368406541,4.28798592898571,-1.13172382283282));
#20413=CARTESIAN_POINT('Ctrl Pts',(83.4152253747567,4.25381630894877,-1.25402813920103));
#20414=CARTESIAN_POINT('Ctrl Pts',(83.4095139088594,4.21453487374948,-1.37447619039017));
#20415=CARTESIAN_POINT('Ctrl Pts',(83.4070151155812,4.19734906051016,-1.4271727810894));
#20416=CARTESIAN_POINT('Ctrl Pts',(83.404516322303,4.17918541196736,-1.4795143296501));
#20417=CARTESIAN_POINT('Ctrl Pts',(83.4020175290248,4.16006142107037,-1.53146269067254));
#20418=CARTESIAN_POINT('Ctrl Pts',(83.3963041942983,4.11633561059467,-1.65023937284239));
#20419=CARTESIAN_POINT('Ctrl Pts',(83.3905908595718,4.06745177772856,-1.76732409392234));
#20420=CARTESIAN_POINT('Ctrl Pts',(83.3848775248453,4.01356072289606,-1.88223784990793));
#20421=CARTESIAN_POINT('Ctrl Pts',(83.3791711450774,3.959735270741,-1.9970117190405));
#20422=CARTESIAN_POINT('Ctrl Pts',(83.3734647653095,3.90091489140313,-2.10961952289275));
#20423=CARTESIAN_POINT('Ctrl Pts',(83.3677583855417,3.83729944594922,-2.21959950489222));
#20424=CARTESIAN_POINT('Ctrl Pts',(83.3620575361312,3.7737456536217,-2.32947289941625));
#20425=CARTESIAN_POINT('Ctrl Pts',(83.3563566867208,3.70540624107761,-2.43672319658693));
#20426=CARTESIAN_POINT('Ctrl Pts',(83.3506558373104,3.6325280306422,-2.54091107805817));
#20427=CARTESIAN_POINT('Ctrl Pts',(83.344959098619,3.55970237059481,-2.64502383263528));
#20428=CARTESIAN_POINT('Ctrl Pts',(83.3392623599276,3.48234465443669,-2.74607824093065));
#20429=CARTESIAN_POINT('Ctrl Pts',(83.3335656212362,3.40074601005896,-2.84366235250743));
#20430=CARTESIAN_POINT('Ctrl Pts',(83.3278710137284,3.31917789221498,-2.94120995729297));
#20431=CARTESIAN_POINT('Ctrl Pts',(83.3221764062205,3.23337225624653,-3.03528954135123));
#20432=CARTESIAN_POINT('Ctrl Pts',(83.3164817987127,3.14366145661774,-3.12552101995427));
#20433=CARTESIAN_POINT('Ctrl Pts',(83.3107881223432,3.05396532580863,-3.21573774460022));
#20434=CARTESIAN_POINT('Ctrl Pts',(83.3050944459738,2.960365582564,-3.30210733266954));
#20435=CARTESIAN_POINT('Ctrl Pts',(83.2994007696043,2.8632321262774,-3.38428586130856));
#20436=CARTESIAN_POINT('Ctrl Pts',(83.2937067447069,2.76609272414436,-3.46646942035554));
#20437=CARTESIAN_POINT('Ctrl Pts',(83.2880127198095,2.66541948321974,-3.54446115213014));
#20438=CARTESIAN_POINT('Ctrl Pts',(83.282318694912,2.5616157255802,-3.617957141048));
#20439=CARTESIAN_POINT('Ctrl Pts',(83.2766230418857,2.45778228666819,-3.69147414514414));
#20440=CARTESIAN_POINT('Ctrl Pts',(83.2709273888593,2.35081687564506,-3.76049261868623));
#20441=CARTESIAN_POINT('Ctrl Pts',(83.2652317358329,2.24115171398086,-3.82475201744122));
#20442=CARTESIAN_POINT('Ctrl Pts',(83.2595300481698,2.13137036029987,-3.88907950007103));
#20443=CARTESIAN_POINT('Ctrl Pts',(83.2538283605067,2.01888388917474,-3.94863763852377));
#20444=CARTESIAN_POINT('Ctrl Pts',(83.2481266728436,1.90414931067986,-4.00321176090366));
#20445=CARTESIAN_POINT('Ctrl Pts',(83.2424215404412,1.7893454139882,-4.0578188548585));
#20446=CARTESIAN_POINT('Ctrl Pts',(83.2367164080389,1.67229107071298,-4.10743577863478));
#20447=CARTESIAN_POINT('Ctrl Pts',(83.2310112756365,1.5534620216424,-4.15189652415793));
#20448=CARTESIAN_POINT('Ctrl Pts',(83.22529800601,1.43446348682922,-4.19642068399374));
#20449=CARTESIAN_POINT('Ctrl Pts',(83.2195847363836,1.31368557021128,-4.23577385751035));
#20450=CARTESIAN_POINT('Ctrl Pts',(83.2138714667571,1.19161822687623,-4.26984016110397));
#20451=CARTESIAN_POINT('Ctrl Pts',(83.2113925338022,1.13865437607026,-4.28462120386076));
#20452=CARTESIAN_POINT('Ctrl Pts',(83.2089136008473,1.08544789663886,-4.29840759029817));
#20453=CARTESIAN_POINT('Ctrl Pts',(83.2064346678924,1.03203923524623,-4.31119287632928));
#20454=CARTESIAN_POINT('Ctrl Pts',(83.2007300562091,0.90913325944449,-4.34061484674728));
#20455=CARTESIAN_POINT('Ctrl Pts',(83.1950254445258,0.784776113443813,-4.36482277943889));
#20456=CARTESIAN_POINT('Ctrl Pts',(83.1893208328425,0.659448564409288,-4.38367615032161));
#20457=CARTESIAN_POINT('Ctrl Pts',(83.1836231915243,0.534274150910706,-4.40250648460084));
#20458=CARTESIAN_POINT('Ctrl Pts',(83.177925550206,0.408132085508736,-4.41599521387896));
#20459=CARTESIAN_POINT('Ctrl Pts',(83.1722279088878,0.281516077405062,-4.42405218076849));
#20460=CARTESIAN_POINT('Ctrl Pts',(83.1665358030648,0.155023082012252,-4.43210131998005));
#20461=CARTESIAN_POINT('Ctrl Pts',(83.1608436972417,0.0280574572038139,
-4.43472917186113));
#20462=CARTESIAN_POINT('Ctrl Pts',(83.1551515914187,-0.0988796452240617,
-4.43189708993343));
#20463=CARTESIAN_POINT('Ctrl Pts',(83.1494635912445,-0.225725189414087,
-4.42906705075308));
#20464=CARTESIAN_POINT('Ctrl Pts',(83.1437755910704,-0.352541853464863,
-4.4207849244752));
#20465=CARTESIAN_POINT('Ctrl Pts',(83.1380875908963,-0.478826635252343,
-4.40706410815329));
#20466=CARTESIAN_POINT('Ctrl Pts',(83.1324016826762,-0.605064971550271,
-4.39334833812454));
#20467=CARTESIAN_POINT('Ctrl Pts',(83.126715774456,-0.730771417290483,-4.3741978978697));
#20468=CARTESIAN_POINT('Ctrl Pts',(83.1210298662359,-0.855446582372364,
-4.34967816564714));
#20469=CARTESIAN_POINT('Ctrl Pts',(83.1153448622648,-0.980101919944643,
-4.32516233287981));
#20470=CARTESIAN_POINT('Ctrl Pts',(83.1096598582938,-1.10372591053141,-4.29527898367961));
#20471=CARTESIAN_POINT('Ctrl Pts',(83.1039748543227,-1.22582841724243,-4.26014479700877));
#20472=CARTESIAN_POINT('Ctrl Pts',(83.0982894657907,-1.34793918355144,-4.22500823369338));
#20473=CARTESIAN_POINT('Ctrl Pts',(83.0926040772588,-1.46852787668371,-4.18462023711314));
#20474=CARTESIAN_POINT('Ctrl Pts',(83.0869186887268,-1.58711911719866,-4.13914748563307));
#20475=CARTESIAN_POINT('Ctrl Pts',(83.0812316268597,-1.70574526172996,-4.09366135051981));
#20476=CARTESIAN_POINT('Ctrl Pts',(83.0755445649925,-1.82237241065795,-4.04308762666087));
#20477=CARTESIAN_POINT('Ctrl Pts',(83.0698575031254,-1.93654526686745,-3.98764108582672));
#20478=CARTESIAN_POINT('Ctrl Pts',(83.0641642922638,-2.05084156964352,-3.93213459479668));
#20479=CARTESIAN_POINT('Ctrl Pts',(83.0584710814022,-2.16267792118752,-3.87174494253703));
#20480=CARTESIAN_POINT('Ctrl Pts',(83.0527778705406,-2.27162347021219,-3.8067329574822));
#20481=CARTESIAN_POINT('Ctrl Pts',(83.0470811612202,-2.38063596590833,-3.74168102278238));
#20482=CARTESIAN_POINT('Ctrl Pts',(83.0413844518998,-2.48675378667198,-3.67200131658452));
#20483=CARTESIAN_POINT('Ctrl Pts',(83.0356877425793,-2.58957623773381,-3.59799720802621));
#20484=CARTESIAN_POINT('Ctrl Pts',(83.0299827406343,-2.69254836608165,-3.52388537266302));
#20485=CARTESIAN_POINT('Ctrl Pts',(83.0242777386892,-2.79221523266356,-3.4454368125276));
#20486=CARTESIAN_POINT('Ctrl Pts',(83.0185727367441,-2.88821001233549,-3.36299448775121));
#20487=CARTESIAN_POINT('Ctrl Pts',(83.0159990934161,-2.9315152253059,-3.3258030650049));
#20488=CARTESIAN_POINT('Ctrl Pts',(83.0134254500881,-2.97407364034082,-3.28779936335854));
#20489=CARTESIAN_POINT('Ctrl Pts',(83.0108518067601,-3.01585417860915,-3.24901717037102));
#20490=CARTESIAN_POINT('Ctrl Pts',(83.0052145989932,-3.10736863683513,-3.16407017047183));
#20491=CARTESIAN_POINT('Ctrl Pts',(82.9995773912263,-3.19545120876946,-3.07510492987072));
#20492=CARTESIAN_POINT('Ctrl Pts',(82.9939401834594,-3.2797227815974,-2.982433146924));
#20493=CARTESIAN_POINT('Ctrl Pts',(82.988309963474,-3.36388989289898,-2.88987623825306));
#20494=CARTESIAN_POINT('Ctrl Pts',(82.9826797434884,-3.4442551250556,-2.79362222478303));
#20495=CARTESIAN_POINT('Ctrl Pts',(82.977049523503,-3.52047370683076,-2.69402187806879));
#20496=CARTESIAN_POINT('Ctrl Pts',(82.9714254739873,-3.59660875644143,-2.59453068889005));
#20497=CARTESIAN_POINT('Ctrl Pts',(82.9658014244717,-3.66860595187104,-2.49170078963833));
#20498=CARTESIAN_POINT('Ctrl Pts',(82.9601773749561,-3.73615911197191,-2.38591787160189));
#20499=CARTESIAN_POINT('Ctrl Pts',(82.9545567511598,-3.80367112411159,-2.28019938802564));
#20500=CARTESIAN_POINT('Ctrl Pts',(82.9489361273636,-3.86674426160977,-2.17153180635648));
#20501=CARTESIAN_POINT('Ctrl Pts',(82.9433155035674,-3.92511438630353,-2.06033153993066));
#20502=CARTESIAN_POINT('Ctrl Pts',(82.9376969531584,-3.9834629788903,-1.9491722940791));
#20503=CARTESIAN_POINT('Ctrl Pts',(82.9320784027494,-4.03711181792837,-1.83548258460658));
#20504=CARTESIAN_POINT('Ctrl Pts',(82.9264598523405,-4.08584198861877,-1.71970469675459));
#20505=CARTESIAN_POINT('Ctrl Pts',(82.9208420249266,-4.13456588871013,-1.60394170720281));
#20506=CARTESIAN_POINT('Ctrl Pts',(82.9152241975128,-4.17837222128289,-1.48609145278783));
#20507=CARTESIAN_POINT('Ctrl Pts',(82.909606370099,-4.21708990039573,-1.36661690754224));
#20508=CARTESIAN_POINT('Ctrl Pts',(82.9039855488592,-4.25582821275085,-1.24707869248756));
#20509=CARTESIAN_POINT('Ctrl Pts',(82.8983647276194,-4.28947232540022,-1.12591484803288));
#20510=CARTESIAN_POINT('Ctrl Pts',(82.8927439063795,-4.31790083432927,-1.00360419733011));
#20511=CARTESIAN_POINT('Ctrl Pts',(82.8871215575249,-4.34633706949776,-0.881260305299895));
#20512=CARTESIAN_POINT('Ctrl Pts',(82.8814992086703,-4.36955479795709,-0.757769389447973));
#20513=CARTESIAN_POINT('Ctrl Pts',(82.8758768598157,-4.38748390115548,-0.633619773287978));
#20514=CARTESIAN_POINT('Ctrl Pts',(82.8702483134227,-4.40543276767853,-0.509333306492264));
#20515=CARTESIAN_POINT('Ctrl Pts',(82.8646197670297,-4.41808132081018,-0.384387097784731));
#20516=CARTESIAN_POINT('Ctrl Pts',(82.8589912206366,-4.42541138808375,-0.259274075485084));
#20517=CARTESIAN_POINT('Ctrl Pts',(82.855058453546,-4.43053303856554,-0.171855345612122));
#20518=CARTESIAN_POINT('Ctrl Pts',(82.8511256864554,-4.43305926183473,-0.0843552441526603));
#20519=CARTESIAN_POINT('Ctrl Pts',(82.8471929193648,-4.43299894467431,0.00305884233548282));
#20520=CARTESIAN_POINT('Origin',(80.1322559480305,0.,0.));
#20521=CARTESIAN_POINT('',(89.5072559480779,-3.72274932293675,0.00224523361020461));
#20522=CARTESIAN_POINT('Ctrl Pts',(89.3502471949048,-2.62112000711957,2.64359555733806));
#20523=CARTESIAN_POINT('Ctrl Pts',(89.3561947378413,-2.70028756086394,2.5651010771752));
#20524=CARTESIAN_POINT('Ctrl Pts',(89.3621422807778,-2.77597243042016,2.48300129230493));
#20525=CARTESIAN_POINT('Ctrl Pts',(89.3680898237143,-2.84783768146393,2.39764219652019));
#20526=CARTESIAN_POINT('Ctrl Pts',(89.374035835165,-2.91968442728483,2.31230508060844));
#20527=CARTESIAN_POINT('Ctrl Pts',(89.3799818466158,-2.98771324183078,2.2237106411624));
#20528=CARTESIAN_POINT('Ctrl Pts',(89.3859278580665,-3.05162626314291,2.13223936568961));
#20529=CARTESIAN_POINT('Ctrl Pts',(89.3918737993332,-3.11553853005399,2.04076916990333));
#20530=CARTESIAN_POINT('Ctrl Pts',(89.3978197405998,-3.17533486192985,1.94642254760151));
#20531=CARTESIAN_POINT('Ctrl Pts',(89.4037656818665,-3.23076011931727,1.84960985451772));
#20532=CARTESIAN_POINT('Ctrl Pts',(89.4097130138169,-3.28619834000165,1.75277451811663));
#20533=CARTESIAN_POINT('Ctrl Pts',(89.4156603457672,-3.33726324673087,1.65347232600807));
#20534=CARTESIAN_POINT('Ctrl Pts',(89.4216076777176,-3.38374551156931,1.55213848461875));
#20535=CARTESIAN_POINT('Ctrl Pts',(89.4275612789431,-3.43027677486806,1.45069782394632));
#20536=CARTESIAN_POINT('Ctrl Pts',(89.4335148801687,-3.47221557776334,1.34722161762241));
#20537=CARTESIAN_POINT('Ctrl Pts',(89.4394684813942,-3.50940062625379,1.24216537021022));
#20538=CARTESIAN_POINT('Ctrl Pts',(89.445425610418,-3.54660770869388,1.13704687186226));
#20539=CARTESIAN_POINT('Ctrl Pts',(89.4513827394418,-3.57905530506113,1.03034686604588));
#20540=CARTESIAN_POINT('Ctrl Pts',(89.4573398684656,-3.60663242416782,0.922534616933895));
#20541=CARTESIAN_POINT('Ctrl Pts',(89.463305882831,-3.63425067586094,0.814561560718077));
#20542=CARTESIAN_POINT('Ctrl Pts',(89.4692718971964,-3.65698385982863,0.705473356159652));
#20543=CARTESIAN_POINT('Ctrl Pts',(89.4752379115619,-3.67477232943987,0.59574817606357));
#20544=CARTESIAN_POINT('Ctrl Pts',(89.4781531178931,-3.6834644069403,0.542132559319297));
#20545=CARTESIAN_POINT('Ctrl Pts',(89.4810683242243,-3.69097665121069,0.48836491923504));
#20546=CARTESIAN_POINT('Ctrl Pts',(89.4839835305554,-3.69730662674047,0.434501174176788));
#20547=CARTESIAN_POINT('Ctrl Pts',(89.4917410030471,-3.71415092709746,0.291167744869728));
#20548=CARTESIAN_POINT('Ctrl Pts',(89.4994984755388,-3.72266211806776,0.146836753085815));
#20549=CARTESIAN_POINT('Ctrl Pts',(89.5072559480305,-3.72274932293622,0.00224523449340528));
#20550=CARTESIAN_POINT('',(90.4429954109251,0.0296350623540759,3.72263204273257));
#20551=CARTESIAN_POINT('Ctrl Pts',(89.5072559480779,-3.72274932293675,0.00224523361020212));
#20552=CARTESIAN_POINT('Ctrl Pts',(89.5131410009605,-3.72281547915724,-0.107446258588759));
#20553=CARTESIAN_POINT('Ctrl Pts',(89.5190260538432,-3.71802930879369,-0.217318185000411));
#20554=CARTESIAN_POINT('Ctrl Pts',(89.5249111067258,-3.7083694126923,-0.326900384686496));
#20555=CARTESIAN_POINT('Ctrl Pts',(89.5307896394189,-3.69872021901865,-0.436361175657531));
#20556=CARTESIAN_POINT('Ctrl Pts',(89.5366681721121,-3.68420807032288,-0.545532453701019));
#20557=CARTESIAN_POINT('Ctrl Pts',(89.5425467048052,-3.66486360378298,-0.653943673542932));
#20558=CARTESIAN_POINT('Ctrl Pts',(89.5484203959138,-3.64553506942815,-0.762265605442191));
#20559=CARTESIAN_POINT('Ctrl Pts',(89.5542940870223,-3.62138220595615,-0.869828303288613));
#20560=CARTESIAN_POINT('Ctrl Pts',(89.5601677781308,-3.59248741612288,-0.976166854333197));
#20561=CARTESIAN_POINT('Ctrl Pts',(89.5660389041895,-3.56360524468848,-1.08245896717004));
#20562=CARTESIAN_POINT('Ctrl Pts',(89.5719100302482,-3.52998537330877,-1.18752758208424));
#20563=CARTESIAN_POINT('Ctrl Pts',(89.5777811563069,-3.49176103452334,-1.29091922298975));
#20564=CARTESIAN_POINT('Ctrl Pts',(89.5836512556447,-3.45354338026902,-1.3942927831472));
#20565=CARTESIAN_POINT('Ctrl Pts',(89.5895213549825,-3.41072300784237,-1.49598955000986));
#20566=CARTESIAN_POINT('Ctrl Pts',(89.5953914543204,-3.36348232776787,-1.59557331178897));
#20567=CARTESIAN_POINT('Ctrl Pts',(89.6012620640808,-3.31623753997572,-1.6951657326724));
#20568=CARTESIAN_POINT('Ctrl Pts',(89.6071326738412,-3.26457186568472,-1.7926443963283));
#20569=CARTESIAN_POINT('Ctrl Pts',(89.6130032836017,-3.20871455758169,-1.8875959447041));
#20570=CARTESIAN_POINT('Ctrl Pts',(89.618879452578,-3.15280435500192,-1.98263740812659));
#20571=CARTESIAN_POINT('Ctrl Pts',(89.6247556215542,-3.09269481009817,-2.07514660714444));
#20572=CARTESIAN_POINT('Ctrl Pts',(89.6306317905305,-3.02865953453122,-2.16473762530085));
#20573=CARTESIAN_POINT('Ctrl Pts',(89.6365108408342,-2.9645928598335,-2.25437257362028));
#20574=CARTESIAN_POINT('Ctrl Pts',(89.6423898911379,-2.89659688667175,-2.3410861548138));
#20575=CARTESIAN_POINT('Ctrl Pts',(89.6482689414417,-2.82498546918569,-2.4245256569873));
#20576=CARTESIAN_POINT('Ctrl Pts',(89.6541571245999,-2.75326280640904,-2.50809477887778));
#20577=CARTESIAN_POINT('Ctrl Pts',(89.6600453077582,-2.67791377583524,-2.58837935118275));
#20578=CARTESIAN_POINT('Ctrl Pts',(89.6659334909165,-2.59928914039452,-2.66506351277547));
#20579=CARTESIAN_POINT('Ctrl Pts',(89.6704777911736,-2.53860931073468,-2.72424575046689));
#20580=CARTESIAN_POINT('Ctrl Pts',(89.6750220914307,-2.47597921985387,-2.78128424885584));
#20581=CARTESIAN_POINT('Ctrl Pts',(89.6795663916879,-2.41157259940264,-2.8360509798504));
#20582=CARTESIAN_POINT('Ctrl Pts',(89.6855255449048,-2.32711318921056,-2.90786915266465));
#20583=CARTESIAN_POINT('Ctrl Pts',(89.6914846981217,-2.23930494820216,-2.97602838174629));
#20584=CARTESIAN_POINT('Ctrl Pts',(89.6974438513386,-2.14849817249947,-3.0402011718415));
#20585=CARTESIAN_POINT('Ctrl Pts',(89.7033954330532,-2.05780677287308,-3.10429242611883));
#20586=CARTESIAN_POINT('Ctrl Pts',(89.7093470147677,-1.96412475304399,-3.16440707422553));
#20587=CARTESIAN_POINT('Ctrl Pts',(89.7152985964823,-1.86783655449855,-3.22025684816894));
#20588=CARTESIAN_POINT('Ctrl Pts',(89.7212442421847,-1.77164439225896,-3.27605091844304));
#20589=CARTESIAN_POINT('Ctrl Pts',(89.727189887887,-1.67285158099827,-3.32758836649288));
#20590=CARTESIAN_POINT('Ctrl Pts',(89.7331355335894,-1.57187209771999,-3.37462378212881));
#20591=CARTESIAN_POINT('Ctrl Pts',(89.7390770554423,-1.47096265295516,-3.42162657439924));
#20592=CARTESIAN_POINT('Ctrl Pts',(89.7450185772952,-1.36786993061414,-3.4641333692047));
#20593=CARTESIAN_POINT('Ctrl Pts',(89.7509600991481,-1.26303248756112,-3.50194467372989));
#20594=CARTESIAN_POINT('Ctrl Pts',(89.7568994468785,-1.15823340663876,-3.53974214233767));
#20595=CARTESIAN_POINT('Ctrl Pts',(89.762838794609,-1.05169126684827,-3.57284739456322));
#20596=CARTESIAN_POINT('Ctrl Pts',(89.7687781423395,-0.943863968004348,
-3.60110932525008));
#20597=CARTESIAN_POINT('Ctrl Pts',(89.7747167859086,-0.836049453025415,
-3.62936790523902));
#20598=CARTESIAN_POINT('Ctrl Pts',(89.7806554294777,-0.726950486274686,
-3.65278419961963));
#20599=CARTESIAN_POINT('Ctrl Pts',(89.7865940730467,-0.617038715247114,
-3.6712573849277));
#20600=CARTESIAN_POINT('Ctrl Pts',(89.7925334815143,-0.507112787561259,
-3.68973294958577));
#20601=CARTESIAN_POINT('Ctrl Pts',(89.7984728899819,-0.396374259757346,
-3.70326407049529));
#20602=CARTESIAN_POINT('Ctrl Pts',(89.8044122984495,-0.285302749002038,
-3.71180143648766));
#20603=CARTESIAN_POINT('Ctrl Pts',(89.8103577330006,-0.174118545845956,
-3.72034746443361));
#20604=CARTESIAN_POINT('Ctrl Pts',(89.8163031675517,-0.0626011024771197,
-3.72388958443186));
#20605=CARTESIAN_POINT('Ctrl Pts',(89.8222486021027,0.0487669533004773,
-3.72243056977102));
#20606=CARTESIAN_POINT('Ctrl Pts',(89.828197013161,0.160190764097268,-3.7209708246728));
#20607=CARTESIAN_POINT('Ctrl Pts',(89.8341454242193,0.271464620812649,-3.71450498062451));
#20608=CARTESIAN_POINT('Ctrl Pts',(89.8400938352775,0.382109900634831,-3.70308784480423));
#20609=CARTESIAN_POINT('Ctrl Pts',(89.8460520730076,0.492937964538579,-3.69165184807376));
#20610=CARTESIAN_POINT('Ctrl Pts',(89.8520103107377,0.603134962393357,-3.67524827598416));
#20611=CARTESIAN_POINT('Ctrl Pts',(89.8579685484677,0.712230864897388,-3.65398340959391));
#20612=CARTESIAN_POINT('Ctrl Pts',(89.8636954499186,0.817090978010045,-3.63354417912029));
#20613=CARTESIAN_POINT('Ctrl Pts',(89.8694223513694,0.920933598171998,-3.60861424150156));
#20614=CARTESIAN_POINT('Ctrl Pts',(89.8751492528202,1.02335606424254,-3.57933093304852));
#20615=CARTESIAN_POINT('Ctrl Pts',(89.8811214150547,1.13016488382587,-3.54879353505999));
#20616=CARTESIAN_POINT('Ctrl Pts',(89.8870935772892,1.2357768263794,-3.5134222186467));
#20617=CARTESIAN_POINT('Ctrl Pts',(89.8930657395237,1.33972368461136,-3.47332808864803));
#20618=CARTESIAN_POINT('Ctrl Pts',(89.8990302904206,1.44353806576116,-3.43328505738812));
#20619=CARTESIAN_POINT('Ctrl Pts',(89.9049948413175,1.5456911979247,-3.38853133134063));
#20620=CARTESIAN_POINT('Ctrl Pts',(89.9109593922145,1.64572867738106,-3.33922815676701));
#20621=CARTESIAN_POINT('Ctrl Pts',(89.9169179513963,1.74566566375918,-3.28997450990847));
#20622=CARTESIAN_POINT('Ctrl Pts',(89.9228765105781,1.84349085378072,-3.23618068824731));
#20623=CARTESIAN_POINT('Ctrl Pts',(89.9288350697599,1.9387691973511,-3.17805625530804));
#20624=CARTESIAN_POINT('Ctrl Pts',(89.9347893692583,2.03397942788164,-3.11997337464254));
#20625=CARTESIAN_POINT('Ctrl Pts',(89.9407436687567,2.12664607998298,-3.05756625762786));
#20626=CARTESIAN_POINT('Ctrl Pts',(89.9466979682551,2.21635873816701,-2.99109035407671));
#20627=CARTESIAN_POINT('Ctrl Pts',(89.9526500068231,2.30603733120718,-2.92463969235056));
#20628=CARTESIAN_POINT('Ctrl Pts',(89.9586020453912,2.39276382656832,-2.85412356309229));
#20629=CARTESIAN_POINT('Ctrl Pts',(89.9645540839593,2.47615736440155,-2.77984033160539));
#20630=CARTESIAN_POINT('Ctrl Pts',(89.9705053172727,2.55953961987637,-2.70556714993846));
#20631=CARTESIAN_POINT('Ctrl Pts',(89.9764565505861,2.63958950407324,-2.62752815635622));
#20632=CARTESIAN_POINT('Ctrl Pts',(89.9824077838996,2.71596037037465,-2.54606104189479));
#20633=CARTESIAN_POINT('Ctrl Pts',(89.9883596666548,2.79233957081956,-2.46458503715026));
#20634=CARTESIAN_POINT('Ctrl Pts',(89.9943115494101,2.86503867095313,-2.37968047156783));
#20635=CARTESIAN_POINT('Ctrl Pts',(90.0002634321653,2.93374944851159,-2.29172025689392));
#20636=CARTESIAN_POINT('Ctrl Pts',(90.0062210830347,3.00252681535395,-2.20367479783893));
#20637=CARTESIAN_POINT('Ctrl Pts',(90.0121787339041,3.0673078817417,-2.11256810252635));
#20638=CARTESIAN_POINT('Ctrl Pts',(90.0181363847736,3.1278260792076,-2.01880449294348));
#20639=CARTESIAN_POINT('Ctrl Pts',(90.0240968896036,3.18837326738795,-1.92499596672158));
#20640=CARTESIAN_POINT('Ctrl Pts',(90.0300573944337,3.24465330725029,-1.82852834930477));
#20641=CARTESIAN_POINT('Ctrl Pts',(90.0360178992638,3.29644510455139,-1.72983156266128));
#20642=CARTESIAN_POINT('Ctrl Pts',(90.0419878953307,3.34831937275502,-1.6309776157435));
#20643=CARTESIAN_POINT('Ctrl Pts',(90.0479578913976,3.39569093916524,-1.5298877833216));
#20644=CARTESIAN_POINT('Ctrl Pts',(90.0539278874645,3.43838627710061,-1.42701344490732));
#20645=CARTESIAN_POINT('Ctrl Pts',(90.0595292962938,3.47844560715767,-1.33049056263903));
#20646=CARTESIAN_POINT('Ctrl Pts',(90.0651307051232,3.51438867417209,-1.23239716786626));
#20647=CARTESIAN_POINT('Ctrl Pts',(90.0707321139525,3.54611246929201,-1.13311690377988));
#20648=CARTESIAN_POINT('Ctrl Pts',(90.0767130680232,3.57998583353691,-1.02710951925937));
#20649=CARTESIAN_POINT('Ctrl Pts',(90.082694022094,3.6091539858786,-0.919418023660391));
#20650=CARTESIAN_POINT('Ctrl Pts',(90.0886749761647,3.63345076832199,-0.810495574744447));
#20651=CARTESIAN_POINT('Ctrl Pts',(90.0946484815713,3.65771729161799,-0.701708777552929));
#20652=CARTESIAN_POINT('Ctrl Pts',(90.1006219869779,3.6771244218003,-0.591694477428052));
#20653=CARTESIAN_POINT('Ctrl Pts',(90.1065954923845,3.69155544891906,-0.480921958384125));
#20654=CARTESIAN_POINT('Ctrl Pts',(90.1125631543477,3.70597235921939,-0.370257799994276));
#20655=CARTESIAN_POINT('Ctrl Pts',(90.1185308163109,3.71542279680153,-0.258837307097464));
#20656=CARTESIAN_POINT('Ctrl Pts',(90.124498478274,3.7198410318604,-0.147140273846959));
#20657=CARTESIAN_POINT('Ctrl Pts',(90.130462064005,3.7242562490285,-0.0355195356421509));
#20658=CARTESIAN_POINT('Ctrl Pts',(90.136425649736,3.72364608555073,0.076376954208075));
#20659=CARTESIAN_POINT('Ctrl Pts',(90.1423892354669,3.71799667388885,0.188064604462056));
#20660=CARTESIAN_POINT('Ctrl Pts',(90.1483506677351,3.71234930224091,0.299711924080306));
#20661=CARTESIAN_POINT('Ctrl Pts',(90.1543121000032,3.70166632145048,0.411150140640219));
#20662=CARTESIAN_POINT('Ctrl Pts',(90.1602735322713,3.6859859660511,0.521895603137585));
#20663=CARTESIAN_POINT('Ctrl Pts',(90.1662342543009,3.67030747879221,0.632627871540938));
#20664=CARTESIAN_POINT('Ctrl Pts',(90.1721949763305,3.64963285929706,0.742667139782877));
#20665=CARTESIAN_POINT('Ctrl Pts',(90.1781556983601,3.62405202518205,0.851536541361508));
#20666=CARTESIAN_POINT('Ctrl Pts',(90.1841171524673,3.59846804930732,0.960419313946667));
#20667=CARTESIAN_POINT('Ctrl Pts',(90.1900786065745,3.56797675585565,1.06813153082633));
#20668=CARTESIAN_POINT('Ctrl Pts',(90.1960400606817,3.53271865541614,1.17420886735485));
#20669=CARTESIAN_POINT('Ctrl Pts',(90.2020073510064,3.49742603756896,1.28039005277553));
#20670=CARTESIAN_POINT('Ctrl Pts',(90.2079746413311,3.45735742142443,1.3849327665398));
#20671=CARTESIAN_POINT('Ctrl Pts',(90.2139419316557,3.41270252760531,1.4873900028494));
#20672=CARTESIAN_POINT('Ctrl Pts',(90.2199121266179,3.36802589757602,1.58989711122969));
#20673=CARTESIAN_POINT('Ctrl Pts',(90.22588232158,3.31875872333222,1.69031634674488));
#20674=CARTESIAN_POINT('Ctrl Pts',(90.2318525165421,3.26513721747072,1.78822440246955));
#20675=CARTESIAN_POINT('Ctrl Pts',(90.2378321847936,3.21143062694341,1.88628781515534));
#20676=CARTESIAN_POINT('Ctrl Pts',(90.2438118530451,3.15335611271743,1.98183173031227));
#20677=CARTESIAN_POINT('Ctrl Pts',(90.2497915212967,3.09119409200401,2.0744605679693));
#20678=CARTESIAN_POINT('Ctrl Pts',(90.2552993392261,3.03393722125247,2.15978014614141));
#20679=CARTESIAN_POINT('Ctrl Pts',(90.2608071571555,2.97321311211844,2.24262669166008));
#20680=CARTESIAN_POINT('Ctrl Pts',(90.2663149750849,2.90927030595616,2.32271691115852));
#20681=CARTESIAN_POINT('Ctrl Pts',(90.2721536793902,2.8414860867939,2.40761861186677));
#20682=CARTESIAN_POINT('Ctrl Pts',(90.2779923836955,2.76984747689865,2.48971884002926));
#20683=CARTESIAN_POINT('Ctrl Pts',(90.2838310880009,2.69461904302155,2.56863694894503));
#20684=CARTESIAN_POINT('Ctrl Pts',(90.2896622591304,2.61948766989435,2.64745323664192));
#20685=CARTESIAN_POINT('Ctrl Pts',(90.2954934302599,2.54077597214089,2.72309524927075));
#20686=CARTESIAN_POINT('Ctrl Pts',(90.3013246013894,2.45879016274089,2.79521349776875));
#20687=CARTESIAN_POINT('Ctrl Pts',(90.3072275517867,2.37579514245696,2.86821949161985));
#20688=CARTESIAN_POINT('Ctrl Pts',(90.313130502184,2.2894451207709,2.93761401254684));
#20689=CARTESIAN_POINT('Ctrl Pts',(90.3190334525814,2.20009821870295,3.00307099326009));
#20690=CARTESIAN_POINT('Ctrl Pts',(90.3248549934603,2.11198352896493,3.06762523535735));
#20691=CARTESIAN_POINT('Ctrl Pts',(90.3306765343393,2.02095446068037,3.12834959116476));
#20692=CARTESIAN_POINT('Ctrl Pts',(90.3364980752183,1.92738871149693,3.18497100729257));
#20693=CARTESIAN_POINT('Ctrl Pts',(90.3423177972162,1.83385219597801,3.2415747326361));
#20694=CARTESIAN_POINT('Ctrl Pts',(90.348137519214,1.73778094652395,3.29407783912181));
#20695=CARTESIAN_POINT('Ctrl Pts',(90.3539572412119,1.63958106793698,3.34225096067944));
#20696=CARTESIAN_POINT('Ctrl Pts',(90.3597767137142,1.54138539924807,3.39042201702136));
#20697=CARTESIAN_POINT('Ctrl Pts',(90.3655961862165,1.4410616746966,3.434263266282));
#20698=CARTESIAN_POINT('Ctrl Pts',(90.3714156587188,1.33903905919695,3.47359208319643));
#20699=CARTESIAN_POINT('Ctrl Pts',(90.3773806380693,1.23446552705938,3.51390425593767));
#20700=CARTESIAN_POINT('Ctrl Pts',(90.3833456174198,1.12810746066854,3.54947515349255));
#20701=CARTESIAN_POINT('Ctrl Pts',(90.3893105967704,1.02044559762071,3.58016177634426));
#20702=CARTESIAN_POINT('Ctrl Pts',(90.3951373490544,0.915278593754489,3.61013729499801));
#20703=CARTESIAN_POINT('Ctrl Pts',(90.4009641013384,0.80886800737136,3.63545240450293));
#20704=CARTESIAN_POINT('Ctrl Pts',(90.4067908536225,0.701672758016952,3.65602556106449));
#20705=CARTESIAN_POINT('Ctrl Pts',(90.4128249465063,0.590663046299211,3.67733079793624));
#20706=CARTESIAN_POINT('Ctrl Pts',(90.41885903939,0.47881230049198,3.69355024052747));
#20707=CARTESIAN_POINT('Ctrl Pts',(90.4248931322738,0.36663482167895,3.70465200390434));
#20708=CARTESIAN_POINT('Ctrl Pts',(90.4309272251575,0.254457342865911,3.71575376728122));
#20709=CARTESIAN_POINT('Ctrl Pts',(90.4369613180413,0.141953645119487,3.72173789897472));
#20710=CARTESIAN_POINT('Ctrl Pts',(90.4429954109251,0.029635062354076,3.72263204273257));
#20711=CARTESIAN_POINT('',(90.4430005297901,3.5302572329849,1.18158852036477));
#20712=CARTESIAN_POINT('Origin',(90.4430005297901,0.,0.));
#20713=CARTESIAN_POINT('',(89.7537451115497,-3.72274996600548,0.000503096633030775));
#20714=CARTESIAN_POINT('Ctrl Pts',(89.7537451115497,-3.72274996600548,0.000503096633030831));
#20715=CARTESIAN_POINT('Ctrl Pts',(89.7599512036108,-3.7227657376518,-0.11620190985295));
#20716=CARTESIAN_POINT('Ctrl Pts',(89.7661572956718,-3.71728927921443,-0.232822253785277));
#20717=CARTESIAN_POINT('Ctrl Pts',(89.7723633877328,-3.70637040353398,-0.348835196485874));
#20718=CARTESIAN_POINT('Ctrl Pts',(89.7785765674432,-3.6954390579834,-0.464980631429494));
#20719=CARTESIAN_POINT('Ctrl Pts',(89.7847897471536,-3.67905293405017,-0.580516922988185));
#20720=CARTESIAN_POINT('Ctrl Pts',(89.791002926864,-3.65731331519107,-0.694929404347014));
#20721=CARTESIAN_POINT('Ctrl Pts',(89.7972291983796,-3.63552788873094,-0.809582964509177));
#20722=CARTESIAN_POINT('Ctrl Pts',(89.8034554698953,-3.60836649028465,-0.923107626647784));
#20723=CARTESIAN_POINT('Ctrl Pts',(89.809681741411,-3.57598115751633,-1.03500063941437));
#20724=CARTESIAN_POINT('Ctrl Pts',(89.8159150699073,-3.543559118564,-1.14702047395997));
#20725=CARTESIAN_POINT('Ctrl Pts',(89.8221483984037,-3.50590144927669,-1.25740462855842));
#20726=CARTESIAN_POINT('Ctrl Pts',(89.8283817269001,-3.46320891153749,-1.36566891944839));
#20727=CARTESIAN_POINT('Ctrl Pts',(89.8346278435039,-3.42042878708434,-1.4741553220698));
#20728=CARTESIAN_POINT('Ctrl Pts',(89.8408739601077,-3.37259329515473,-1.58051283856969));
#20729=CARTESIAN_POINT('Ctrl Pts',(89.8471200767115,-3.31995031615005,-1.6842795079188));
#20730=CARTESIAN_POINT('Ctrl Pts',(89.850164033272,-3.29429550509387,-1.73484872619658));
#20731=CARTESIAN_POINT('Ctrl Pts',(89.8532079898325,-3.26749960874441,-1.78480303788735));
#20732=CARTESIAN_POINT('Ctrl Pts',(89.856251946393,-3.23959504134923,-1.83409147279122));
#20733=CARTESIAN_POINT('Ctrl Pts',(89.8621583025938,-3.18545027568409,-1.92972853177436));
#20734=CARTESIAN_POINT('Ctrl Pts',(89.8680646587945,-3.12696964229294,-2.02313739625222));
#20735=CARTESIAN_POINT('Ctrl Pts',(89.8739710149952,-3.06436251000767,-2.11389450298719));
#20736=CARTESIAN_POINT('Ctrl Pts',(89.8798697866757,-3.001835773325,-2.20453506593522));
#20737=CARTESIAN_POINT('Ctrl Pts',(89.8857685583561,-2.93519330999383,-2.29253029220606));
#20738=CARTESIAN_POINT('Ctrl Pts',(89.8916673300365,-2.86469027909109,-2.37748126541115));
#20739=CARTESIAN_POINT('Ctrl Pts',(89.8975602106855,-2.79425765870664,-2.46234739911394));
#20740=CARTESIAN_POINT('Ctrl Pts',(89.9034530913345,-2.7199724064974,-2.54417499829643));
#20741=CARTESIAN_POINT('Ctrl Pts',(89.9093459719835,-2.64213238104237,-2.62259490649001));
#20742=CARTESIAN_POINT('Ctrl Pts',(89.9152830067977,-2.56370911598825,-2.701602399227));
#20743=CARTESIAN_POINT('Ctrl Pts',(89.921220041612,-2.48167783266002,-2.77715055978529));
#20744=CARTESIAN_POINT('Ctrl Pts',(89.9271570764262,-2.39638394500998,-2.84889654964837));
#20745=CARTESIAN_POINT('Ctrl Pts',(89.9330440800188,-2.31180882649886,-2.92003793811767));
#20746=CARTESIAN_POINT('Ctrl Pts',(89.9389310836114,-2.22402622323072,-2.98744072580214));
#20747=CARTESIAN_POINT('Ctrl Pts',(89.9448180872039,-2.13340829389835,-3.05080917364979));
#20748=CARTESIAN_POINT('Ctrl Pts',(89.9507046169406,-2.04279765857208,-3.11417252085292));
#20749=CARTESIAN_POINT('Ctrl Pts',(89.9565911466773,-1.94935249985621,-3.1735019293205));
#20750=CARTESIAN_POINT('Ctrl Pts',(89.9624776764139,-1.85347519871799,-3.22854413787969));
#20751=CARTESIAN_POINT('Ctrl Pts',(89.9683652527117,-1.7575808516366,-3.28359613234594));
#20752=CARTESIAN_POINT('Ctrl Pts',(89.9742528290094,-1.65925387239635,-3.33435920010058));
#20753=CARTESIAN_POINT('Ctrl Pts',(89.9801404053071,-1.55892176495189,-3.38062575468792));
#20754=CARTESIAN_POINT('Ctrl Pts',(89.9861149388253,-1.45710779115981,-3.42757564835794));
#20755=CARTESIAN_POINT('Ctrl Pts',(89.9920894723435,-1.35322939292269,-3.46989494412881));
#20756=CARTESIAN_POINT('Ctrl Pts',(89.9980640058617,-1.24775336896973,-3.5074177242987));
#20757=CARTESIAN_POINT('Ctrl Pts',(90.0039617045284,-1.14363380817999,-3.54445794675382));
#20758=CARTESIAN_POINT('Ctrl Pts',(90.0098594031951,-1.03795790361118,-3.57682424444751));
#20759=CARTESIAN_POINT('Ctrl Pts',(90.0157571018618,-0.931187775105836,
-3.60440798051406));
#20760=CARTESIAN_POINT('Ctrl Pts',(90.0217700528058,-0.822331154708589,
-3.63253075537785));
#20761=CARTESIAN_POINT('Ctrl Pts',(90.0277830037497,-0.712337557539733,
-3.65568200449768));
#20762=CARTESIAN_POINT('Ctrl Pts',(90.0337959546936,-0.601703826612937,
-3.67380185469213));
#20763=CARTESIAN_POINT('Ctrl Pts',(90.0398089056375,-0.491070095686133,
-3.69192170488658));
#20764=CARTESIAN_POINT('Ctrl Pts',(90.0458218565815,-0.379796697029761,
-3.70501017755296));
#20765=CARTESIAN_POINT('Ctrl Pts',(90.0518348075254,-0.268380670821446,
-3.71306334150516));
#20766=CARTESIAN_POINT('Ctrl Pts',(90.0578840925175,-0.156291398598147,
-3.72116516776137));
#20767=CARTESIAN_POINT('Ctrl Pts',(90.0639333775095,-0.043666389847885,
-3.7241992834387));
#20768=CARTESIAN_POINT('Ctrl Pts',(90.0699826625016,0.0690062792362871,
-3.72211038201797));
#20769=CARTESIAN_POINT('Ctrl Pts',(90.0760236191776,0.181523826912398,-3.72002435647949));
#20770=CARTESIAN_POINT('Ctrl Pts',(90.0820645758535,0.29408850410863,-3.71282935507544));
#20771=CARTESIAN_POINT('Ctrl Pts',(90.0881055325295,0.406208228326725,-3.70052191423584));
#20772=CARTESIAN_POINT('Ctrl Pts',(90.0941396621041,0.518201242032032,-3.68822838247558));
#20773=CARTESIAN_POINT('Ctrl Pts',(90.1001737916788,0.629749904560712,-3.67083395347465));
#20774=CARTESIAN_POINT('Ctrl Pts',(90.1062079212534,0.740363809626243,-3.64838717680782));
#20775=CARTESIAN_POINT('Ctrl Pts',(90.1122361716886,0.850869941968559,-3.62596227035926));
#20776=CARTESIAN_POINT('Ctrl Pts',(90.1182644221237,0.960442736497499,-3.59849489909187));
#20777=CARTESIAN_POINT('Ctrl Pts',(90.1242926725589,1.06859925975183,-3.56608513422743));
#20778=CARTESIAN_POINT('Ctrl Pts',(90.1303176185233,1.17669649547857,-3.53369313523388));
#20779=CARTESIAN_POINT('Ctrl Pts',(90.1363425644877,1.28337861886902,-3.49636424846651));
#20780=CARTESIAN_POINT('Ctrl Pts',(90.1423675104521,1.38817548640195,-3.45424903292347));
#20781=CARTESIAN_POINT('Ctrl Pts',(90.1483904990954,1.49293830862879,-3.41214749932949));
#20782=CARTESIAN_POINT('Ctrl Pts',(90.1544134877387,1.59581671987081,-3.36526288194251));
#20783=CARTESIAN_POINT('Ctrl Pts',(90.1604364763819,1.69635882928629,-3.31379454474813));
#20784=CARTESIAN_POINT('Ctrl Pts',(90.166458852972,1.7968907216628,-3.26233143774048));
#20785=CARTESIAN_POINT('Ctrl Pts',(90.1724812295622,1.89508642622163,-3.20628572291655));
#20786=CARTESIAN_POINT('Ctrl Pts',(90.1785036061523,1.9905175443936,-3.14590328331328));
#20787=CARTESIAN_POINT('Ctrl Pts',(90.1845293098987,2.08600138498086,-3.08548748448591));
#20788=CARTESIAN_POINT('Ctrl Pts',(90.1905550136451,2.17871724465894,-3.02073038761758));
#20789=CARTESIAN_POINT('Ctrl Pts',(90.1965807173915,2.26826465617017,-2.95192191835577));
#20790=CARTESIAN_POINT('Ctrl Pts',(90.2026080049839,2.35783560506721,-2.88309536290408));
#20791=CARTESIAN_POINT('Ctrl Pts',(90.2086352925763,2.44423613268206,-2.81021556759798));
#20792=CARTESIAN_POINT('Ctrl Pts',(90.2146625801687,2.52709895717264,-2.73361270540597));
#20793=CARTESIAN_POINT('Ctrl Pts',(90.2206965450462,2.61005358061807,-2.65692497931112));
#20794=CARTESIAN_POINT('Ctrl Pts',(90.2267305099237,2.6894623804383,-2.57650622715388));
#20795=CARTESIAN_POINT('Ctrl Pts',(90.2327644748012,2.76499482777154,-2.49272364390773));
#20796=CARTESIAN_POINT('Ctrl Pts',(90.2376488727534,2.82613713445795,-2.42490298430147));
#20797=CARTESIAN_POINT('Ctrl Pts',(90.2425332707056,2.88474007503412,-2.35487887900625));
#20798=CARTESIAN_POINT('Ctrl Pts',(90.2474176686577,2.94064827745286,-2.28286120270452));
#20799=CARTESIAN_POINT('Ctrl Pts',(90.2534516475349,3.00971490874737,-2.1938936079576));
#20800=CARTESIAN_POINT('Ctrl Pts',(90.2594856264121,3.07480863629318,-2.10170138960284));
#20801=CARTESIAN_POINT('Ctrl Pts',(90.2655196052893,3.13562421825931,-2.00667095567901));
#20802=CARTESIAN_POINT('Ctrl Pts',(90.2715487836387,3.19639141641505,-1.91171612630169));
#20803=CARTESIAN_POINT('Ctrl Pts',(90.2775779619882,3.25288702530268,-1.81392791401824));
#20804=CARTESIAN_POINT('Ctrl Pts',(90.2836071403376,3.30484797888165,-1.71372325624118));
#20805=CARTESIAN_POINT('Ctrl Pts',(90.289632992101,3.35678026311715,-1.61357388616678));
#20806=CARTESIAN_POINT('Ctrl Pts',(90.2956588438643,3.40418268650556,-1.51101108237129));
#20807=CARTESIAN_POINT('Ctrl Pts',(90.3016846956277,3.44683746281631,-1.40647753889851));
#20808=CARTESIAN_POINT('Ctrl Pts',(90.3077085814766,3.48947832314596,-1.30197809915199));
#20809=CARTESIAN_POINT('Ctrl Pts',(90.3137324673256,3.5273744688306,-1.19550957398247));
#20810=CARTESIAN_POINT('Ctrl Pts',(90.3197563531745,3.56035595604716,-1.08753529999698));
#20811=CARTESIAN_POINT('Ctrl Pts',(90.3257805290223,3.5933390310418,-0.97955582796857));
#20812=CARTESIAN_POINT('Ctrl Pts',(90.3318047048702,3.62140685386691,-0.870070847711997));
#20813=CARTESIAN_POINT('Ctrl Pts',(90.337828880718,3.6444392446607,-0.75955918431481));
#20814=CARTESIAN_POINT('Ctrl Pts',(90.3402889535533,3.65384490617449,-0.714429900579265));
#20815=CARTESIAN_POINT('Ctrl Pts',(90.3427490263886,3.66241142849172,-0.669129549522075));
#20816=CARTESIAN_POINT('Ctrl Pts',(90.3452090992239,3.67013307523028,-0.623691247814765));
#20817=CARTESIAN_POINT('Ctrl Pts',(90.3519493338375,3.69128924177713,-0.499197041970545));
#20818=CARTESIAN_POINT('Ctrl Pts',(90.3586895684512,3.70608966530002,-0.37372607149069));
#20819=CARTESIAN_POINT('Ctrl Pts',(90.3654298030648,3.71448732777005,-0.247894038524024));
#20820=CARTESIAN_POINT('Ctrl Pts',(90.3721853209071,3.72290403162413,-0.121776686151497));
#20821=CARTESIAN_POINT('Ctrl Pts',(90.3789408387494,3.72488891581502,0.00470315930204165));
#20822=CARTESIAN_POINT('Ctrl Pts',(90.3856963565917,3.72044700092353,0.130926222809181));
#20823=CARTESIAN_POINT('Ctrl Pts',(90.3924547873692,3.7160031707073,0.25720371287845));
#20824=CARTESIAN_POINT('Ctrl Pts',(90.3992132181468,3.70512702164482,0.383223993907095));
#20825=CARTESIAN_POINT('Ctrl Pts',(90.4059716489243,3.68787564481499,0.508370721895352));
#20826=CARTESIAN_POINT('Ctrl Pts',(90.4127260755569,3.67063448885085,0.633443304619199));
#20827=CARTESIAN_POINT('Ctrl Pts',(90.4194805021895,3.64702568694021,0.757643165561556));
#20828=CARTESIAN_POINT('Ctrl Pts',(90.4262349288221,3.6171578044059,0.88036184635948));
#20829=CARTESIAN_POINT('Ctrl Pts',(90.4318234624781,3.59244546746669,0.981897848623131));
#20830=CARTESIAN_POINT('Ctrl Pts',(90.4374119961341,3.56344927633744,1.082419944246));
#20831=CARTESIAN_POINT('Ctrl Pts',(90.4430005297901,3.5302572329849,1.18158852036477));
#20832=CARTESIAN_POINT('Ctrl Pts',(89.7566589927103,-3.72274994160873,0.000659357419522499));
#20833=CARTESIAN_POINT('Ctrl Pts',(89.7548842680598,-3.72274408006351,0.0337538012808603));
#20834=CARTESIAN_POINT('Ctrl Pts',(89.7530965611029,-3.72229691578573,0.0668461131889498));
#20835=CARTESIAN_POINT('Ctrl Pts',(89.7488269168412,-3.72019059588082,0.145287725484996));
#20836=CARTESIAN_POINT('Ctrl Pts',(89.7463339333092,-3.7181433796351,0.190620476795769));
#20837=CARTESIAN_POINT('Ctrl Pts',(89.7266764545911,-3.69567992210142,0.54440014442492));
#20838=CARTESIAN_POINT('Ctrl Pts',(89.708392504169,-3.6377447484145,0.849223948899964));
#20839=CARTESIAN_POINT('Ctrl Pts',(89.6849660701368,-3.51479749359358,1.23020361268767));
#20840=CARTESIAN_POINT('Ctrl Pts',(89.679660158538,-3.48357147177563,1.31602944805247));
#20841=CARTESIAN_POINT('Ctrl Pts',(89.6709090180228,-3.42585376385813,1.45816693176171));
#20842=CARTESIAN_POINT('Ctrl Pts',(89.6674128539193,-3.40104952542244,1.51511970867108));
#20843=CARTESIAN_POINT('Ctrl Pts',(89.6623070451736,-3.36199869035049,1.59898607879666));
#20844=CARTESIAN_POINT('Ctrl Pts',(89.6606458111315,-3.34882924909552,1.62638693204885));
#20845=CARTESIAN_POINT('Ctrl Pts',(89.6576145772363,-3.32390150226231,1.67666567167764));
#20846=CARTESIAN_POINT('Ctrl Pts',(89.6562397927448,-3.31223993366645,1.69958690024722));
#20847=CARTESIAN_POINT('Ctrl Pts',(89.652861576564,-3.28270889279143,1.75617260522631));
#20848=CARTESIAN_POINT('Ctrl Pts',(89.6508741592126,-3.26455855763923,1.78968643437814));
#20849=CARTESIAN_POINT('Ctrl Pts',(89.642385997097,-3.1838545696962,1.93338841465287));
#20850=CARTESIAN_POINT('Ctrl Pts',(89.636136557727,-3.11620874804651,2.04062945968947));
#20851=CARTESIAN_POINT('Ctrl Pts',(89.6193872732306,-2.91743945728341,2.32273632390737));
#20852=CARTESIAN_POINT('Ctrl Pts',(89.6090943159204,-2.77619621897553,2.48983778588698));
#20853=CARTESIAN_POINT('Ctrl Pts',(89.5984125828405,-2.62112000708803,2.64359555736933));
#20854=CARTESIAN_POINT('Ctrl Pts',(90.1028989154209,-1.84736391785682,1.20202435615052));
#20855=CARTESIAN_POINT('Ctrl Pts',(90.140690073821,-2.22792678283258,0.617153363646938));
#20856=CARTESIAN_POINT('Ctrl Pts',(90.2162692554159,-2.38778162526882,-0.933200414266254));
#20857=CARTESIAN_POINT('Ctrl Pts',(90.3296364602056,-0.62872205324772,-2.48534112021196));
#20858=CARTESIAN_POINT('Ctrl Pts',(90.4052125065953,0.88959187531312,-2.13379067845246));
#20859=CARTESIAN_POINT('Ctrl Pts',(90.4430005297901,1.42252785196827,-1.68345790276281));
#20860=CARTESIAN_POINT('Ctrl Pts',(90.1853507684723,-1.72766177787012,1.12413775981909));
#20861=CARTESIAN_POINT('Ctrl Pts',(90.2231419268724,-2.08356561984736,0.577164178184089));
#20862=CARTESIAN_POINT('Ctrl Pts',(90.2987211084673,-2.23306247783782,-0.872732584650031));
#20863=CARTESIAN_POINT('Ctrl Pts',(90.4120883132569,-0.587983260796952,
-2.32430048939166));
#20864=CARTESIAN_POINT('Ctrl Pts',(90.4876643596466,0.831949712791466,-1.99552917619753));
#20865=CARTESIAN_POINT('Ctrl Pts',(90.5254523828415,1.33035346963605,-1.5743762477676));
#20866=CARTESIAN_POINT('Ctrl Pts',(90.2678026215237,-1.60795963788343,1.04625116348766));
#20867=CARTESIAN_POINT('Ctrl Pts',(90.3055937799238,-1.93920445686214,0.537174992721241));
#20868=CARTESIAN_POINT('Ctrl Pts',(90.3811729615186,-2.07834333040681,-0.812264755033806));
#20869=CARTESIAN_POINT('Ctrl Pts',(90.4945401663084,-0.547244468346182,
-2.16325985857137));
#20870=CARTESIAN_POINT('Ctrl Pts',(90.5701162126981,0.774307550269809,-1.85726767394259));
#20871=CARTESIAN_POINT('Ctrl Pts',(90.6079042358929,1.23817908730384,-1.4652945927724));
#20872=CARTESIAN_POINT('Ctrl Pts',(90.3502544745751,-1.48825749789673,0.968364567156219));
#20873=CARTESIAN_POINT('Ctrl Pts',(90.3880456329751,-1.79484329387692,0.497185807258393));
#20874=CARTESIAN_POINT('Ctrl Pts',(90.4636248145701,-1.92362418297579,-0.751796925417581));
#20875=CARTESIAN_POINT('Ctrl Pts',(90.5769920193598,-0.506505675895414,
-2.00221922775108));
#20876=CARTESIAN_POINT('Ctrl Pts',(90.6525680657495,0.716665387748153,-1.71900617168766));
#20877=CARTESIAN_POINT('Ctrl Pts',(90.6903560889443,1.14600470497162,-1.35621293777719));
#20878=CARTESIAN_POINT('',(90.4430005297901,1.42252785196811,-1.68345790276294));
#20879=CARTESIAN_POINT('',(90.4428667905869,-1.7396164773305,-0.358885182614483));
#20880=CARTESIAN_POINT('Ctrl Pts',(90.4430005297901,1.4225278519681,-1.68345790276293));
#20881=CARTESIAN_POINT('Ctrl Pts',(90.4430005297901,1.35849356753156,-1.72802743598208));
#20882=CARTESIAN_POINT('Ctrl Pts',(90.4430005297901,1.29211327677448,-1.7687933284719));
#20883=CARTESIAN_POINT('Ctrl Pts',(90.4430005297901,1.22375356660468,-1.80575874571043));
#20884=CARTESIAN_POINT('Ctrl Pts',(90.4430005297901,1.15444662535534,-1.84323637682451));
#20885=CARTESIAN_POINT('Ctrl Pts',(90.4430005297901,1.08310399461725,-1.87680762782933));
#20886=CARTESIAN_POINT('Ctrl Pts',(90.4430005297901,1.01008882142485,-1.90642508439205));
#20887=CARTESIAN_POINT('Ctrl Pts',(90.4430005297901,0.937375387734288,-1.93592014507186));
#20888=CARTESIAN_POINT('Ctrl Pts',(90.4430005297901,0.863002156171073,-1.96149402884632));
#20889=CARTESIAN_POINT('Ctrl Pts',(90.4430005297901,0.787324930426492,-1.98304902266566));
#20890=CARTESIAN_POINT('Ctrl Pts',(90.4430005297901,0.744830143821219,-1.99515272828672));
#20891=CARTESIAN_POINT('Ctrl Pts',(90.4430005297901,0.701924229083204,-2.0059883116318));
#20892=CARTESIAN_POINT('Ctrl Pts',(90.4430005297901,0.658671653783695,-2.0155313726465));
#20893=CARTESIAN_POINT('Ctrl Pts',(90.4430005297901,0.646172907588059,-2.01828904191188));
#20894=CARTESIAN_POINT('Ctrl Pts',(90.4430005297901,0.633654218360875,-2.02093674442495));
#20895=CARTESIAN_POINT('Ctrl Pts',(90.4430005297901,0.6211203149044,-2.02347372260163));
#20896=CARTESIAN_POINT('Ctrl Pts',(90.4430005297901,0.545600596598426,-2.0387596132195));
#20897=CARTESIAN_POINT('Ctrl Pts',(90.4430005297901,0.469491648685046,-2.0500382632572));
#20898=CARTESIAN_POINT('Ctrl Pts',(90.4430005297901,0.393135312093146,-2.05726598238603));
#20899=CARTESIAN_POINT('Ctrl Pts',(90.4430005297901,0.317994445849382,-2.06437864782478));
#20900=CARTESIAN_POINT('Ctrl Pts',(90.4430005297901,0.242613051514531,-2.06756819235912));
#20901=CARTESIAN_POINT('Ctrl Pts',(90.4430005297901,0.167322657723717,-2.06674371029438));
#20902=CARTESIAN_POINT('Ctrl Pts',(90.4430005297901,0.111038822526298,-2.06612736323709));
#20903=CARTESIAN_POINT('Ctrl Pts',(90.4430005297901,0.0548058830297967,
-2.0632668109814));
#20904=CARTESIAN_POINT('Ctrl Pts',(90.4430005297901,-0.00123083108011989,
-2.05810621712316));
#20905=CARTESIAN_POINT('Ctrl Pts',(90.4430005297901,-0.0254665698698807,
-2.05587427317829));
#20906=CARTESIAN_POINT('Ctrl Pts',(90.4430005297901,-0.0496655066289073,
-2.05321190325344));
#20907=CARTESIAN_POINT('Ctrl Pts',(90.4430005297901,-0.0738153724767186,
-2.05011370335277));
#20908=CARTESIAN_POINT('Ctrl Pts',(90.4430005297901,-0.0915898373131226,
-2.04783340724109));
#20909=CARTESIAN_POINT('Ctrl Pts',(90.4430005297901,-0.109337713577794,
-2.04531700834962));
#20910=CARTESIAN_POINT('Ctrl Pts',(90.4430005297901,-0.12705398082619,-2.04256216657337));
#20911=CARTESIAN_POINT('Ctrl Pts',(90.4430005297901,-0.141731501026051,
-2.04027984348287));
#20912=CARTESIAN_POINT('Ctrl Pts',(90.4430005297901,-0.156389839833323,
-2.03783328837979));
#20913=CARTESIAN_POINT('Ctrl Pts',(90.4430005297901,-0.171003090990929,
-2.03522554868848));
#20914=CARTESIAN_POINT('Ctrl Pts',(90.4430005297901,-0.242576842352592,
-2.02245318815975));
#20915=CARTESIAN_POINT('Ctrl Pts',(90.4430005297901,-0.313187615395148,
-2.00580133374315));
#20916=CARTESIAN_POINT('Ctrl Pts',(90.4430005297901,-0.382533842296707,
-1.98519475375429));
#20917=CARTESIAN_POINT('Ctrl Pts',(90.4430005297901,-0.42007629343071,-1.97403882564058));
#20918=CARTESIAN_POINT('Ctrl Pts',(90.4430005297901,-0.457247853160681,
-1.96172298204887));
#20919=CARTESIAN_POINT('Ctrl Pts',(90.4430005297901,-0.493997977180846,
-1.94822944989875));
#20920=CARTESIAN_POINT('Ctrl Pts',(90.4430005297901,-0.563441751304489,
-1.92273179992486));
#20921=CARTESIAN_POINT('Ctrl Pts',(90.4430005297901,-0.631383008777137,
-1.89303101435383));
#20922=CARTESIAN_POINT('Ctrl Pts',(90.4430005297901,-0.697549630821063,
-1.85938942477736));
#20923=CARTESIAN_POINT('Ctrl Pts',(90.4430005297901,-0.728482655886315,
-1.84366191592987));
#20924=CARTESIAN_POINT('Ctrl Pts',(90.4430005297901,-0.759027301881822,
-1.82707257188128));
#20925=CARTESIAN_POINT('Ctrl Pts',(90.4430005297901,-0.789152711196381,
-1.80964576389468));
#20926=CARTESIAN_POINT('Ctrl Pts',(90.4430005297901,-0.805665241648401,
-1.80009367135528));
#20927=CARTESIAN_POINT('Ctrl Pts',(90.4430005297901,-0.822051778690102,
-1.79028994553457));
#20928=CARTESIAN_POINT('Ctrl Pts',(90.4430005297901,-0.838306956091588,
-1.78023844910883));
#20929=CARTESIAN_POINT('Ctrl Pts',(90.4430005297901,-0.848486765356263,
-1.77394369674094));
#20930=CARTESIAN_POINT('Ctrl Pts',(90.4430005297901,-0.858617377556729,
-1.76755026518767));
#20931=CARTESIAN_POINT('Ctrl Pts',(90.4430005297901,-0.868689640147188,
-1.76106412386971));
#20932=CARTESIAN_POINT('Ctrl Pts',(90.4430005297901,-0.929470414251205,
-1.72192369373168));
#20933=CARTESIAN_POINT('Ctrl Pts',(90.4430005297901,-0.98799906476567,-1.67949685006462));
#20934=CARTESIAN_POINT('Ctrl Pts',(90.4430005297901,-1.04404927334162,-1.63406019156795));
#20935=CARTESIAN_POINT('Ctrl Pts',(90.4430005297901,-1.09986300683067,-1.5888152297311));
#20936=CARTESIAN_POINT('Ctrl Pts',(90.4430005297901,-1.15321978054266,-1.54058487743322));
#20937=CARTESIAN_POINT('Ctrl Pts',(90.4430005297901,-1.20385708288004,-1.48960963106486));
#20938=CARTESIAN_POINT('Ctrl Pts',(90.4430005297901,-1.25409004216062,-1.43904142626441));
#20939=CARTESIAN_POINT('Ctrl Pts',(90.4430005297901,-1.30164732632187,-1.38577112858578));
#20940=CARTESIAN_POINT('Ctrl Pts',(90.4430005297901,-1.34622563323271,-1.3300145930638));
#20941=CARTESIAN_POINT('Ctrl Pts',(90.4430005297901,-1.36342852935171,-1.30849798655699));
#20942=CARTESIAN_POINT('Ctrl Pts',(90.4430005297901,-1.38018725088433,-1.28661099372197));
#20943=CARTESIAN_POINT('Ctrl Pts',(90.4430005297901,-1.39648221326537,-1.26436566883623));
#20944=CARTESIAN_POINT('Ctrl Pts',(90.4430005297901,-1.40413618854342,-1.25391672377294));
#20945=CARTESIAN_POINT('Ctrl Pts',(90.4430005297901,-1.41168748957156,-1.24338902200558));
#20946=CARTESIAN_POINT('Ctrl Pts',(90.4430005297901,-1.41912637484512,-1.2327951746032));
#20947=CARTESIAN_POINT('Ctrl Pts',(90.4430005297901,-1.45875449510069,-1.17636007130584));
#20948=CARTESIAN_POINT('Ctrl Pts',(90.4430005297901,-1.49525634166901,-1.11796797580368));
#20949=CARTESIAN_POINT('Ctrl Pts',(90.4430005297901,-1.52837656473231,-1.05783238657754));
#20950=CARTESIAN_POINT('Ctrl Pts',(90.4430005297901,-1.5611740548108,-0.998282775838552));
#20951=CARTESIAN_POINT('Ctrl Pts',(90.4430005297902,-1.59065591048662,-0.937022733178433));
#20952=CARTESIAN_POINT('Ctrl Pts',(90.4430005297902,-1.616524485471,-0.874251203149238));
#20953=CARTESIAN_POINT('Ctrl Pts',(90.4430005297902,-1.62298306524415,-0.858579101596652));
#20954=CARTESIAN_POINT('Ctrl Pts',(90.4430005297902,-1.62921615191983,-0.842812771601484));
#20955=CARTESIAN_POINT('Ctrl Pts',(90.4430005297902,-1.63521857834345,-0.826955310014826));
#20956=CARTESIAN_POINT('Ctrl Pts',(90.4430005297902,-1.64047153672405,-0.813077824501807));
#20957=CARTESIAN_POINT('Ctrl Pts',(90.4430005297902,-1.64554478527699,-0.799138477894352));
#20958=CARTESIAN_POINT('Ctrl Pts',(90.4430005297902,-1.65043379611914,-0.785144399166619));
#20959=CARTESIAN_POINT('Ctrl Pts',(90.4430005297902,-1.66472446959871,-0.74423943572875));
#20960=CARTESIAN_POINT('Ctrl Pts',(90.4430005297902,-1.6774468220569,-0.702853420185196));
#20961=CARTESIAN_POINT('Ctrl Pts',(90.4430005297902,-1.6885285201336,-0.661040028896644));
#20962=CARTESIAN_POINT('Ctrl Pts',(90.4430005297902,-1.70605020045711,-0.594927338374926));
#20963=CARTESIAN_POINT('Ctrl Pts',(90.4430005297902,-1.71947262347024,-0.527745396103237));
#20964=CARTESIAN_POINT('Ctrl Pts',(90.4430005297902,-1.72885247363129,-0.459849352294044));
#20965=CARTESIAN_POINT('Ctrl Pts',(90.4430005297902,-1.73338742826376,-0.427023083951613));
#20966=CARTESIAN_POINT('Ctrl Pts',(90.4430005297902,-1.7369766488472,-0.394030018132786));
#20967=CARTESIAN_POINT('Ctrl Pts',(90.4430005297902,-1.73962237473193,-0.360911589357311));
#20968=CARTESIAN_POINT('',(90.3498698986824,-0.176530238082943,-2.19735656904503));
#20969=CARTESIAN_POINT('Ctrl Pts',(90.4430005297901,1.42252785196811,-1.68345790276294));
#20970=CARTESIAN_POINT('Ctrl Pts',(90.4119569860875,0.984711319553738,-2.05341441334118));
#20971=CARTESIAN_POINT('Ctrl Pts',(90.380913442385,0.394220067868452,-2.23807424546201));
#20972=CARTESIAN_POINT('Ctrl Pts',(90.3498698986824,-0.175612058744845,
-2.19751079506226));
#20973=CARTESIAN_POINT('',(90.3498698986825,-1.48890580190326,0.968619417293912));
#20974=CARTESIAN_POINT('Ctrl Pts',(90.3498698986825,-0.181591443149779,
-2.19650644155094));
#20975=CARTESIAN_POINT('Ctrl Pts',(90.3498698986824,-0.257547497917166,
-2.18363784310906));
#20976=CARTESIAN_POINT('Ctrl Pts',(90.3498698986824,-0.332599118530171,
-2.16671926797206));
#20977=CARTESIAN_POINT('Ctrl Pts',(90.3498698986824,-0.406428811432396,
-2.14565653022378));
#20978=CARTESIAN_POINT('Ctrl Pts',(90.3498698986824,-0.449282745765007,
-2.13343080985508));
#20979=CARTESIAN_POINT('Ctrl Pts',(90.3498698986825,-0.491724687026791,
-2.11980798846392));
#20980=CARTESIAN_POINT('Ctrl Pts',(90.3498698986825,-0.533688867832712,
-2.1047624027297));
#20981=CARTESIAN_POINT('Ctrl Pts',(90.3498698986825,-0.572294897306728,
-2.09092082843577));
#20982=CARTESIAN_POINT('Ctrl Pts',(90.3498698986825,-0.610496552067541,
-2.07587494667674));
#20983=CARTESIAN_POINT('Ctrl Pts',(90.3498698986825,-0.648253856041703,
-2.05966215463177));
#20984=CARTESIAN_POINT('Ctrl Pts',(90.3498698986825,-0.670857500514949,
-2.0499562660028));
#20985=CARTESIAN_POINT('Ctrl Pts',(90.3498698986824,-0.693301845759939,
-2.03983211447534));
#20986=CARTESIAN_POINT('Ctrl Pts',(90.3498698986824,-0.715577834954399,
-2.02929728759008));
#20987=CARTESIAN_POINT('Ctrl Pts',(90.3498698986824,-0.727802722918561,
-2.0235158573124));
#20988=CARTESIAN_POINT('Ctrl Pts',(90.3498698986825,-0.739974677490576,
-2.01761172654651));
#20989=CARTESIAN_POINT('Ctrl Pts',(90.3498698986825,-0.752084605070809,
-2.01159021316281));
#20990=CARTESIAN_POINT('Ctrl Pts',(90.3498698986825,-0.821813208959802,
-1.97691851766653));
#20991=CARTESIAN_POINT('Ctrl Pts',(90.3498698986824,-0.889562996748929,
-1.93832331975832));
#20992=CARTESIAN_POINT('Ctrl Pts',(90.3498698986824,-0.955077779448591,
-1.89609020462415));
#20993=CARTESIAN_POINT('Ctrl Pts',(90.3498698986824,-1.00782120597658,-1.86208995134789));
#20994=CARTESIAN_POINT('Ctrl Pts',(90.3498698986824,-1.05911566372965,-1.82573079165565));
#20995=CARTESIAN_POINT('Ctrl Pts',(90.3498698986824,-1.10880929161884,-1.78714529169387));
#20996=CARTESIAN_POINT('Ctrl Pts',(90.3498698986824,-1.1354927483652,-1.76642644778973));
#20997=CARTESIAN_POINT('Ctrl Pts',(90.3498698986825,-1.16171434281069,-1.74506547534868));
#20998=CARTESIAN_POINT('Ctrl Pts',(90.3498698986825,-1.18744825102447,-1.72308164576251));
#20999=CARTESIAN_POINT('Ctrl Pts',(90.3498698986825,-1.19640383196496,-1.7154311185435));
#21000=CARTESIAN_POINT('Ctrl Pts',(90.3498698986825,-1.20529911666185,-1.70770612424302));
#21001=CARTESIAN_POINT('Ctrl Pts',(90.3498698986825,-1.2141260236274,-1.69991389128878));
#21002=CARTESIAN_POINT('Ctrl Pts',(90.3498698986825,-1.27138360827367,-1.64936793677692));
#21003=CARTESIAN_POINT('Ctrl Pts',(90.3498698986825,-1.32585220394147,-1.59592345892405));
#21004=CARTESIAN_POINT('Ctrl Pts',(90.3498698986825,-1.37729079287515,-1.5398445336278));
#21005=CARTESIAN_POINT('Ctrl Pts',(90.3498698986825,-1.42791166624659,-1.48465709098842));
#21006=CARTESIAN_POINT('Ctrl Pts',(90.3498698986825,-1.47559858119264,-1.42691740718162));
#21007=CARTESIAN_POINT('Ctrl Pts',(90.3498698986825,-1.52007933169953,-1.3668518276762));
#21008=CARTESIAN_POINT('Ctrl Pts',(90.3498698986825,-1.55818476635096,-1.31539529898545));
#21009=CARTESIAN_POINT('Ctrl Pts',(90.3498698986825,-1.59393674881727,-1.26223114492617));
#21010=CARTESIAN_POINT('Ctrl Pts',(90.3498698986825,-1.62713471283202,-1.20749362086064));
#21011=CARTESIAN_POINT('Ctrl Pts',(90.3498698986825,-1.64205050302996,-1.18290014203907));
#21012=CARTESIAN_POINT('Ctrl Pts',(90.3498698986825,-1.65645032490888,-1.15798898503546));
#21013=CARTESIAN_POINT('Ctrl Pts',(90.3498698986825,-1.67031397481906,-1.13277214815258));
#21014=CARTESIAN_POINT('Ctrl Pts',(90.3498698986825,-1.6764049122983,-1.12169323474428));
#21015=CARTESIAN_POINT('Ctrl Pts',(90.3498698986825,-1.68239233832552,-1.11055531714204));
#21016=CARTESIAN_POINT('Ctrl Pts',(90.3498698986825,-1.68827445817782,-1.09935941317281));
#21017=CARTESIAN_POINT('Ctrl Pts',(90.3498698986825,-1.69384736498092,-1.08875205885776));
#21018=CARTESIAN_POINT('Ctrl Pts',(90.3498698986825,-1.69932144666419,-1.07810081173515));
#21019=CARTESIAN_POINT('Ctrl Pts',(90.3498698986825,-1.70469477757153,-1.06740844245854));
#21020=CARTESIAN_POINT('Ctrl Pts',(90.3498698986825,-1.73697093002357,-1.00318225821703));
#21021=CARTESIAN_POINT('Ctrl Pts',(90.3498698986825,-1.76562679489482,-0.93745261723568));
#21022=CARTESIAN_POINT('Ctrl Pts',(90.3498698986825,-1.79041933775187,-0.870427041020484));
#21023=CARTESIAN_POINT('Ctrl Pts',(90.3498698986825,-1.80872633921582,-0.82093484778445));
#21024=CARTESIAN_POINT('Ctrl Pts',(90.3498698986825,-1.82492598564089,-0.770735606075043));
#21025=CARTESIAN_POINT('Ctrl Pts',(90.3498698986825,-1.83890236465801,-0.719909707048012));
#21026=CARTESIAN_POINT('Ctrl Pts',(90.3498698986825,-1.85827904310889,-0.649445311283019));
#21027=CARTESIAN_POINT('Ctrl Pts',(90.3498698986825,-1.87338410188164,-0.577775460624741));
#21028=CARTESIAN_POINT('Ctrl Pts',(90.3498698986825,-1.88426075716109,-0.505262831297774));
#21029=CARTESIAN_POINT('Ctrl Pts',(90.3498698986825,-1.88955943874573,-0.469937510802043));
#21030=CARTESIAN_POINT('Ctrl Pts',(90.3498698986825,-1.89385383550167,-0.434412328240286));
#21031=CARTESIAN_POINT('Ctrl Pts',(90.3498698986825,-1.8971447051508,-0.398730679953565));
#21032=CARTESIAN_POINT('Ctrl Pts',(90.3498698986825,-1.89872539720831,-0.381591837015542));
#21033=CARTESIAN_POINT('Ctrl Pts',(90.3498698986825,-1.90007477485771,-0.364410850502332));
#21034=CARTESIAN_POINT('Ctrl Pts',(90.3498698986825,-1.90119093547224,-0.347226454365849));
#21035=CARTESIAN_POINT('Ctrl Pts',(90.3498698986825,-1.90580822290102,-0.276138749586064));
#21036=CARTESIAN_POINT('Ctrl Pts',(90.3498698986825,-1.90644977781024,-0.204903322611939));
#21037=CARTESIAN_POINT('Ctrl Pts',(90.3498698986825,-1.90320526373546,-0.133853409269437));
#21038=CARTESIAN_POINT('Ctrl Pts',(90.3498698986825,-1.89997246403425,-0.0630600228543288));
#21039=CARTESIAN_POINT('Ctrl Pts',(90.3498698986825,-1.89288121916131,0.00755020257709174));
#21040=CARTESIAN_POINT('Ctrl Pts',(90.3498698986825,-1.88197092147295,0.0776346496953351));
#21041=CARTESIAN_POINT('Ctrl Pts',(90.3498698986825,-1.87114890638586,0.147151996127894));
#21042=CARTESIAN_POINT('Ctrl Pts',(90.3498698986825,-1.85656900401952,0.216152960759292));
#21043=CARTESIAN_POINT('Ctrl Pts',(90.3498698986825,-1.83822688126874,0.284276007636229));
#21044=CARTESIAN_POINT('Ctrl Pts',(90.3498698986825,-1.83385334097406,0.300519432378364));
#21045=CARTESIAN_POINT('Ctrl Pts',(90.3498698986825,-1.82926572255453,0.316712786174135));
#21046=CARTESIAN_POINT('Ctrl Pts',(90.3498698986825,-1.82446364132743,0.332850848989152));
#21047=CARTESIAN_POINT('Ctrl Pts',(90.3498698986825,-1.82014892639808,0.347351049478418));
#21048=CARTESIAN_POINT('Ctrl Pts',(90.3498698986825,-1.81565974396159,0.361810316796932));
#21049=CARTESIAN_POINT('Ctrl Pts',(90.3498698986825,-1.81100440526727,0.376199140206946));
#21050=CARTESIAN_POINT('Ctrl Pts',(90.3498698986825,-1.78985030303721,0.441582705479499));
#21051=CARTESIAN_POINT('Ctrl Pts',(90.3498698986825,-1.7652408840571,0.505614703301049));
#21052=CARTESIAN_POINT('Ctrl Pts',(90.3498698986825,-1.73722113972244,0.567982945175986));
#21053=CARTESIAN_POINT('Ctrl Pts',(90.3498698986825,-1.70966066292315,0.629328918311083));
#21054=CARTESIAN_POINT('Ctrl Pts',(90.3498698986825,-1.67880028902505,0.689065998029432));
#21055=CARTESIAN_POINT('Ctrl Pts',(90.3498698986825,-1.64464358716772,0.746866444995096));
#21056=CARTESIAN_POINT('Ctrl Pts',(90.3498698986825,-1.61157576824413,0.802824269083222));
#21057=CARTESIAN_POINT('Ctrl Pts',(90.3498698986825,-1.57541798153181,0.856967478920098));
#21058=CARTESIAN_POINT('Ctrl Pts',(90.3498698986825,-1.5361431033198,0.90896063293066));
#21059=CARTESIAN_POINT('Ctrl Pts',(90.3498698986825,-1.52086991362194,0.929179697644421));
#21060=CARTESIAN_POINT('Ctrl Pts',(90.3498698986825,-1.50512503817006,0.949073159038998));
#21061=CARTESIAN_POINT('Ctrl Pts',(90.3498698986825,-1.48890580190332,0.968619417293828));
#21062=CARTESIAN_POINT('Ctrl Pts',(90.3498698986825,-1.48890580190326,0.968619417293918));
#21063=CARTESIAN_POINT('Ctrl Pts',(90.3541932148582,-1.52398815970758,0.914692843918768));
#21064=CARTESIAN_POINT('Ctrl Pts',(90.3585165310339,-1.5561759881181,0.858798217428194));
#21065=CARTESIAN_POINT('Ctrl Pts',(90.3628398472097,-1.58525053530777,0.801276982576202));
#21066=CARTESIAN_POINT('Ctrl Pts',(90.367160134058,-1.61430471009857,0.743796052583733));
#21067=CARTESIAN_POINT('Ctrl Pts',(90.3714804209064,-1.64024971073537,0.684691215118076));
#21068=CARTESIAN_POINT('Ctrl Pts',(90.3758007077547,-1.66291209690492,0.624329576800017));
#21069=CARTESIAN_POINT('Ctrl Pts',(90.3801194360565,-1.68556630760244,0.563989713986172));
#21070=CARTESIAN_POINT('Ctrl Pts',(90.3844381643583,-1.70494008238903,0.502394412118546));
#21071=CARTESIAN_POINT('Ctrl Pts',(90.3887568926601,-1.72090833927923,0.439930165252616));
#21072=CARTESIAN_POINT('Ctrl Pts',(90.3932660508206,-1.73758069994543,0.374711622010738));
#21073=CARTESIAN_POINT('Ctrl Pts',(90.3977752089812,-1.75054004309615,0.308546266800645));
#21074=CARTESIAN_POINT('Ctrl Pts',(90.4022843671418,-1.75970278433496,0.241888762251942));
#21075=CARTESIAN_POINT('Ctrl Pts',(90.4066067777444,-1.76848604907515,0.177991889677299));
#21076=CARTESIAN_POINT('Ctrl Pts',(90.410929188347,-1.77378100929878,0.113643352831989));
#21077=CARTESIAN_POINT('Ctrl Pts',(90.4152515989496,-1.77556711921805,0.0492490370638697));
#21078=CARTESIAN_POINT('Ctrl Pts',(90.419576346189,-1.7773541946842,-0.0151800894010165));
#21079=CARTESIAN_POINT('Ctrl Pts',(90.4239010934283,-1.77562865381725,-0.0796545509734151));
#21080=CARTESIAN_POINT('Ctrl Pts',(90.4282258406677,-1.7704220529785,-0.143770013658602));
#21081=CARTESIAN_POINT('Ctrl Pts',(90.4325566335551,-1.76520817373151,-0.207975104591915));
#21082=CARTESIAN_POINT('Ctrl Pts',(90.4368874264424,-1.75650359197293,-0.271819707280591));
#21083=CARTESIAN_POINT('Ctrl Pts',(90.4412182193298,-1.7443913320854,-0.334907364871723));
#21084=CARTESIAN_POINT('Ctrl Pts',(90.4417677430822,-1.74285443695412,-0.342912403955771));
#21085=CARTESIAN_POINT('Ctrl Pts',(90.4423172668345,-1.74126274301271,-0.350905274149106));
#21086=CARTESIAN_POINT('Ctrl Pts',(90.4428667905869,-1.7396164773305,-0.358885182614482));
#21087=CARTESIAN_POINT('Origin',(88.3562164250559,0.,0.));
#21088=CARTESIAN_POINT('',(90.4430005297901,-0.906280710947669,1.52765157528285));
#21089=CARTESIAN_POINT('Origin',(90.4430005297901,0.,0.));
#21090=CARTESIAN_POINT('',(90.3500036506772,0.430448222620968,1.72330449722109));
#21091=CARTESIAN_POINT('Origin',(90.3498698986825,0.,0.));
#21092=CARTESIAN_POINT('Ctrl Pts',(90.3500036506772,0.430448222620968,1.72330449722109));
#21093=CARTESIAN_POINT('Ctrl Pts',(90.3543334549293,0.368162530036945,1.73886226180115));
#21094=CARTESIAN_POINT('Ctrl Pts',(90.3586632591815,0.304931496232834,1.75106421633573));
#21095=CARTESIAN_POINT('Ctrl Pts',(90.3629930634336,0.241145549042035,1.75980478652526));
#21096=CARTESIAN_POINT('Ctrl Pts',(90.3673177204846,0.177435429551993,1.76853496606653));
#21097=CARTESIAN_POINT('Ctrl Pts',(90.3716423775356,0.113172191084751,1.77381185872338));
#21098=CARTESIAN_POINT('Ctrl Pts',(90.3759670345866,0.0487574122840727,
1.77558068733791));
#21099=CARTESIAN_POINT('Ctrl Pts',(90.3802880212225,-0.0156026965218813,
1.77734801471541));
#21100=CARTESIAN_POINT('Ctrl Pts',(90.3846090078583,-0.0801135989579022,
1.77561317440503));
#21101=CARTESIAN_POINT('Ctrl Pts',(90.3889299944942,-0.144369453052096,
1.77037327237095));
#21102=CARTESIAN_POINT('Ctrl Pts',(90.3934358724355,-0.211374759932788,
1.76490915943109));
#21103=CARTESIAN_POINT('Ctrl Pts',(90.3979417503768,-0.278102135650947,
1.75563321327166));
#21104=CARTESIAN_POINT('Ctrl Pts',(90.4024476283182,-0.34409391660832,1.74260249025793));
#21105=CARTESIAN_POINT('Ctrl Pts',(90.4067670445942,-0.407354834117631,
1.73011100295907));
#21106=CARTESIAN_POINT('Ctrl Pts',(90.4110864608703,-0.469939331470611,
1.71416954088058));
#21107=CARTESIAN_POINT('Ctrl Pts',(90.4154058771463,-0.531454112471102,
1.6948807004735));
#21108=CARTESIAN_POINT('Ctrl Pts',(90.4197258212459,-0.592976410447589,
1.67558950301097));
#21109=CARTESIAN_POINT('Ctrl Pts',(90.4240457653455,-0.653428264985323,
1.65295027247733));
#21110=CARTESIAN_POINT('Ctrl Pts',(90.4283657094451,-0.712433136210315,
1.62711495873203));
#21111=CARTESIAN_POINT('Ctrl Pts',(90.4326892060825,-0.771486530525676,
1.60125839912622));
#21112=CARTESIAN_POINT('Ctrl Pts',(90.4370127027199,-0.829090122470763,
1.57220072507932));
#21113=CARTESIAN_POINT('Ctrl Pts',(90.4413361993573,-0.884890167582664,
1.54014072532854));
#21114=CARTESIAN_POINT('Ctrl Pts',(90.4418909761683,-0.89205024510147,1.5360268920331));
#21115=CARTESIAN_POINT('Ctrl Pts',(90.4424457529792,-0.899180664056975,
1.53186368467218));
#21116=CARTESIAN_POINT('Ctrl Pts',(90.4430005297901,-0.90628071094767,1.52765157528285));
#21117=CARTESIAN_POINT('Ctrl Pts',(90.1025143645163,1.30770975493414,-1.2010560632029));
#21118=CARTESIAN_POINT('Ctrl Pts',(90.1403023877111,1.68793071858886,-0.787071505416501));
#21119=CARTESIAN_POINT('Ctrl Pts',(90.2158784341009,2.0214346950512,0.423355288987036));
#21120=CARTESIAN_POINT('Ctrl Pts',(90.3292456386917,0.830626863199002,1.8909219215733));
#21121=CARTESIAN_POINT('Ctrl Pts',(90.4048248200878,-0.422610284094226,
1.81385139676035));
#21122=CARTESIAN_POINT('Ctrl Pts',(90.442615978289,-0.906052876477412,1.52699333780199));
#21123=CARTESIAN_POINT('Ctrl Pts',(90.1849662092383,1.41289023394354,-1.29765827295793));
#21124=CARTESIAN_POINT('Ctrl Pts',(90.2227542324332,1.82369277193898,-0.850376499236438));
#21125=CARTESIAN_POINT('Ctrl Pts',(90.2983302788229,2.18402082604052,0.457406202745833));
#21126=CARTESIAN_POINT('Ctrl Pts',(90.4116974834138,0.897435060522396,2.04301077212292));
#21127=CARTESIAN_POINT('Ctrl Pts',(90.4872766648098,-0.45660127632136,1.95974138346671));
#21128=CARTESIAN_POINT('Ctrl Pts',(90.525067823011,-0.978927667841591,1.64981102736054));
#21129=CARTESIAN_POINT('Ctrl Pts',(90.2674180539604,1.51807071295294,-1.39426048271296));
#21130=CARTESIAN_POINT('Ctrl Pts',(90.3052060771553,1.95945482528912,-0.913681493056375));
#21131=CARTESIAN_POINT('Ctrl Pts',(90.3807821235449,2.34660695702982,0.491457116504633));
#21132=CARTESIAN_POINT('Ctrl Pts',(90.4941493281359,0.964243257845793,2.19509962267253));
#21133=CARTESIAN_POINT('Ctrl Pts',(90.5697285095319,-0.490592268548493,
2.10563137017308));
#21134=CARTESIAN_POINT('Ctrl Pts',(90.607519667733,-1.05180245920577,1.77262871691909));
#21135=CARTESIAN_POINT('Ctrl Pts',(90.3498698986825,1.62325119196233,-1.49086269246798));
#21136=CARTESIAN_POINT('Ctrl Pts',(90.3876579218773,2.09521687863925,-0.976986486876311));
#21137=CARTESIAN_POINT('Ctrl Pts',(90.463233968267,2.50919308801913,0.52550803026343));
#21138=CARTESIAN_POINT('Ctrl Pts',(90.5766011728579,1.03105145516918,2.34718847322216));
#21139=CARTESIAN_POINT('Ctrl Pts',(90.6521803542539,-0.524583260775627,
2.25152135687945));
#21140=CARTESIAN_POINT('Ctrl Pts',(90.6899715124551,-1.12467725056995,1.89544640647765));
#21141=CARTESIAN_POINT('',(90.4430005297901,2.20288941995875,0.0846757462792571));
#21142=CARTESIAN_POINT('Ctrl Pts',(90.4430005297901,-0.906280710947681,
1.52765157528286));
#21143=CARTESIAN_POINT('Ctrl Pts',(90.4430005297901,-0.85427776061733,1.56729260000203));
#21144=CARTESIAN_POINT('Ctrl Pts',(90.4430005297901,-0.800108744347126,
1.60369925010846));
#21145=CARTESIAN_POINT('Ctrl Pts',(90.4430005297901,-0.74412579004436,1.6369238377391));
#21146=CARTESIAN_POINT('Ctrl Pts',(90.4430005297901,-0.686154010778423,
1.67132874695323));
#21147=CARTESIAN_POINT('Ctrl Pts',(90.4430005297901,-0.626236599135055,
1.70232196502649));
#21148=CARTESIAN_POINT('Ctrl Pts',(90.4430005297901,-0.56471892524639,1.72992757470838));
#21149=CARTESIAN_POINT('Ctrl Pts',(90.4430005297901,-0.512092172819651,
1.75354344791171));
#21150=CARTESIAN_POINT('Ctrl Pts',(90.4430005297901,-0.458293231183982,
1.77467969048158));
#21151=CARTESIAN_POINT('Ctrl Pts',(90.4430005297901,-0.403518249784151,
1.7933288252926));
#21152=CARTESIAN_POINT('Ctrl Pts',(90.4430005297901,-0.378653325916346,
1.80179453911716));
#21153=CARTESIAN_POINT('Ctrl Pts',(90.4430005297901,-0.353587059186379,
1.80974744290714));
#21154=CARTESIAN_POINT('Ctrl Pts',(90.4430005297901,-0.328336895404222,
1.81718529672686));
#21155=CARTESIAN_POINT('Ctrl Pts',(90.4430005297901,-0.315371182046074,
1.82100456227533));
#21156=CARTESIAN_POINT('Ctrl Pts',(90.4430005297901,-0.302356972411376,
1.82468800737921));
#21157=CARTESIAN_POINT('Ctrl Pts',(90.4430005297901,-0.289296585325212,
1.82823522504612));
#21158=CARTESIAN_POINT('Ctrl Pts',(90.4430005297901,-0.27797522962883,1.83131011958597));
#21159=CARTESIAN_POINT('Ctrl Pts',(90.4430005297901,-0.266619082046209,
1.83428258023669));
#21160=CARTESIAN_POINT('Ctrl Pts',(90.4430005297901,-0.255244023393882,
1.83714894810173));
#21161=CARTESIAN_POINT('Ctrl Pts',(90.4430005297901,-0.186861532625867,
1.85438045257656));
#21162=CARTESIAN_POINT('Ctrl Pts',(90.4430005297901,-0.117671879173756,
1.86781631415273));
#21163=CARTESIAN_POINT('Ctrl Pts',(90.4430005297901,-0.0480425183926124,
1.87748511039214));
#21164=CARTESIAN_POINT('Ctrl Pts',(90.4430005297901,0.022546181818848,1.88728712137563));
#21165=CARTESIAN_POINT('Ctrl Pts',(90.4430005297901,0.0935877174917611,
1.89321794763905));
#21166=CARTESIAN_POINT('Ctrl Pts',(90.4430005297901,0.164729041340744,1.89526279950741));
#21167=CARTESIAN_POINT('Ctrl Pts',(90.4430005297901,0.235739474401595,1.89730388911415));
#21168=CARTESIAN_POINT('Ctrl Pts',(90.4430005297901,0.306850371500938,1.895473589152));
#21169=CARTESIAN_POINT('Ctrl Pts',(90.4430005297901,0.377725173679166,1.88970801775623));
#21170=CARTESIAN_POINT('Ctrl Pts',(90.4430005297901,0.387086066100972,1.88894652154139));
#21171=CARTESIAN_POINT('Ctrl Pts',(90.4430005297901,0.396442847540759,1.88811630351686));
#21172=CARTESIAN_POINT('Ctrl Pts',(90.4430005297901,0.405794746349183,1.88721714781832));
#21173=CARTESIAN_POINT('Ctrl Pts',(90.4430005297901,0.419068452783981,1.88594092263388));
#21174=CARTESIAN_POINT('Ctrl Pts',(90.4430005297901,0.432332323108796,1.88452581977723));
#21175=CARTESIAN_POINT('Ctrl Pts',(90.4430005297901,0.445584146956699,1.88297116443227));
#21176=CARTESIAN_POINT('Ctrl Pts',(90.4430005297901,0.458728559964045,1.88142911013296));
#21177=CARTESIAN_POINT('Ctrl Pts',(90.4430005297901,0.471853391141756,1.87975060439523));
#21178=CARTESIAN_POINT('Ctrl Pts',(90.4430005297901,0.484948310227803,1.87793672161782));
#21179=CARTESIAN_POINT('Ctrl Pts',(90.4430005297901,0.557788263474285,1.8678470726606));
#21180=CARTESIAN_POINT('Ctrl Pts',(90.4430005297901,0.629779464650554,1.85356363281225));
#21181=CARTESIAN_POINT('Ctrl Pts',(90.4430005297901,0.700551912386963,1.8350809107756));
#21182=CARTESIAN_POINT('Ctrl Pts',(90.4430005297901,0.732380673074809,1.82676860626473));
#21183=CARTESIAN_POINT('Ctrl Pts',(90.4430005297901,0.763963163282869,1.81760628974153));
#21184=CARTESIAN_POINT('Ctrl Pts',(90.4430005297901,0.795266463078774,1.80759010215849));
#21185=CARTESIAN_POINT('Ctrl Pts',(90.4430005297901,0.862738051477974,1.78600106552856));
#21186=CARTESIAN_POINT('Ctrl Pts',(90.4430005297901,0.928913182268453,1.76044866334016));
#21187=CARTESIAN_POINT('Ctrl Pts',(90.4430005297901,0.993607519094083,1.73121543301718));
#21188=CARTESIAN_POINT('Ctrl Pts',(90.4430005297901,1.05227136538682,1.70470718184011));
#21189=CARTESIAN_POINT('Ctrl Pts',(90.4430005297901,1.10971794982988,1.67517139596582));
#21190=CARTESIAN_POINT('Ctrl Pts',(90.4430005297901,1.16580106122499,1.64278422184807));
#21191=CARTESIAN_POINT('Ctrl Pts',(90.4430005297901,1.17624228698311,1.63675456714064));
#21192=CARTESIAN_POINT('Ctrl Pts',(90.4430005297901,1.18662850495695,1.63063043366676));
#21193=CARTESIAN_POINT('Ctrl Pts',(90.4430005297901,1.19695660054927,1.62441474165913));
#21194=CARTESIAN_POINT('Ctrl Pts',(90.4430005297901,1.2599916564761,1.58647875531759));
#21195=CARTESIAN_POINT('Ctrl Pts',(90.4430005297901,1.32088999312167,1.54512054404452));
#21196=CARTESIAN_POINT('Ctrl Pts',(90.4430005297901,1.37946364278683,1.50067032138885));
#21197=CARTESIAN_POINT('Ctrl Pts',(90.4430005297901,1.43980234043913,1.45488064359463));
#21198=CARTESIAN_POINT('Ctrl Pts',(90.4430005297901,1.49767496244285,1.4058094546661));
#21199=CARTESIAN_POINT('Ctrl Pts',(90.4430005297901,1.55286316604442,1.35376300242344));
#21200=CARTESIAN_POINT('Ctrl Pts',(90.4430005297901,1.60805136964599,1.30171655018078));
#21201=CARTESIAN_POINT('Ctrl Pts',(90.4430005297901,1.66055597518215,1.24669418492708));
#21202=CARTESIAN_POINT('Ctrl Pts',(90.4430005297901,1.7101335714528,1.18895618401779));
#21203=CARTESIAN_POINT('Ctrl Pts',(90.4430005297901,1.72296507476097,1.17401263278892));
#21204=CARTESIAN_POINT('Ctrl Pts',(90.4430005297901,1.73560034241774,1.15888696127209));
#21205=CARTESIAN_POINT('Ctrl Pts',(90.4430005297901,1.74803477487698,1.14358326375263));
#21206=CARTESIAN_POINT('Ctrl Pts',(90.4430005297901,1.76083174777711,1.12783336900912));
#21207=CARTESIAN_POINT('Ctrl Pts',(90.4430005297901,1.77341879728596,1.11189092493476));
#21208=CARTESIAN_POINT('Ctrl Pts',(90.4430005297901,1.78576841317895,1.09579034652114));
#21209=CARTESIAN_POINT('Ctrl Pts',(90.4430005297901,1.83344349969373,1.0336348531472));
#21210=CARTESIAN_POINT('Ctrl Pts',(90.4430005297901,1.87765235973484,0.96904318707649));
#21211=CARTESIAN_POINT('Ctrl Pts',(90.4430005297901,1.91815905619862,0.902327591878008));
#21212=CARTESIAN_POINT('Ctrl Pts',(90.4430005297901,1.95747515212669,0.837572947098043));
#21213=CARTESIAN_POINT('Ctrl Pts',(90.4430005297901,1.9933041333804,0.770816566127668));
#21214=CARTESIAN_POINT('Ctrl Pts',(90.4430005297901,2.025399552996,0.702308430193668));
#21215=CARTESIAN_POINT('Ctrl Pts',(90.4430005297901,2.03357309269835,0.684861891849661));
#21216=CARTESIAN_POINT('Ctrl Pts',(90.4430005297901,2.04150431230283,0.667301596050374));
#21217=CARTESIAN_POINT('Ctrl Pts',(90.4430005297901,2.04918873720808,0.649631385046058));
#21218=CARTESIAN_POINT('Ctrl Pts',(90.4430005297901,2.05507993245338,0.636084676693029));
#21219=CARTESIAN_POINT('Ctrl Pts',(90.4430005297901,2.06082532051455,0.622474881182825));
#21220=CARTESIAN_POINT('Ctrl Pts',(90.4430005297901,2.06641865115953,0.608814817998374));
#21221=CARTESIAN_POINT('Ctrl Pts',(90.4430005297901,2.08828602816888,0.555410188344606));
#21222=CARTESIAN_POINT('Ctrl Pts',(90.4430005297901,2.10785002137055,0.501192775045439));
#21223=CARTESIAN_POINT('Ctrl Pts',(90.4430005297901,2.12501355371717,0.446278571766083));
#21224=CARTESIAN_POINT('Ctrl Pts',(90.4430005297901,2.14793295023584,0.372948654937288));
#21225=CARTESIAN_POINT('Ctrl Pts',(90.4430005297901,2.16657429829944,0.298376904669313));
#21226=CARTESIAN_POINT('Ctrl Pts',(90.4430005297901,2.181072682182,0.222889057477663));
#21227=CARTESIAN_POINT('Ctrl Pts',(90.4430005297901,2.18985901388012,0.177141802474964));
#21228=CARTESIAN_POINT('Ctrl Pts',(90.4430005297901,2.19712286143767,0.131057562767499));
#21229=CARTESIAN_POINT('Ctrl Pts',(90.4430005297901,2.20288574446881,0.0847053108012298));
#21230=CARTESIAN_POINT('',(90.3498698986825,1.62325119196235,-1.49086269246796));
#21231=CARTESIAN_POINT('Ctrl Pts',(90.3498698986825,0.432473260079398,1.72322635770741));
#21232=CARTESIAN_POINT('Ctrl Pts',(90.3498698986825,0.500689037073845,1.71492876273113));
#21233=CARTESIAN_POINT('Ctrl Pts',(90.3498698986825,0.568201159921543,1.70262361322679));
#21234=CARTESIAN_POINT('Ctrl Pts',(90.3498698986825,0.634646799814703,1.68629351059737));
#21235=CARTESIAN_POINT('Ctrl Pts',(90.3498698986825,0.666771821708387,1.67839826110711));
#21236=CARTESIAN_POINT('Ctrl Pts',(90.3498698986825,0.698647807968656,1.66956143909893));
#21237=CARTESIAN_POINT('Ctrl Pts',(90.3498698986825,0.730234584403302,1.65977677709576));
#21238=CARTESIAN_POINT('Ctrl Pts',(90.3498698986825,0.766337183991592,1.64859324479901));
#21239=CARTESIAN_POINT('Ctrl Pts',(90.3498698986825,0.80206203264144,1.63617162624099));
#21240=CARTESIAN_POINT('Ctrl Pts',(90.3498698986825,0.83737540599978,1.62256200026643));
#21241=CARTESIAN_POINT('Ctrl Pts',(90.3498698986825,0.852643420161424,1.6166777716484));
#21242=CARTESIAN_POINT('Ctrl Pts',(90.3498698986825,0.867834507669581,1.61057139499706));
#21243=CARTESIAN_POINT('Ctrl Pts',(90.3498698986825,0.882945892123966,1.60424660726946));
#21244=CARTESIAN_POINT('Ctrl Pts',(90.3498698986825,0.894457590187188,1.59942844869149));
#21245=CARTESIAN_POINT('Ctrl Pts',(90.3498698986825,0.905920948354237,1.59448434130904));
#21246=CARTESIAN_POINT('Ctrl Pts',(90.3498698986825,0.917326683635243,1.58941980305413));
#21247=CARTESIAN_POINT('Ctrl Pts',(90.3498698986825,0.979664976032291,1.56173945989233));
#21248=CARTESIAN_POINT('Ctrl Pts',(90.3498698986825,1.04035172112798,1.53043727359164));
#21249=CARTESIAN_POINT('Ctrl Pts',(90.3498698986825,1.09919843954761,1.49582959806102));
#21250=CARTESIAN_POINT('Ctrl Pts',(90.3498698986825,1.15010544629707,1.46589125622763));
#21251=CARTESIAN_POINT('Ctrl Pts',(90.3498698986825,1.19963574840911,1.43347809868508));
#21252=CARTESIAN_POINT('Ctrl Pts',(90.3498698986825,1.24766201189903,1.39876400501926));
#21253=CARTESIAN_POINT('Ctrl Pts',(90.3498698986825,1.26296034952527,1.38770614028657));
#21254=CARTESIAN_POINT('Ctrl Pts',(90.3498698986825,1.27810601388692,1.37641460218754));
#21255=CARTESIAN_POINT('Ctrl Pts',(90.3498698986825,1.2930946896096,1.364894468081));
#21256=CARTESIAN_POINT('Ctrl Pts',(90.3498698986825,1.30640467453454,1.35466455757203));
#21257=CARTESIAN_POINT('Ctrl Pts',(90.3498698986825,1.31959368966207,1.34425192002827));
#21258=CARTESIAN_POINT('Ctrl Pts',(90.3498698986825,1.33263794396078,1.33367724437742));
#21259=CARTESIAN_POINT('Ctrl Pts',(90.3498698986825,1.387780351554,1.28897456827561));
#21260=CARTESIAN_POINT('Ctrl Pts',(90.3498698986825,1.44040951214014,1.24132658213606));
#21261=CARTESIAN_POINT('Ctrl Pts',(90.3498698986825,1.49033018857133,1.19105566693961));
#21262=CARTESIAN_POINT('Ctrl Pts',(90.3498698986825,1.54132495681077,1.13970312420791));
#21263=CARTESIAN_POINT('Ctrl Pts',(90.3498698986825,1.58949432646132,1.08561309737197));
#21264=CARTESIAN_POINT('Ctrl Pts',(90.3498698986825,1.63461237100243,1.02907775284));
#21265=CARTESIAN_POINT('Ctrl Pts',(90.3498698986825,1.67109719585865,0.983360298450885));
#21266=CARTESIAN_POINT('Ctrl Pts',(90.3498698986825,1.70558655723711,0.936042670436095));
#21267=CARTESIAN_POINT('Ctrl Pts',(90.3498698986825,1.73794656373636,0.887259053299169));
#21268=CARTESIAN_POINT('Ctrl Pts',(90.3498698986825,1.75291021222756,0.864700933634306));
#21269=CARTESIAN_POINT('Ctrl Pts',(90.3498698986825,1.76741833878176,0.841829120502182));
#21270=CARTESIAN_POINT('Ctrl Pts',(90.3498698986825,1.78145646826647,0.818655805601395));
#21271=CARTESIAN_POINT('Ctrl Pts',(90.3498698986825,1.7878902939984,0.808035226138496));
#21272=CARTESIAN_POINT('Ctrl Pts',(90.3498698986825,1.7942263747759,0.797349598647959));
#21273=CARTESIAN_POINT('Ctrl Pts',(90.3498698986825,1.80046011156049,0.786605484523132));
#21274=CARTESIAN_POINT('Ctrl Pts',(90.3498698986825,1.83793113462125,0.722022560660496));
#21275=CARTESIAN_POINT('Ctrl Pts',(90.3498698986825,1.87157440109655,0.65556035740974));
#21276=CARTESIAN_POINT('Ctrl Pts',(90.3498698986825,1.90116665684937,0.587535602342418));
#21277=CARTESIAN_POINT('Ctrl Pts',(90.3498698986825,1.926007323006,0.530433492752384));
#21278=CARTESIAN_POINT('Ctrl Pts',(90.3498698986825,1.94799336759589,0.472229235594803));
#21279=CARTESIAN_POINT('Ctrl Pts',(90.3498698986825,1.96697450572884,0.41308845846253));
#21280=CARTESIAN_POINT('Ctrl Pts',(90.3498698986825,1.9890681716311,0.344249774395821));
#21281=CARTESIAN_POINT('Ctrl Pts',(90.3498698986825,2.00709239698971,0.274142320648795));
#21282=CARTESIAN_POINT('Ctrl Pts',(90.3498698986825,2.02116104200378,0.2030743095277));
#21283=CARTESIAN_POINT('Ctrl Pts',(90.3498698986825,2.0284921104876,0.166041286374636));
#21284=CARTESIAN_POINT('Ctrl Pts',(90.3498698986825,2.03474828995425,0.128747041235049));
#21285=CARTESIAN_POINT('Ctrl Pts',(90.3498698986825,2.03994046639292,0.0912332730845004));
#21286=CARTESIAN_POINT('Ctrl Pts',(90.3498698986825,2.04159548143424,0.0792756958951614));
#21287=CARTESIAN_POINT('Ctrl Pts',(90.3498698986825,2.04314268181887,0.0672931065835392));
#21288=CARTESIAN_POINT('Ctrl Pts',(90.3498698986825,2.04458127608794,0.0552958865448529));
#21289=CARTESIAN_POINT('Ctrl Pts',(90.3498698986825,2.05337295176515,-0.0180226785820481));
#21290=CARTESIAN_POINT('Ctrl Pts',(90.3498698986825,2.05809534086584,-0.091727701576409));
#21291=CARTESIAN_POINT('Ctrl Pts',(90.3498698986825,2.05891131036719,-0.165484762986751));
#21292=CARTESIAN_POINT('Ctrl Pts',(90.3498698986825,2.05975504538824,-0.241751603424167));
#21293=CARTESIAN_POINT('Ctrl Pts',(90.3498698986825,2.05642222258532,-0.318074882014285));
#21294=CARTESIAN_POINT('Ctrl Pts',(90.3498698986825,2.04904110315175,-0.394108580285359));
#21295=CARTESIAN_POINT('Ctrl Pts',(90.3498698986825,2.04165998371819,-0.470142278556433));
#21296=CARTESIAN_POINT('Ctrl Pts',(90.3498698986825,2.03023052284998,-0.545887393004193));
#21297=CARTESIAN_POINT('Ctrl Pts',(90.3498698986825,2.01482901135003,-0.621007387284472));
#21298=CARTESIAN_POINT('Ctrl Pts',(90.3498698986825,2.0082558082846,-0.653067810489035));
#21299=CARTESIAN_POINT('Ctrl Pts',(90.3498698986825,2.00095845789534,-0.685014398435952));
#21300=CARTESIAN_POINT('Ctrl Pts',(90.3498698986825,1.99294003791299,-0.716820819516161));
#21301=CARTESIAN_POINT('Ctrl Pts',(90.3498698986825,1.98892248395689,-0.732757127806477));
#21302=CARTESIAN_POINT('Ctrl Pts',(90.3498698986825,1.98472264433956,-0.748662300766753));
#21303=CARTESIAN_POINT('Ctrl Pts',(90.3498698986825,1.98034860459118,-0.764505835419562));
#21304=CARTESIAN_POINT('Ctrl Pts',(90.3498698986825,1.95934426572363,-0.840587213242088));
#21305=CARTESIAN_POINT('Ctrl Pts',(90.3498698986825,1.93430052129626,-0.915360726877347));
#21306=CARTESIAN_POINT('Ctrl Pts',(90.3498698986825,1.9053538503144,-0.988470818961527));
#21307=CARTESIAN_POINT('Ctrl Pts',(90.3498698986825,1.87638204881937,-1.06164438273589));
#21308=CARTESIAN_POINT('Ctrl Pts',(90.3498698986825,1.8435004604713,-1.13315267365001));
#21309=CARTESIAN_POINT('Ctrl Pts',(90.3498698986825,1.80679432960359,-1.202641416107));
#21310=CARTESIAN_POINT('Ctrl Pts',(90.3498698986825,1.77047936629771,-1.27138963535113));
#21311=CARTESIAN_POINT('Ctrl Pts',(90.3498698986825,1.73042077500903,-1.33816212418568));
#21312=CARTESIAN_POINT('Ctrl Pts',(90.3498698986825,1.6866526119066,-1.4026027958059));
#21313=CARTESIAN_POINT('Ctrl Pts',(90.3498698986825,1.66632005262628,-1.43253879683743));
#21314=CARTESIAN_POINT('Ctrl Pts',(90.3498698986825,1.64518626524376,-1.46197129625266));
#21315=CARTESIAN_POINT('Ctrl Pts',(90.3498698986825,1.62325119196239,-1.49086269246791));
#21316=CARTESIAN_POINT('Ctrl Pts',(90.3498698986825,1.62325119196235,-1.49086269246796));
#21317=CARTESIAN_POINT('Ctrl Pts',(90.380913442385,2.01097952971941,-1.06870410630073));
#21318=CARTESIAN_POINT('Ctrl Pts',(90.4119569860876,2.21987663538069,-0.486345711720857));
#21319=CARTESIAN_POINT('Ctrl Pts',(90.4430005297901,2.20288941995875,0.0846757462792571));
#21320=CARTESIAN_POINT('Origin',(90.3498698986825,-2.40291074888303E-16,
0.));
#21321=CARTESIAN_POINT('',(90.3498698986825,-2.69912154532077E-16,2.204));
#21322=CARTESIAN_POINT('Origin',(90.3498698986825,0.,0.));
#21323=CARTESIAN_POINT('Origin',(90.3498698986825,0.,0.));
#21324=CARTESIAN_POINT('Origin',(66.9212607628943,0.,0.));
#21325=CARTESIAN_POINT('',(81.4430005297901,-2.69912154532077E-16,2.204));
#21326=CARTESIAN_POINT('Origin',(81.4430005297901,0.,0.));
#21327=CARTESIAN_POINT('',(66.9212607628943,-2.69912154532077E-16,2.204));
#21328=CARTESIAN_POINT('Origin',(90.4430005297901,0.,0.));
#21329=CARTESIAN_POINT('Ctrl Pts',(82.0295201802136,-1.65306427348725,3.32899555241991));
#21330=CARTESIAN_POINT('Ctrl Pts',(82.0621173237355,-2.19852390520666,3.05813912872495));
#21331=CARTESIAN_POINT('Ctrl Pts',(82.1273116107797,-3.14747075323877,2.24346380767911));
#21332=CARTESIAN_POINT('Ctrl Pts',(82.257700184868,-4.08359169347408,-0.09571649437622));
#21333=CARTESIAN_POINT('Ctrl Pts',(82.4206859024783,-2.86883663152734,-3.29923455674864));
#21334=CARTESIAN_POINT('Ctrl Pts',(82.6162687636106,1.16238339903618,-4.2168753806827));
#21335=CARTESIAN_POINT('Ctrl Pts',(82.811851624743,4.15031934985653,-1.37057296918483));
#21336=CARTESIAN_POINT('Ctrl Pts',(83.0074344858754,3.44345504116371,2.69406016453184));
#21337=CARTESIAN_POINT('Ctrl Pts',(83.2030173470079,-0.333719683741995,
4.35943641705783));
#21338=CARTESIAN_POINT('Ctrl Pts',(83.39860020814,-3.81263960805445,2.13930714802621));
#21339=CARTESIAN_POINT('Ctrl Pts',(83.5941830692725,-3.8944646466128,-1.98684861864105));
#21340=CARTESIAN_POINT('Ctrl Pts',(83.7897659304049,-0.50564373165627,-4.3426562533637));
#21341=CARTESIAN_POINT('Ctrl Pts',(83.9853487915373,3.3336643879048,-2.8285491238196));
#21342=CARTESIAN_POINT('Ctrl Pts',(84.1809316526696,4.20232603899528,1.20609443396036));
#21343=CARTESIAN_POINT('Ctrl Pts',(84.3765145138021,1.32618441591987,4.16598292634243));
#21344=CARTESIAN_POINT('Ctrl Pts',(84.5720973749343,-2.73173526363988,3.41346879580696));
#21345=CARTESIAN_POINT('Ctrl Pts',(84.7676802360668,-4.35535562891122,-0.380852351780076));
#21346=CARTESIAN_POINT('Ctrl Pts',(84.963263097199,-2.09782657360965,-3.83579056771449));
#21347=CARTESIAN_POINT('Ctrl Pts',(85.1588459583315,2.02911726294498,-3.87257613345951));
#21348=CARTESIAN_POINT('Ctrl Pts',(85.3544288194639,4.34787387083917,-0.458430425156126));
#21349=CARTESIAN_POINT('Ctrl Pts',(85.5500116805963,2.7921507497253,3.36423229852469));
#21350=CARTESIAN_POINT('Ctrl Pts',(85.7455945417287,-1.25171488096045,4.18895863102669));
#21351=CARTESIAN_POINT('Ctrl Pts',(85.9411774028608,-4.18015184799219,1.28081826434192));
#21352=CARTESIAN_POINT('Ctrl Pts',(86.1367602639934,-3.38356990681389,-2.76868550442667));
#21353=CARTESIAN_POINT('Ctrl Pts',(86.3323431251257,0.428180394291547,-4.35095693918743));
#21354=CARTESIAN_POINT('Ctrl Pts',(86.5279259862581,3.85837041772825,-2.05600160947017));
#21355=CARTESIAN_POINT('Ctrl Pts',(86.7235088473905,3.85028754068497,2.07109884112684));
#21356=CARTESIAN_POINT('Ctrl Pts',(86.9190917085228,0.4111347439794,4.3526007156551));
#21357=CARTESIAN_POINT('Ctrl Pts',(87.1146745696552,-3.39438885318226,2.7554110337347));
#21358=CARTESIAN_POINT('Ctrl Pts',(87.3102574307876,-4.17510263508425,-1.29718185414927));
#21359=CARTESIAN_POINT('Ctrl Pts',(87.50584029192,-1.23529790690718,-4.19382935913003));
#21360=CARTESIAN_POINT('Ctrl Pts',(87.7014231530522,2.80530789506251,-3.35326986418407));
#21361=CARTESIAN_POINT('Ctrl Pts',(87.8970060141848,4.34604268780248,0.475457386481673));
#21362=CARTESIAN_POINT('Ctrl Pts',(88.092588875317,2.01393751246173,3.88049411074219));
#21363=CARTESIAN_POINT('Ctrl Pts',(88.2881717364494,-2.11284414771308,3.82754458225146));
#21364=CARTESIAN_POINT('Ctrl Pts',(88.4837545975819,-4.35679539852597,0.36378874697873));
#21365=CARTESIAN_POINT('Ctrl Pts',(88.6793374587141,-2.71838192148609,-3.42414057059281));
#21366=CARTESIAN_POINT('Ctrl Pts',(88.8749203198466,1.34256965287038,-4.16076063290167));
#21367=CARTESIAN_POINT('Ctrl Pts',(89.0705031809788,4.20685975871864,-1.18961625113958));
#21368=CARTESIAN_POINT('Ctrl Pts',(89.2660860421113,3.322882630607,2.84156747674539));
#21369=CARTESIAN_POINT('Ctrl Pts',(89.4616689032436,-0.523309385250935,
4.34067852736659));
#21370=CARTESIAN_POINT('Ctrl Pts',(89.6572517643761,-3.9008702141681,1.97150514629555));
#21371=CARTESIAN_POINT('Ctrl Pts',(89.8528346255084,-3.80698675149828,-2.15407172965046));
#21372=CARTESIAN_POINT('Ctrl Pts',(90.0484174866407,-0.310961962579554,
-4.3610176492037));
#21373=CARTESIAN_POINT('Ctrl Pts',(90.211403204251,2.81536141761182,-2.95949706107794));
#21374=CARTESIAN_POINT('Ctrl Pts',(90.3418371019651,3.81133709361766,-0.644214494217));
#21375=CARTESIAN_POINT('Ctrl Pts',(90.4070767126353,3.71781142410833,0.603927146986502));
#21376=CARTESIAN_POINT('Ctrl Pts',(90.4397191797832,3.52383717212292,1.18211855844504));
#21377=CARTESIAN_POINT('Ctrl Pts',(82.1679464117515,-1.7596983336205,3.54373875243549));
#21378=CARTESIAN_POINT('Ctrl Pts',(82.2005435552736,-2.34034387801246,3.25541021913475));
#21379=CARTESIAN_POINT('Ctrl Pts',(82.2657378423178,-3.35050435026915,2.38818271450672));
#21380=CARTESIAN_POINT('Ctrl Pts',(82.3961264164059,-4.3470115551126,-0.101890869190768));
#21381=CARTESIAN_POINT('Ctrl Pts',(82.5591121340164,-3.05389640372448,-3.51205796704222));
#21382=CARTESIAN_POINT('Ctrl Pts',(82.7546949951485,1.23736515459081,-4.48889296047683));
#21383=CARTESIAN_POINT('Ctrl Pts',(82.950277856281,4.41804360608959,-1.45898438957369));
#21384=CARTESIAN_POINT('Ctrl Pts',(83.1458607174133,3.66558166855189,2.86784564776733));
#21385=CARTESIAN_POINT('Ctrl Pts',(83.3414435785458,-0.355246907694826,
4.64065016808941));
#21386=CARTESIAN_POINT('Ctrl Pts',(83.5370264396781,-4.05858118924538,2.27730723109914));
#21387=CARTESIAN_POINT('Ctrl Pts',(83.7326093008106,-4.14568450779682,-2.1150140738347));
#21388=CARTESIAN_POINT('Ctrl Pts',(83.9281921619428,-0.538261243843927,
-4.62278756796911));
#21389=CARTESIAN_POINT('Ctrl Pts',(84.1237750230752,3.54870876004771,-3.01101007358229));
#21390=CARTESIAN_POINT('Ctrl Pts',(84.3193578842077,4.47340508578664,1.28389585309453));
#21391=CARTESIAN_POINT('Ctrl Pts',(84.5149407453399,1.41173246811791,4.43471759141661));
#21392=CARTESIAN_POINT('Ctrl Pts',(84.7105236064724,-2.90795105091632,3.63366110331307));
#21393=CARTESIAN_POINT('Ctrl Pts',(84.9061064676047,-4.63630614092931,-0.405419958274843));
#21394=CARTESIAN_POINT('Ctrl Pts',(85.101689328737,-2.23315087320723,-4.08322554566206));
#21395=CARTESIAN_POINT('Ctrl Pts',(85.2972721898696,2.16000933756338,-4.12238403440385));
#21396=CARTESIAN_POINT('Ctrl Pts',(85.4928550510018,4.62834175779969,-0.488002353064227));
#21397=CARTESIAN_POINT('Ctrl Pts',(85.6884379121341,2.97226375302626,3.58124851197556));
#21398=CARTESIAN_POINT('Ctrl Pts',(85.8840207732666,-1.33245913393765,4.45917538770145));
#21399=CARTESIAN_POINT('Ctrl Pts',(86.0796036343989,-4.44980050634992,1.36343988650758));
#21400=CARTESIAN_POINT('Ctrl Pts',(86.2751864955313,-3.60183352952659,-2.94728483737715));
#21401=CARTESIAN_POINT('Ctrl Pts',(86.4707693566637,0.455800986330859,-4.63162370534514));
#21402=CARTESIAN_POINT('Ctrl Pts',(86.666352217796,4.10726195191672,-2.18862791007724));
#21403=CARTESIAN_POINT('Ctrl Pts',(86.8619350789284,4.09865767349148,2.20469901742291));
#21404=CARTESIAN_POINT('Ctrl Pts',(87.0575179400608,0.437655773872509,4.63337351674533));
#21405=CARTESIAN_POINT('Ctrl Pts',(87.2531008011932,-3.61335037264109,2.93315407166466));
#21406=CARTESIAN_POINT('Ctrl Pts',(87.4486836623255,-4.44442558434435,-1.38085904084892));
#21407=CARTESIAN_POINT('Ctrl Pts',(87.6442665234579,-1.3149831516979,-4.46436031140006));
#21408=CARTESIAN_POINT('Ctrl Pts',(87.8398493845903,2.98626962508849,-3.56957892492381));
#21409=CARTESIAN_POINT('Ctrl Pts',(88.0354322457226,4.62639245081271,0.506127670967299));
#21410=CARTESIAN_POINT('Ctrl Pts',(88.2310151068551,2.14385038835701,4.13081277589528));
#21411=CARTESIAN_POINT('Ctrl Pts',(88.4265979679873,-2.24913718453744,4.07444763719772));
#21412=CARTESIAN_POINT('Ctrl Pts',(88.6221808291198,-4.63783878562587,0.38725563313876));
#21413=CARTESIAN_POINT('Ctrl Pts',(88.817763690252,-2.89373632598811,-3.64502128126175));
#21414=CARTESIAN_POINT('Ctrl Pts',(89.0133465513846,1.42917466599261,-4.42915842398874));
#21415=CARTESIAN_POINT('Ctrl Pts',(89.2089294125167,4.47823126173771,-1.26635471369913));
#21416=CARTESIAN_POINT('Ctrl Pts',(89.4045122736493,3.53723150495561,3.02486820016417));
#21417=CARTESIAN_POINT('Ctrl Pts',(89.6000951347816,-0.557066454077677,
4.6206822649889));
#21418=CARTESIAN_POINT('Ctrl Pts',(89.795677995914,-4.15250327869021,2.09868084157544));
#21419=CARTESIAN_POINT('Ctrl Pts',(89.9912608570463,-4.05256368440808,-2.29302423018833));
#21420=CARTESIAN_POINT('Ctrl Pts',(90.1868437181788,-0.331021156374193,
-4.64233340062719));
#21421=CARTESIAN_POINT('Ctrl Pts',(90.349829435789,2.99697166926231,-3.150405056996));
#21422=CARTESIAN_POINT('Ctrl Pts',(90.4802633335032,4.05719465363349,-0.685770777428021));
#21423=CARTESIAN_POINT('Ctrl Pts',(90.5455029441732,3.95763593264129,0.642884618114954));
#21424=CARTESIAN_POINT('Ctrl Pts',(90.5781454113212,3.75114900200069,1.25837336805383));
#21425=CARTESIAN_POINT('Ctrl Pts',(82.3063726432896,-1.86633239375375,3.75848195245107));
#21426=CARTESIAN_POINT('Ctrl Pts',(82.3389697868116,-2.48216385081827,3.45268130954456));
#21427=CARTESIAN_POINT('Ctrl Pts',(82.4041640738558,-3.55353794729953,2.53290162133432));
#21428=CARTESIAN_POINT('Ctrl Pts',(82.5345526479439,-4.6104314167511,-0.108065244005317));
#21429=CARTESIAN_POINT('Ctrl Pts',(82.6975383655543,-3.23895617592162,-3.72488137733581));
#21430=CARTESIAN_POINT('Ctrl Pts',(82.8931212266866,1.31234691014545,-4.76091054027098));
#21431=CARTESIAN_POINT('Ctrl Pts',(83.088704087819,4.68576786232264,-1.54739580996254));
#21432=CARTESIAN_POINT('Ctrl Pts',(83.2842869489514,3.88770829594007,3.0416311310028));
#21433=CARTESIAN_POINT('Ctrl Pts',(83.4798698100836,-0.376774131647662,
4.921863919121));
#21434=CARTESIAN_POINT('Ctrl Pts',(83.6754526712162,-4.30452277043632,2.41530731417207));
#21435=CARTESIAN_POINT('Ctrl Pts',(83.8710355323485,-4.39690436898086,-2.24317952902834));
#21436=CARTESIAN_POINT('Ctrl Pts',(84.0666183934809,-0.570878756031578,
-4.90291888257454));
#21437=CARTESIAN_POINT('Ctrl Pts',(84.2622012546133,3.7637531321906,-3.19347102334498));
#21438=CARTESIAN_POINT('Ctrl Pts',(84.4577841157455,4.744484132578,1.3616972722287));
#21439=CARTESIAN_POINT('Ctrl Pts',(84.653366976878,1.49728052031594,4.70345225649081));
#21440=CARTESIAN_POINT('Ctrl Pts',(84.8489498380103,-3.08416683819274,3.85385341081919));
#21441=CARTESIAN_POINT('Ctrl Pts',(85.0445326991427,-4.91725665294739,-0.429987564769618));
#21442=CARTESIAN_POINT('Ctrl Pts',(85.2401155602752,-2.3684751728048,-4.33066052360962));
#21443=CARTESIAN_POINT('Ctrl Pts',(85.4356984214075,2.29090141218177,-4.37219193534821));
#21444=CARTESIAN_POINT('Ctrl Pts',(85.6312812825399,4.90880964476019,-0.517574280972326));
#21445=CARTESIAN_POINT('Ctrl Pts',(85.8268641436722,3.15237675632724,3.79826472542643));
#21446=CARTESIAN_POINT('Ctrl Pts',(86.0224470048046,-1.41320338691484,4.72939214437619));
#21447=CARTESIAN_POINT('Ctrl Pts',(86.2180298659369,-4.71944916470767,1.44606150867324));
#21448=CARTESIAN_POINT('Ctrl Pts',(86.4136127270693,-3.8200971522393,-3.12588417032763));
#21449=CARTESIAN_POINT('Ctrl Pts',(86.6091955882017,0.483421578370174,-4.91229047150286));
#21450=CARTESIAN_POINT('Ctrl Pts',(86.804778449334,4.3561534861052,-2.32125421068431));
#21451=CARTESIAN_POINT('Ctrl Pts',(87.0003613104665,4.347027806298,2.33829919371898));
#21452=CARTESIAN_POINT('Ctrl Pts',(87.1959441715988,0.46417680376561,4.91414631783558));
#21453=CARTESIAN_POINT('Ctrl Pts',(87.3915270327312,-3.83231189209993,3.11089710959462));
#21454=CARTESIAN_POINT('Ctrl Pts',(87.5871098938635,-4.71374853360445,-1.46453622754857));
#21455=CARTESIAN_POINT('Ctrl Pts',(87.782692754996,-1.39466839648862,-4.73489126367011));
#21456=CARTESIAN_POINT('Ctrl Pts',(87.9782756161282,3.16723135511446,-3.78588798566355));
#21457=CARTESIAN_POINT('Ctrl Pts',(88.1738584772607,4.90674221382295,0.536797955452923));
#21458=CARTESIAN_POINT('Ctrl Pts',(88.369441338393,2.27376326425229,4.3811314410484));
#21459=CARTESIAN_POINT('Ctrl Pts',(88.5650241995254,-2.38543022136179,4.32135069214399));
#21460=CARTESIAN_POINT('Ctrl Pts',(88.7606070606577,-4.91888217272578,0.410722519298791));
#21461=CARTESIAN_POINT('Ctrl Pts',(88.9561899217902,-3.06909073049012,-3.86590199193068));
#21462=CARTESIAN_POINT('Ctrl Pts',(89.1517727829225,1.51577967911484,-4.6975562150758));
#21463=CARTESIAN_POINT('Ctrl Pts',(89.3473556440549,4.7496027647568,-1.34309317625867));
#21464=CARTESIAN_POINT('Ctrl Pts',(89.5429385051872,3.75158037930423,3.20816892358296));
#21465=CARTESIAN_POINT('Ctrl Pts',(89.7385213663196,-0.590823522904417,
4.90068600261121));
#21466=CARTESIAN_POINT('Ctrl Pts',(89.934104227452,-4.40413634321233,2.22585653685535));
#21467=CARTESIAN_POINT('Ctrl Pts',(90.1296870885844,-4.2981406173179,-2.43197673072621));
#21468=CARTESIAN_POINT('Ctrl Pts',(90.3252699497168,-0.351080350168827,
-4.92364915205066));
#21469=CARTESIAN_POINT('Ctrl Pts',(90.4882556673271,3.17858192091281,-3.34131305291405));
#21470=CARTESIAN_POINT('Ctrl Pts',(90.6186895650412,4.30305221364934,-0.727327060639044));
#21471=CARTESIAN_POINT('Ctrl Pts',(90.6839291757112,4.19746044117425,0.681842089243407));
#21472=CARTESIAN_POINT('Ctrl Pts',(90.7165716428592,3.97846083187846,1.33462817766261));
#21473=CARTESIAN_POINT('Ctrl Pts',(82.4447988748275,-1.972966453887,3.97322515246666));
#21474=CARTESIAN_POINT('Ctrl Pts',(82.4773960183496,-2.62398382362407,3.64995239995436));
#21475=CARTESIAN_POINT('Ctrl Pts',(82.5425903053937,-3.7565715443299,2.67762052816192));
#21476=CARTESIAN_POINT('Ctrl Pts',(82.6729788794819,-4.87385127838962,-0.114239618819863));
#21477=CARTESIAN_POINT('Ctrl Pts',(82.8359645970922,-3.42401594811876,-3.93770478762939));
#21478=CARTESIAN_POINT('Ctrl Pts',(83.0315474582246,1.38732866570007,-5.03292812006512));
#21479=CARTESIAN_POINT('Ctrl Pts',(83.2271303193571,4.95349211855569,-1.6358072303514));
#21480=CARTESIAN_POINT('Ctrl Pts',(83.4227131804892,4.10983492332825,3.21541661423828));
#21481=CARTESIAN_POINT('Ctrl Pts',(83.6182960416218,-0.398301355600491,
5.20307767015258));
#21482=CARTESIAN_POINT('Ctrl Pts',(83.813878902754,-4.55046435162727,2.55330739724501));
#21483=CARTESIAN_POINT('Ctrl Pts',(84.0094617638865,-4.6481242301649,-2.37134498422198));
#21484=CARTESIAN_POINT('Ctrl Pts',(84.2050446250188,-0.603496268219234,
-5.18305019717995));
#21485=CARTESIAN_POINT('Ctrl Pts',(84.4006274861513,3.9787975043335,-3.37593197310767));
#21486=CARTESIAN_POINT('Ctrl Pts',(84.5962103472836,5.01556317936936,1.43949869136288));
#21487=CARTESIAN_POINT('Ctrl Pts',(84.7917932084159,1.58282857251398,4.97218692156499));
#21488=CARTESIAN_POINT('Ctrl Pts',(84.9873760695484,-3.26038262546918,4.0740457183253));
#21489=CARTESIAN_POINT('Ctrl Pts',(85.1829589306806,-5.19820716496546,-0.454555171264389));
#21490=CARTESIAN_POINT('Ctrl Pts',(85.3785417918131,-2.50379947240239,-4.5780955015572));
#21491=CARTESIAN_POINT('Ctrl Pts',(85.5741246529455,2.42179348680017,-4.62199983629255));
#21492=CARTESIAN_POINT('Ctrl Pts',(85.7697075140778,5.1892775317207,-0.547146208880429));
#21493=CARTESIAN_POINT('Ctrl Pts',(85.9652903752102,3.33248975962821,4.0152809388773));
#21494=CARTESIAN_POINT('Ctrl Pts',(86.1608732363425,-1.49394763989204,4.99960890105093));
#21495=CARTESIAN_POINT('Ctrl Pts',(86.3564560974749,-4.9890978230654,1.52868313083891));
#21496=CARTESIAN_POINT('Ctrl Pts',(86.5520389586073,-4.038360774952,-3.30448350327812));
#21497=CARTESIAN_POINT('Ctrl Pts',(86.7476218197397,0.511042170409484,-5.19295723766057));
#21498=CARTESIAN_POINT('Ctrl Pts',(86.9432046808719,4.60504502029368,-2.45388051129137));
#21499=CARTESIAN_POINT('Ctrl Pts',(87.1387875420045,4.5953979391045,2.47189937001505));
#21500=CARTESIAN_POINT('Ctrl Pts',(87.3343704031367,0.490697833658717,5.19491911892581));
#21501=CARTESIAN_POINT('Ctrl Pts',(87.5299532642692,-4.05127341155876,3.28864014752458));
#21502=CARTESIAN_POINT('Ctrl Pts',(87.7255361254015,-4.98307148286454,-1.54821341424822));
#21503=CARTESIAN_POINT('Ctrl Pts',(87.9211189865339,-1.47435364127935,-5.00542221594014));
#21504=CARTESIAN_POINT('Ctrl Pts',(88.1167018476662,3.34819308514044,-4.00219704640328));
#21505=CARTESIAN_POINT('Ctrl Pts',(88.3122847087986,5.18709197683317,0.567468239938547));
#21506=CARTESIAN_POINT('Ctrl Pts',(88.507867569931,2.40367614014758,4.6314501062015));
#21507=CARTESIAN_POINT('Ctrl Pts',(88.7034504310633,-2.52172325818615,4.56825374709024));
#21508=CARTESIAN_POINT('Ctrl Pts',(88.8990332921958,-5.19992555982569,0.434189405458823));
#21509=CARTESIAN_POINT('Ctrl Pts',(89.0946161533281,-3.24444513499214,-4.08678270259963));
#21510=CARTESIAN_POINT('Ctrl Pts',(89.2901990144604,1.60238469223707,-4.96595400616287));
#21511=CARTESIAN_POINT('Ctrl Pts',(89.4857818755929,5.02097426777587,-1.41983163881822));
#21512=CARTESIAN_POINT('Ctrl Pts',(89.6813647367252,3.96592925365284,3.39146964700175));
#21513=CARTESIAN_POINT('Ctrl Pts',(89.8769475978576,-0.624580591731157,
5.18068974023352));
#21514=CARTESIAN_POINT('Ctrl Pts',(90.0725304589899,-4.65576940773444,2.35303223213525));
#21515=CARTESIAN_POINT('Ctrl Pts',(90.2681133201223,-4.54371755022769,-2.57092923126409));
#21516=CARTESIAN_POINT('Ctrl Pts',(90.4636961812547,-0.371139543963468,
-5.20496490347415));
#21517=CARTESIAN_POINT('Ctrl Pts',(90.626681898865,3.36019217256331,-3.53222104883211));
#21518=CARTESIAN_POINT('Ctrl Pts',(90.7571157965791,4.54890977366517,-0.768883343850067));
#21519=CARTESIAN_POINT('Ctrl Pts',(90.8223554072492,4.43728494970721,0.720799560371859));
#21520=CARTESIAN_POINT('Ctrl Pts',(90.8549978743971,4.20577266175623,1.4108829872714));
#21521=CARTESIAN_POINT('Ctrl Pts',(90.4430005297901,-0.735206482746314,
-4.37679204773777));
#21522=CARTESIAN_POINT('Ctrl Pts',(90.4430005297901,-0.604538703831446,
-4.38932243272125));
#21523=CARTESIAN_POINT('Ctrl Pts',(90.4430005297901,-0.4737103423462,-4.39569211060463));
#21524=CARTESIAN_POINT('Ctrl Pts',(90.4430005297901,-0.343055129970595,
-4.39568396726793));
#21525=CARTESIAN_POINT('Ctrl Pts',(90.4430005297901,-0.334607555765649,
-4.39568344075667));
#21526=CARTESIAN_POINT('Ctrl Pts',(90.4430005297901,-0.326160705233621,
-4.3956562347694));
#21527=CARTESIAN_POINT('Ctrl Pts',(90.4430005297901,-0.317714668695277,
-4.39560228305826));
#21528=CARTESIAN_POINT('Ctrl Pts',(90.4430005297901,-0.185997485435185,
-4.39476089818014));
#21529=CARTESIAN_POINT('Ctrl Pts',(90.4430005297901,-0.0544775308838946,
-4.38741913239467));
#21530=CARTESIAN_POINT('Ctrl Pts',(90.4430005297901,0.0764804063569064,
-4.37382331815595));
#21531=CARTESIAN_POINT('Ctrl Pts',(90.4430005297901,0.212139516582048,-4.35973943671073));
#21532=CARTESIAN_POINT('Ctrl Pts',(90.4430005297901,0.347196453092427,-4.33894421155611));
#21533=CARTESIAN_POINT('Ctrl Pts',(90.4430005297901,0.481228112669947,-4.3116562756427));
#21534=CARTESIAN_POINT('Ctrl Pts',(90.4430005297901,0.615259772247468,-4.2843683397293));
#21535=CARTESIAN_POINT('Ctrl Pts',(90.4430005297901,0.748267008611165,-4.25058714871171));
#21536=CARTESIAN_POINT('Ctrl Pts',(90.4430005297901,0.8797960890982,-4.2104833822017));
#21537=CARTESIAN_POINT('Ctrl Pts',(90.4430005297901,0.896953403142723,-4.20525204542178));
#21538=CARTESIAN_POINT('Ctrl Pts',(90.4430005297901,0.91408551176748,-4.19991306416615));
#21539=CARTESIAN_POINT('Ctrl Pts',(90.4430005297901,0.931191357547314,-4.19446676463672));
#21540=CARTESIAN_POINT('Ctrl Pts',(90.4430005297901,0.947772132258863,-4.18918764154211));
#21541=CARTESIAN_POINT('Ctrl Pts',(90.4430005297901,0.964318662466662,-4.18381073214009));
#21542=CARTESIAN_POINT('Ctrl Pts',(90.4430005297901,0.980829620677612,-4.17833682356824));
#21543=CARTESIAN_POINT('Ctrl Pts',(90.4430005297901,1.10554259859417,-4.13699049889609));
#21544=CARTESIAN_POINT('Ctrl Pts',(90.4430005297901,1.22823748709574,-4.09011104027403));
#21545=CARTESIAN_POINT('Ctrl Pts',(90.4430005297901,1.3485575220433,-4.03793699452255));
#21546=CARTESIAN_POINT('Ctrl Pts',(90.4430005297901,1.4690034609849,-3.98570835336851));
#21547=CARTESIAN_POINT('Ctrl Pts',(90.4430005297901,1.58707030875767,-3.92817353589151));
#21548=CARTESIAN_POINT('Ctrl Pts',(90.4430005297901,1.70237501425449,-3.86552606398859));
#21549=CARTESIAN_POINT('Ctrl Pts',(90.4430005297901,1.81579371193992,-3.80390329980132));
#21550=CARTESIAN_POINT('Ctrl Pts',(90.4430005297901,1.92654047357856,-3.73733320225429));
#21551=CARTESIAN_POINT('Ctrl Pts',(90.4430005297901,2.03421675054925,-3.66596377326627));
#21552=CARTESIAN_POINT('Ctrl Pts',(90.4430005297901,2.12284103122993,-3.60722228921239));
#21553=CARTESIAN_POINT('Ctrl Pts',(90.4430005297901,2.20938482207715,-3.54522882338617));
#21554=CARTESIAN_POINT('Ctrl Pts',(90.4430005297901,2.29360397058158,-3.48005089866155));
#21555=CARTESIAN_POINT('Ctrl Pts',(90.4430005297901,2.31916577926078,-3.46026839466449));
#21556=CARTESIAN_POINT('Ctrl Pts',(90.4430005297901,2.34451328416945,-3.44019244944633));
#21557=CARTESIAN_POINT('Ctrl Pts',(90.4430005297901,2.36963923936791,-3.41982474290588));
#21558=CARTESIAN_POINT('Ctrl Pts',(90.4430005297901,2.38341896005213,-3.40865456828412));
#21559=CARTESIAN_POINT('Ctrl Pts',(90.4430005297901,2.39712536031612,-3.39740203463942));
#21560=CARTESIAN_POINT('Ctrl Pts',(90.4430005297901,2.4107546065151,-3.38607005694199));
#21561=CARTESIAN_POINT('Ctrl Pts',(90.4430005297901,2.46077454371223,-3.34448119689286));
#21562=CARTESIAN_POINT('Ctrl Pts',(90.4430005297901,2.50976810825464,-3.30181224193952));
#21563=CARTESIAN_POINT('Ctrl Pts',(90.4430005297901,2.55768970288188,-3.25808790138363));
#21564=CARTESIAN_POINT('Ctrl Pts',(90.4430005297901,2.65095689235614,-3.17298959889633));
#21565=CARTESIAN_POINT('Ctrl Pts',(90.4430005297901,2.74016608735159,-3.08389558277388));
#21566=CARTESIAN_POINT('Ctrl Pts',(90.4430005297901,2.82495239396308,-2.99096257965398));
#21567=CARTESIAN_POINT('Ctrl Pts',(90.4430005297901,2.90759162314816,-2.90038295600232));
#21568=CARTESIAN_POINT('Ctrl Pts',(90.4430005297901,2.98602952066637,-2.80615579142114));
#21569=CARTESIAN_POINT('Ctrl Pts',(90.4430005297901,3.05988679011808,-2.70840035946947));
#21570=CARTESIAN_POINT('Ctrl Pts',(90.4430005297901,3.11277433976829,-2.63839986663643));
#21571=CARTESIAN_POINT('Ctrl Pts',(90.4430005297901,3.16331226028424,-2.56658964974082));
#21572=CARTESIAN_POINT('Ctrl Pts',(90.4430005297901,3.2113460253676,-2.49300717327591));
#21573=CARTESIAN_POINT('Ctrl Pts',(90.4430005297901,3.25596252339907,-2.42465957631677));
#21574=CARTESIAN_POINT('Ctrl Pts',(90.4430005297901,3.29841825709039,-2.354782644304));
#21575=CARTESIAN_POINT('Ctrl Pts',(90.4430005297901,3.33867108373867,-2.28349579149761));
#21576=CARTESIAN_POINT('Ctrl Pts',(90.4430005297901,3.35066966420012,-2.26224657472299));
#21577=CARTESIAN_POINT('Ctrl Pts',(90.4430005297901,3.36247245082681,-2.24087208124526));
#21578=CARTESIAN_POINT('Ctrl Pts',(90.4430005297901,3.37407817045466,-2.21937547389451));
#21579=CARTESIAN_POINT('Ctrl Pts',(90.4430005297901,3.38225827070718,-2.20422394440242));
#21580=CARTESIAN_POINT('Ctrl Pts',(90.4430005297901,3.39034041097382,-2.18901172139937));
#21581=CARTESIAN_POINT('Ctrl Pts',(90.4430005297901,3.39831759446147,-2.17375281910387));
#21582=CARTESIAN_POINT('Ctrl Pts',(90.4430005297901,3.4551234429507,-2.06509355443337));
#21583=CARTESIAN_POINT('Ctrl Pts',(90.4430005297901,3.50669909621418,-1.95390743199697));
#21584=CARTESIAN_POINT('Ctrl Pts',(90.4430005297901,3.55299874508288,-1.84063291121359));
#21585=CARTESIAN_POINT('Ctrl Pts',(90.4430005297901,3.59985305587428,-1.72600138092743));
#21586=CARTESIAN_POINT('Ctrl Pts',(90.4430005297901,3.64130438566013,-1.6092302210154));
#21587=CARTESIAN_POINT('Ctrl Pts',(90.4430005297901,3.67725474073973,-1.49075882570099));
#21588=CARTESIAN_POINT('Ctrl Pts',(90.4430005297901,3.71297351100698,-1.37305059881123));
#21589=CARTESIAN_POINT('Ctrl Pts',(90.4430005297901,3.74326199392705,-1.25366307552021));
#21590=CARTESIAN_POINT('Ctrl Pts',(90.4430005297901,3.76797297501044,-1.1330259641585));
#21591=CARTESIAN_POINT('Ctrl Pts',(90.4430005297901,3.78309861206878,-1.05918376598491));
#21592=CARTESIAN_POINT('Ctrl Pts',(90.4430005297901,3.79613353366921,-0.98487341865883));
#21593=CARTESIAN_POINT('Ctrl Pts',(90.4430005297901,3.80703431601147,-0.910195398393028));
#21594=CARTESIAN_POINT('Ctrl Pts',(90.4430005297901,3.81275326778124,-0.87101655941134));
#21595=CARTESIAN_POINT('Ctrl Pts',(90.4430005297901,3.81788468776157,-0.831736555533261));
#21596=CARTESIAN_POINT('Ctrl Pts',(90.4430005297901,3.82242148213659,-0.79237018659198));
#21597=CARTESIAN_POINT('Ctrl Pts',(90.4430005297901,3.82477895958205,-0.771914040860599));
#21598=CARTESIAN_POINT('Ctrl Pts',(90.4430005297901,3.82697612959026,-0.751431871386733));
#21599=CARTESIAN_POINT('Ctrl Pts',(90.4430005297901,3.82901104070976,-0.730934968196635));
#21600=CARTESIAN_POINT('Ctrl Pts',(90.4430005297901,3.83052437597813,-0.715691704649236));
#21601=CARTESIAN_POINT('Ctrl Pts',(90.4430005297901,3.83194777392774,-0.70044244785746));
#21602=CARTESIAN_POINT('Ctrl Pts',(90.4430005297901,3.83328081539605,-0.685190377817854));
#21603=CARTESIAN_POINT('Ctrl Pts',(90.4430005297901,3.83425091868926,-0.674090885622495));
#21604=CARTESIAN_POINT('Ctrl Pts',(90.4430005297901,3.83517321726714,-0.66298940552743));
#21605=CARTESIAN_POINT('Ctrl Pts',(90.4430005297901,3.83604763234583,-0.6518862628284));
#21606=CARTESIAN_POINT('Ctrl Pts',(90.4430005297901,3.84560195174611,-0.530567481532555));
#21607=CARTESIAN_POINT('Ctrl Pts',(90.4430005297901,3.84944379015736,-0.40904962007089));
#21608=CARTESIAN_POINT('Ctrl Pts',(90.4430005297901,3.84760828244277,-0.287700071444294));
#21609=CARTESIAN_POINT('Ctrl Pts',(90.4430005297901,3.84578233258688,-0.166982414381175));
#21610=CARTESIAN_POINT('Ctrl Pts',(90.4430005297901,3.8383377921992,-0.0464305630719454));
#21611=CARTESIAN_POINT('Ctrl Pts',(90.4430005297901,3.82525995553925,0.0735799560127684));
#21612=CARTESIAN_POINT('Ctrl Pts',(90.4430005297901,3.82045107314999,0.117709309112766));
#21613=CARTESIAN_POINT('Ctrl Pts',(90.4430005297901,3.81488003310189,0.16176527531321));
#21614=CARTESIAN_POINT('Ctrl Pts',(90.4430005297901,3.80854450228284,0.205728399455385));
#21615=CARTESIAN_POINT('Ctrl Pts',(90.4430005297901,3.8042331526489,0.235645450542403));
#21616=CARTESIAN_POINT('Ctrl Pts',(90.4430005297901,3.79956659035794,0.265525695687981));
#21617=CARTESIAN_POINT('Ctrl Pts',(90.4430005297901,3.79455002103167,0.29532852943585));
#21618=CARTESIAN_POINT('Ctrl Pts',(90.4430005297901,3.77482815798568,0.412493740824486));
#21619=CARTESIAN_POINT('Ctrl Pts',(90.4430005297901,3.74969110993674,0.528545803738649));
#21620=CARTESIAN_POINT('Ctrl Pts',(90.4430005297901,3.71914658870853,0.643128875915091));
#21621=CARTESIAN_POINT('Ctrl Pts',(90.4430005297901,3.68911896823763,0.75577287442469));
#21622=CARTESIAN_POINT('Ctrl Pts',(90.4430005297901,3.65386504700212,0.86699780500097));
#21623=CARTESIAN_POINT('Ctrl Pts',(90.4430005297901,3.61334804287102,0.97644236203363));
#21624=CARTESIAN_POINT('Ctrl Pts',(90.4430005297901,3.58775745478563,1.04556767465913));
#21625=CARTESIAN_POINT('Ctrl Pts',(90.4430005297901,3.56006645271635,1.11398226507298));
#21626=CARTESIAN_POINT('Ctrl Pts',(90.4430005297901,3.5302572329849,1.18158852036477));
#21627=CARTESIAN_POINT('Ctrl Pts',(82.4430005297901,-2.16672251220859,-3.03255290461516));
#21628=CARTESIAN_POINT('Ctrl Pts',(82.4430005297901,-2.2696406448299,-2.9735626011528));
#21629=CARTESIAN_POINT('Ctrl Pts',(82.4430005297901,-2.36930641006409,-2.90958285743481));
#21630=CARTESIAN_POINT('Ctrl Pts',(82.4430005297901,-2.4652895168029,-2.84070661811296));
#21631=CARTESIAN_POINT('Ctrl Pts',(82.4430005297901,-2.55923374195207,-2.77329345392055));
#21632=CARTESIAN_POINT('Ctrl Pts',(82.4430005297901,-2.64965127392472,-2.70118974547307));
#21633=CARTESIAN_POINT('Ctrl Pts',(82.4430005297901,-2.73645513109191,-2.62479035097945));
#21634=CARTESIAN_POINT('Ctrl Pts',(82.4430005297901,-2.79259033985632,-2.57538360686307));
#21635=CARTESIAN_POINT('Ctrl Pts',(82.4430005297901,-2.84721383859095,-2.52417932868561));
#21636=CARTESIAN_POINT('Ctrl Pts',(82.4430005297901,-2.90029628102234,-2.47127435007986));
#21637=CARTESIAN_POINT('Ctrl Pts',(82.4430005297901,-2.91981754671394,-2.45181834737037));
#21638=CARTESIAN_POINT('Ctrl Pts',(82.4430005297901,-2.93913346768778,-2.43212884764077));
#21639=CARTESIAN_POINT('Ctrl Pts',(82.4430005297901,-2.95822228666816,-2.41223190685226));
#21640=CARTESIAN_POINT('Ctrl Pts',(82.4430005297901,-3.03989891485165,-2.32709751292032));
#21641=CARTESIAN_POINT('Ctrl Pts',(82.4430005297901,-3.11748745097799,-2.23810423358288));
#21642=CARTESIAN_POINT('Ctrl Pts',(82.4430005297901,-3.19090385621255,-2.14566782445364));
#21643=CARTESIAN_POINT('Ctrl Pts',(82.4430005297901,-3.2660819932855,-2.0510132712397));
#21644=CARTESIAN_POINT('Ctrl Pts',(82.4430005297901,-3.33688589309288,-1.95274786922678));
#21645=CARTESIAN_POINT('Ctrl Pts',(82.4430005297901,-3.40319502447745,-1.85127235969848));
#21646=CARTESIAN_POINT('Ctrl Pts',(82.4430005297901,-3.44327359760755,-1.78993852008059));
#21647=CARTESIAN_POINT('Ctrl Pts',(82.4430005297901,-3.48170950646411,-1.72743110356979));
#21648=CARTESIAN_POINT('Ctrl Pts',(82.4430005297901,-3.51846970607509,-1.66383203062367));
#21649=CARTESIAN_POINT('Ctrl Pts',(82.4430005297901,-3.52766288301639,-1.64792685227634));
#21650=CARTESIAN_POINT('Ctrl Pts',(82.4430005297901,-3.53674997798665,-1.63195544603767));
#21651=CARTESIAN_POINT('Ctrl Pts',(82.4430005297901,-3.54572521930434,-1.61592885171508));
#21652=CARTESIAN_POINT('Ctrl Pts',(82.4430005297901,-3.60610285231906,-1.50811583630591));
#21653=CARTESIAN_POINT('Ctrl Pts',(82.4430005297901,-3.66149200213407,-1.39768708900077));
#21654=CARTESIAN_POINT('Ctrl Pts',(82.4430005297901,-3.71180063322066,-1.28507982535995));
#21655=CARTESIAN_POINT('Ctrl Pts',(82.4430005297901,-3.76266962345599,-1.17121829363366));
#21656=CARTESIAN_POINT('Ctrl Pts',(82.4430005297901,-3.8083447828333,-1.05512876825121));
#21657=CARTESIAN_POINT('Ctrl Pts',(82.4430005297901,-3.84869498052848,-0.937223070177858));
#21658=CARTESIAN_POINT('Ctrl Pts',(82.4430005297901,-3.88901078279322,-0.819417877615471));
#21659=CARTESIAN_POINT('Ctrl Pts',(82.4430005297901,-3.92401114105584,-0.699798835821216));
#21660=CARTESIAN_POINT('Ctrl Pts',(82.4430005297901,-3.95352257290869,-0.578747854386884));
#21661=CARTESIAN_POINT('Ctrl Pts',(82.4430005297901,-3.97523656822446,-0.489680659784435));
#21662=CARTESIAN_POINT('Ctrl Pts',(82.4430005297901,-3.99397814296339,-0.399837595278188));
#21663=CARTESIAN_POINT('Ctrl Pts',(82.4430005297901,-4.00966125689264,-0.309364507448106));
#21664=CARTESIAN_POINT('Ctrl Pts',(82.4430005297901,-4.01435795168095,-0.282270112673519));
#21665=CARTESIAN_POINT('Ctrl Pts',(82.4430005297901,-4.01878024374387,-0.255119189321616));
#21666=CARTESIAN_POINT('Ctrl Pts',(82.4430005297901,-4.02292554754272,-0.227915601567328));
#21667=CARTESIAN_POINT('Ctrl Pts',(82.4430005297901,-4.02569591908626,-0.20973501721123));
#21668=CARTESIAN_POINT('Ctrl Pts',(82.4430005297901,-4.02834281759651,-0.191528743140453));
#21669=CARTESIAN_POINT('Ctrl Pts',(82.4430005297901,-4.03086308406066,-0.173316124913731));
#21670=CARTESIAN_POINT('Ctrl Pts',(82.4430005297901,-4.04843750869992,-0.046315154555558));
#21671=CARTESIAN_POINT('Ctrl Pts',(82.4430005297901,-4.05988667809022,0.0811706755403835));
#21672=CARTESIAN_POINT('Ctrl Pts',(82.4430005297901,-4.06508069808529,0.20871668428979));
#21673=CARTESIAN_POINT('Ctrl Pts',(82.4430005297901,-4.0692831193649,0.311912679262398));
#21674=CARTESIAN_POINT('Ctrl Pts',(82.4430005297901,-4.06939010281968,0.415148898919295));
#21675=CARTESIAN_POINT('Ctrl Pts',(82.4430005297901,-4.06531043519685,0.518211439887901));
#21676=CARTESIAN_POINT('Ctrl Pts',(82.4430005297901,-4.06037373247765,0.642924816879996));
#21677=CARTESIAN_POINT('Ctrl Pts',(82.4430005297901,-4.04930850365814,0.767384162347737));
#21678=CARTESIAN_POINT('Ctrl Pts',(82.4430005297901,-4.03236186892168,0.891221661938483));
#21679=CARTESIAN_POINT('Ctrl Pts',(82.4430005297901,-4.01541523418522,1.01505916152923));
#21680=CARTESIAN_POINT('Ctrl Pts',(82.4430005297901,-3.9925869512816,1.13827557220802));
#21681=CARTESIAN_POINT('Ctrl Pts',(82.4430005297901,-3.96407180720897,1.26050316969768));
#21682=CARTESIAN_POINT('Ctrl Pts',(82.4430005297901,-3.95547258916304,1.29736294355562));
#21683=CARTESIAN_POINT('Ctrl Pts',(82.4430005297901,-3.9463558470242,1.33413274985256));
#21684=CARTESIAN_POINT('Ctrl Pts',(82.4430005297901,-3.93672603994556,1.37080234332704));
#21685=CARTESIAN_POINT('Ctrl Pts',(82.4430005297901,-3.93229805917785,1.38766376675315));
#21686=CARTESIAN_POINT('Ctrl Pts',(82.4430005297901,-3.92776385858573,1.40449532876003));
#21687=CARTESIAN_POINT('Ctrl Pts',(82.4430005297901,-3.92312493683007,1.42129347051884));
#21688=CARTESIAN_POINT('Ctrl Pts',(82.4430005297901,-3.88922045173003,1.54406604073413));
#21689=CARTESIAN_POINT('Ctrl Pts',(82.4430005297901,-3.84971460163609,1.66509780758731));
#21690=CARTESIAN_POINT('Ctrl Pts',(82.4430005297901,-3.80489648217205,1.78401656479781));
#21691=CARTESIAN_POINT('Ctrl Pts',(82.4430005297901,-3.75909623686104,1.90554125877099));
#21692=CARTESIAN_POINT('Ctrl Pts',(82.4430005297901,-3.70774825327871,2.02486010777613));
#21693=CARTESIAN_POINT('Ctrl Pts',(82.4430005297901,-3.65110614357196,2.14157776463153));
#21694=CARTESIAN_POINT('Ctrl Pts',(82.4430005297901,-3.59646760585506,2.2541668283041));
#21695=CARTESIAN_POINT('Ctrl Pts',(82.4430005297901,-3.53690231335205,2.36433614459377));
#21696=CARTESIAN_POINT('Ctrl Pts',(82.4430005297901,-3.47259286055702,2.47172179522677));
#21697=CARTESIAN_POINT('Ctrl Pts',(82.4430005297901,-3.40566020000047,2.58348774859871));
#21698=CARTESIAN_POINT('Ctrl Pts',(82.4430005297901,-3.33358842352915,2.69223917331593));
#21699=CARTESIAN_POINT('Ctrl Pts',(82.4430005297901,-3.25661397611833,2.79770775568242));
#21700=CARTESIAN_POINT('Ctrl Pts',(82.4430005297901,-3.2459176943,2.81236355014302));
#21701=CARTESIAN_POINT('Ctrl Pts',(82.4430005297901,-3.23512667474306,2.82695590898395));
#21702=CARTESIAN_POINT('Ctrl Pts',(82.4430005297901,-3.22424148623506,2.84148406610821));
#21703=CARTESIAN_POINT('Ctrl Pts',(82.4430005297901,-3.20381603969898,2.86874533920342));
#21704=CARTESIAN_POINT('Ctrl Pts',(82.4430005297901,-3.18308002897164,2.89575244319934));
#21705=CARTESIAN_POINT('Ctrl Pts',(82.4430005297901,-3.16204383972264,2.92249587205561));
#21706=CARTESIAN_POINT('Ctrl Pts',(82.4430005297901,-3.07995910811394,3.02685066531118));
#21707=CARTESIAN_POINT('Ctrl Pts',(82.4430005297901,-2.99328647074254,3.12722044563493));
#21708=CARTESIAN_POINT('Ctrl Pts',(82.4430005297901,-2.90235593084009,3.22337065901414));
#21709=CARTESIAN_POINT('Ctrl Pts',(82.4430005297901,-2.81091979211652,3.32005549403519));
#21710=CARTESIAN_POINT('Ctrl Pts',(82.4430005297901,-2.71517785948218,3.41247434460212));
#21711=CARTESIAN_POINT('Ctrl Pts',(82.4430005297901,-2.6154171072342,3.50036721001472));
#21712=CARTESIAN_POINT('Ctrl Pts',(82.4430005297901,-2.51634883740782,3.58764997312848));
#21713=CARTESIAN_POINT('Ctrl Pts',(82.4430005297901,-2.41331685430689,3.6704699525819));
#21714=CARTESIAN_POINT('Ctrl Pts',(82.4430005297901,-2.30656133318296,3.74854230234771));
#21715=CARTESIAN_POINT('Ctrl Pts',(82.4430005297901,-2.20467684379054,3.82305237365655));
#21716=CARTESIAN_POINT('Ctrl Pts',(82.4430005297901,-2.09940025075541,3.8932384548752));
#21717=CARTESIAN_POINT('Ctrl Pts',(82.4430005297901,-1.99091130097234,3.9588194824242));
#21718=CARTESIAN_POINT('Ctrl Pts',(82.4430005297901,-1.98447919887494,3.96270765597266));
#21719=CARTESIAN_POINT('Ctrl Pts',(82.4430005297901,-1.97803579776512,3.96657963149843));
#21720=CARTESIAN_POINT('Ctrl Pts',(82.4430005297901,-1.97158113240045,3.97043534620103));
#21721=CARTESIAN_POINT('Ctrl Pts',(82.0310032950812,2.5732449024852,-3.61351950356445));
#21722=CARTESIAN_POINT('Ctrl Pts',(82.0636457680076,3.16616325925722,-3.19130979057643));
#21723=CARTESIAN_POINT('Ctrl Pts',(82.1288853844562,4.13207912470726,-2.05174262577274));
#21724=CARTESIAN_POINT('Ctrl Pts',(82.2593192879487,4.79464520668388,0.882555540610264));
#21725=CARTESIAN_POINT('Ctrl Pts',(82.4223050055592,2.75914274104666,4.42905501007769));
#21726=CARTESIAN_POINT('Ctrl Pts',(82.6178878666914,-2.16479008544544,4.75065483431134));
#21727=CARTESIAN_POINT('Ctrl Pts',(82.8134707278238,-5.14967299145611,0.832949191282387));
#21728=CARTESIAN_POINT('Ctrl Pts',(83.0090535889562,-3.55042897662582,-3.82414592282758));
#21729=CARTESIAN_POINT('Ctrl Pts',(83.2046364500884,1.21504830394734,-5.0748705164238));
#21730=CARTESIAN_POINT('Ctrl Pts',(83.400219311221,4.89660859864141,-1.80258629906098));
#21731=CARTESIAN_POINT('Ctrl Pts',(83.5958021723532,4.21527029670854,3.07568249282053));
#21732=CARTESIAN_POINT('Ctrl Pts',(83.7913850334858,-0.222660655853561,
5.21331275103613));
#21733=CARTESIAN_POINT('Ctrl Pts',(83.9869678946179,-4.46203744762071,2.7051724468734));
#21734=CARTESIAN_POINT('Ctrl Pts',(84.1825507557504,-4.72526831706301,-2.21356276749624));
#21735=CARTESIAN_POINT('Ctrl Pts',(84.3781336168827,-0.777683074796472,
-5.15976630774078));
#21736=CARTESIAN_POINT('Ctrl Pts',(84.5737164780151,3.86289539882142,-3.50798698251897));
#21737=CARTESIAN_POINT('Ctrl Pts',(84.7692993391475,5.06117659898468,1.26982667827935));
#21738=CARTESIAN_POINT('Ctrl Pts',(84.96488220028,1.74933589258655,4.91607408021796));
#21739=CARTESIAN_POINT('Ctrl Pts',(85.1604650614123,-3.12137193940479,4.18150613925552));
#21740=CARTESIAN_POINT('Ctrl Pts',(85.3560479225446,-5.21056228074381,-0.279286952965116));
#21741=CARTESIAN_POINT('Ctrl Pts',(85.5516307836769,-2.65651348040282,-4.49120199383985));
#21742=CARTESIAN_POINT('Ctrl Pts',(85.7472136448093,2.26480862632819,-4.70091489012678));
#21743=CARTESIAN_POINT('Ctrl Pts',(85.9427965059417,5.16791352719978,-0.721546383514633));
#21744=CARTESIAN_POINT('Ctrl Pts',(86.1383793670741,3.46578485734584,3.90080690363208));
#21745=CARTESIAN_POINT('Ctrl Pts',(86.3339622282066,-1.32477558834876,5.04707131090363));
#21746=CARTESIAN_POINT('Ctrl Pts',(86.5295450893389,-4.93480143762726,1.69578718575462));
#21747=CARTESIAN_POINT('Ctrl Pts',(86.7251279504711,-4.14732466254241,-3.16664760615603));
#21748=CARTESIAN_POINT('Ctrl Pts',(86.9207108116036,0.335917868796414,-5.20721791424714));
#21749=CARTESIAN_POINT('Ctrl Pts',(87.1162936727359,4.51981737154225,-2.60752975275673));
#21750=CARTESIAN_POINT('Ctrl Pts',(87.3118765338683,4.67601458569188,2.3157815033228));
#21751=CARTESIAN_POINT('Ctrl Pts',(87.5074593950007,0.665320577523391,5.17545253638813));
#21752=CARTESIAN_POINT('Ctrl Pts',(87.7030422561331,-3.93825640509612,3.42317175243948));
#21753=CARTESIAN_POINT('Ctrl Pts',(87.8986251172654,-5.03236803225271,-1.37956714940564));
#21754=CARTESIAN_POINT('Ctrl Pts',(88.0942079783978,-1.64204264387256,-4.95294612034352));
#21755=CARTESIAN_POINT('Ctrl Pts',(88.2897908395301,3.21155918647893,-4.11265223251709));
#21756=CARTESIAN_POINT('Ctrl Pts',(88.4853737006626,5.20323685809616,0.39250777042273));
#21757=CARTESIAN_POINT('Ctrl Pts',(88.6809565617948,2.55828132447017,4.54790108430783));
#21758=CARTESIAN_POINT('Ctrl Pts',(88.8765394229273,-2.36656955065493,4.65055642185629));
#21759=CARTESIAN_POINT('Ctrl Pts',(89.0721222840597,-5.1821983422279,0.609026662521216));
#21760=CARTESIAN_POINT('Ctrl Pts',(89.2677051451921,-3.38052451202556,-3.97526189866621));
#21761=CARTESIAN_POINT('Ctrl Pts',(89.4632880063243,1.43495189680254,-5.01702611225074));
#21762=CARTESIAN_POINT('Ctrl Pts',(89.6588708674568,4.96896142408185,-1.58819351471315));
#21763=CARTESIAN_POINT('Ctrl Pts',(89.8544537285891,4.08065273654629,3.25627251816026));
#21764=CARTESIAN_POINT('Ctrl Pts',(90.0500365897215,-0.455561874102168,
5.19825550801701));
#21765=CARTESIAN_POINT('Ctrl Pts',(90.2130223073318,-3.87588474101625,2.95720212609757));
#21766=CARTESIAN_POINT('Ctrl Pts',(90.3434108814201,-4.6129921626674,0.0418147320781305));
#21767=CARTESIAN_POINT('Ctrl Pts',(90.4086051684642,-4.26823548650425,-1.41053445637093));
#21768=CARTESIAN_POINT('Ctrl Pts',(90.4412023119862,-3.93156634387324,-2.05472598388759));
#21769=CARTESIAN_POINT('Ctrl Pts',(82.1694296294366,2.43416713531397,-3.41821736823327));
#21770=CARTESIAN_POINT('Ctrl Pts',(82.202072102363,2.99503966500787,-3.01882708611391));
#21771=CARTESIAN_POINT('Ctrl Pts',(82.2673117188115,3.9087500751154,-1.94085081639738));
#21772=CARTESIAN_POINT('Ctrl Pts',(82.3977456223042,4.53550603610597,0.834855512574021));
#21773=CARTESIAN_POINT('Ctrl Pts',(82.5607313399144,2.61001763781187,4.18967512016311));
#21774=CARTESIAN_POINT('Ctrl Pts',(82.7563142010469,-2.04778832972938,4.49389323874026));
#21775=CARTESIAN_POINT('Ctrl Pts',(82.9518970621792,-4.8713454134545,0.787930268451231));
#21776=CARTESIAN_POINT('Ctrl Pts',(83.1474799233117,-3.3585367342309,-3.61745993045656));
#21777=CARTESIAN_POINT('Ctrl Pts',(83.3430627844438,1.14937783280214,-4.80058583429903));
#21778=CARTESIAN_POINT('Ctrl Pts',(83.5386456455763,4.63195854922217,-1.70516079658948));
#21779=CARTESIAN_POINT('Ctrl Pts',(83.7342285067087,3.98744496211903,2.90944916881162));
#21780=CARTESIAN_POINT('Ctrl Pts',(83.9298113678411,-0.210626376946379,
4.93154559538018));
#21781=CARTESIAN_POINT('Ctrl Pts',(84.1253942289734,-4.22087493539727,2.55896430968406));
#21782=CARTESIAN_POINT('Ctrl Pts',(84.3209770901058,-4.46987880237384,-2.09392496430875));
#21783=CARTESIAN_POINT('Ctrl Pts',(84.5165599512381,-0.735651154124987,
-4.88089320999837));
#21784=CARTESIAN_POINT('Ctrl Pts',(84.7121428123705,3.6541150894287,-3.31838862896805));
#21785=CARTESIAN_POINT('Ctrl Pts',(84.9077256735029,4.78763204053,1.20119556627793));
#21786=CARTESIAN_POINT('Ctrl Pts',(85.1033085346353,1.65478844794245,4.65037196781321));
#21787=CARTESIAN_POINT('Ctrl Pts',(85.2988913957676,-2.95266920946872,3.95550567707689));
#21788=CARTESIAN_POINT('Ctrl Pts',(85.4944742569001,-4.92894378146587,-0.264192157370293));
#21789=CARTESIAN_POINT('Ctrl Pts',(85.6900571180323,-2.51293524462826,-4.24846320725372));
#21790=CARTESIAN_POINT('Ctrl Pts',(85.8856399791648,2.14240110634607,-4.44684162024508));
#21791=CARTESIAN_POINT('Ctrl Pts',(86.0812228402971,4.88860009162169,-0.682548517500101));
#21792=CARTESIAN_POINT('Ctrl Pts',(86.2768057014295,3.27846742829351,3.6899775675672));
#21793=CARTESIAN_POINT('Ctrl Pts',(86.4723885625619,-1.25317461844009,4.7742891097239));
#21794=CARTESIAN_POINT('Ctrl Pts',(86.6679714236942,-4.6680871560928,1.60413392136281));
#21795=CARTESIAN_POINT('Ctrl Pts',(86.8635542848266,-3.92317162788817,-2.9954978341087));
#21796=CARTESIAN_POINT('Ctrl Pts',(87.0591371459591,0.31776230688313,-4.92578017002461));
#21797=CARTESIAN_POINT('Ctrl Pts',(87.2547200070913,4.27553199184569,-2.46659897096611));
#21798=CARTESIAN_POINT('Ctrl Pts',(87.4503028682238,4.42328711804585,2.19061902056514));
#21799=CARTESIAN_POINT('Ctrl Pts',(87.645885729356,0.62936158260391,4.89573163529303));
#21800=CARTESIAN_POINT('Ctrl Pts',(87.8414685904886,-3.72540301254123,3.23815746036292));
#21801=CARTESIAN_POINT('Ctrl Pts',(88.0370514516208,-4.76038050831605,-1.30500482592964));
#21802=CARTESIAN_POINT('Ctrl Pts',(88.2326343127533,-1.55329414415176,-4.68525116186073));
#21803=CARTESIAN_POINT('Ctrl Pts',(88.4282171738855,3.03798205032592,-3.89037316024618));
#21804=CARTESIAN_POINT('Ctrl Pts',(88.623800035018,4.92201428049067,0.371293658911228));
#21805=CARTESIAN_POINT('Ctrl Pts',(88.8193828961503,2.42001230310359,4.30209784672624));
#21806=CARTESIAN_POINT('Ctrl Pts',(89.0149657572827,-2.23866209472541,4.39920490741982));
#21807=CARTESIAN_POINT('Ctrl Pts',(89.2105486184151,-4.90211284637034,0.576110219826852));
#21808=CARTESIAN_POINT('Ctrl Pts',(89.4061314795474,-3.19781520186777,-3.760408447192));
#21809=CARTESIAN_POINT('Ctrl Pts',(89.6017143406798,1.35739615944824,-4.74586778260333));
#21810=CARTESIAN_POINT('Ctrl Pts',(89.7972972018122,4.70040087652035,-1.50235543235697));
#21811=CARTESIAN_POINT('Ctrl Pts',(89.9928800629445,3.86010316092995,3.08027873276914));
#21812=CARTESIAN_POINT('Ctrl Pts',(90.188462924077,-0.430939838244923,4.91730216053644));
#21813=CARTESIAN_POINT('Ctrl Pts',(90.3514486416872,-3.66640238856974,2.79737238413463));
#21814=CARTESIAN_POINT('Ctrl Pts',(90.4818372157755,-4.36367090710306,0.0395547452550024));
#21815=CARTESIAN_POINT('Ctrl Pts',(90.5470315028196,-4.03754750937051,-1.33429842360129));
#21816=CARTESIAN_POINT('Ctrl Pts',(90.5796286463417,-3.71907453321684,-1.94367293110128));
#21817=CARTESIAN_POINT('Ctrl Pts',(82.307855963792,2.29508936814274,-3.22291523290208));
#21818=CARTESIAN_POINT('Ctrl Pts',(82.3404984367184,2.82391607075853,-2.84634438165137));
#21819=CARTESIAN_POINT('Ctrl Pts',(82.4057380531669,3.68542102552352,-1.82995900702202));
#21820=CARTESIAN_POINT('Ctrl Pts',(82.5361719566594,4.27636686552807,0.787155484537778));
#21821=CARTESIAN_POINT('Ctrl Pts',(82.6991576742698,2.46089253457709,3.95029523024854));
#21822=CARTESIAN_POINT('Ctrl Pts',(82.8947405354022,-1.93078657401334,4.23713164316919));
#21823=CARTESIAN_POINT('Ctrl Pts',(83.0903233965346,-4.59301783545288,0.742911345620072));
#21824=CARTESIAN_POINT('Ctrl Pts',(83.2859062576669,-3.16664449183598,-3.41077393808554));
#21825=CARTESIAN_POINT('Ctrl Pts',(83.4814891187993,1.08370736165695,-4.52630115217425));
#21826=CARTESIAN_POINT('Ctrl Pts',(83.6770719799316,4.36730849980295,-1.60773529411797));
#21827=CARTESIAN_POINT('Ctrl Pts',(83.8726548410641,3.75961962752953,2.7432158448027));
#21828=CARTESIAN_POINT('Ctrl Pts',(84.0682377021964,-0.198592098039204,
4.64977843972425));
#21829=CARTESIAN_POINT('Ctrl Pts',(84.2638205633287,-3.97971242317383,2.41275617249475));
#21830=CARTESIAN_POINT('Ctrl Pts',(84.4594034244612,-4.21448928768466,-1.97428716112127));
#21831=CARTESIAN_POINT('Ctrl Pts',(84.6549862855934,-0.693619233453502,
-4.60202011225595));
#21832=CARTESIAN_POINT('Ctrl Pts',(84.8505691467259,3.44533478003599,-3.12879027541714));
#21833=CARTESIAN_POINT('Ctrl Pts',(85.0461520078582,4.51408748207532,1.13256445427651));
#21834=CARTESIAN_POINT('Ctrl Pts',(85.2417348689906,1.56024100329834,4.38466985540846));
#21835=CARTESIAN_POINT('Ctrl Pts',(85.437317730123,-2.78396647953264,3.72950521489826));
#21836=CARTESIAN_POINT('Ctrl Pts',(85.6329005912553,-4.64732528218793,-0.249097361775471));
#21837=CARTESIAN_POINT('Ctrl Pts',(85.8284834523878,-2.36935700885369,-4.00572442066759));
#21838=CARTESIAN_POINT('Ctrl Pts',(86.02406631352,2.01999358636394,-4.19276835036339));
#21839=CARTESIAN_POINT('Ctrl Pts',(86.2196491746525,4.60928665604361,-0.643550651485564));
#21840=CARTESIAN_POINT('Ctrl Pts',(86.4152320357848,3.09114999924119,3.47914823150234));
#21841=CARTESIAN_POINT('Ctrl Pts',(86.6108148969172,-1.18157364853143,4.50150690854415));
#21842=CARTESIAN_POINT('Ctrl Pts',(86.8063977580496,-4.40137287455832,1.512480656971));
#21843=CARTESIAN_POINT('Ctrl Pts',(87.0019806191819,-3.69901859323395,-2.82434806206138));
#21844=CARTESIAN_POINT('Ctrl Pts',(87.1975634803144,0.299606744969849,-4.6443424258021));
#21845=CARTESIAN_POINT('Ctrl Pts',(87.3931463414466,4.03124661214913,-2.3256681891755));
#21846=CARTESIAN_POINT('Ctrl Pts',(87.5887292025792,4.17055965039982,2.06545653780747));
#21847=CARTESIAN_POINT('Ctrl Pts',(87.7843120637113,0.593402587684435,4.61601073419793));
#21848=CARTESIAN_POINT('Ctrl Pts',(87.9798949248439,-3.51254961998634,3.05314316828636));
#21849=CARTESIAN_POINT('Ctrl Pts',(88.1754777859761,-4.48839298437938,-1.23044250245362));
#21850=CARTESIAN_POINT('Ctrl Pts',(88.3710606471085,-1.46454564443096,-4.41755620337796));
#21851=CARTESIAN_POINT('Ctrl Pts',(88.566643508241,2.8644049141729,-3.66809408797527));
#21852=CARTESIAN_POINT('Ctrl Pts',(88.7622263693732,4.64079170288519,0.350079547399718));
#21853=CARTESIAN_POINT('Ctrl Pts',(88.9578092305058,2.28174328173701,4.05629460914468));
#21854=CARTESIAN_POINT('Ctrl Pts',(89.1533920916379,-2.11075463879587,4.14785339298334));
#21855=CARTESIAN_POINT('Ctrl Pts',(89.3489749527706,-4.62202735051278,0.543193777132494));
#21856=CARTESIAN_POINT('Ctrl Pts',(89.5445578139026,-3.01510589170997,-3.54555499571779));
#21857=CARTESIAN_POINT('Ctrl Pts',(89.7401406750352,1.27984042209396,-4.47470945295592));
#21858=CARTESIAN_POINT('Ctrl Pts',(89.9357235361675,4.43184032895884,-1.41651735000079));
#21859=CARTESIAN_POINT('Ctrl Pts',(90.1313063972999,3.6395535853136,2.90428494737804));
#21860=CARTESIAN_POINT('Ctrl Pts',(90.3268892584322,-0.406317802387683,
4.63634881305585));
#21861=CARTESIAN_POINT('Ctrl Pts',(90.4898749760426,-3.45692003612324,2.63754264217168));
#21862=CARTESIAN_POINT('Ctrl Pts',(90.6202635501308,-4.11434965153871,0.0372947584318718));
#21863=CARTESIAN_POINT('Ctrl Pts',(90.6854578371749,-3.80685953223677,-1.25806239083166));
#21864=CARTESIAN_POINT('Ctrl Pts',(90.718054980697,-3.50658272256043,-1.83261987831497));
#21865=CARTESIAN_POINT('Ctrl Pts',(82.4462822981473,2.15601160097152,-3.0276130975709));
#21866=CARTESIAN_POINT('Ctrl Pts',(82.4789247710738,2.65279247650918,-2.67386167718884));
#21867=CARTESIAN_POINT('Ctrl Pts',(82.5441643875223,3.46209197593166,-1.71906719764665));
#21868=CARTESIAN_POINT('Ctrl Pts',(82.6745982910148,4.01722769495016,0.739455456501537));
#21869=CARTESIAN_POINT('Ctrl Pts',(82.8375840086252,2.3117674313423,3.71091534033396));
#21870=CARTESIAN_POINT('Ctrl Pts',(83.0331668697575,-1.81378481829728,3.98037004759811));
#21871=CARTESIAN_POINT('Ctrl Pts',(83.2287497308899,-4.31469025745127,0.697892422788916));
#21872=CARTESIAN_POINT('Ctrl Pts',(83.4243325920222,-2.97475224944107,-3.20408794571452));
#21873=CARTESIAN_POINT('Ctrl Pts',(83.6199154531546,1.01803689051175,-4.25201647004949));
#21874=CARTESIAN_POINT('Ctrl Pts',(83.815498314287,4.10265845038372,-1.51030979164646));
#21875=CARTESIAN_POINT('Ctrl Pts',(84.0110811754194,3.53179429294001,2.57698252079379));
#21876=CARTESIAN_POINT('Ctrl Pts',(84.2066640365517,-0.186557819132022,
4.3680112840683));
#21877=CARTESIAN_POINT('Ctrl Pts',(84.4022468976841,-3.73854991095039,2.26654803530542));
#21878=CARTESIAN_POINT('Ctrl Pts',(84.5978297588165,-3.95909977299548,-1.85464935793378));
#21879=CARTESIAN_POINT('Ctrl Pts',(84.7934126199488,-0.651587312782014,
-4.32314701451353));
#21880=CARTESIAN_POINT('Ctrl Pts',(84.9889954810813,3.23655447064327,-2.93919192186622));
#21881=CARTESIAN_POINT('Ctrl Pts',(85.1845783422135,4.24054292362064,1.06393334227509));
#21882=CARTESIAN_POINT('Ctrl Pts',(85.380161203346,1.46569355865423,4.11896774300371));
#21883=CARTESIAN_POINT('Ctrl Pts',(85.5757440644783,-2.61526374959657,3.50350475271963));
#21884=CARTESIAN_POINT('Ctrl Pts',(85.7713269256107,-4.36570678291,-0.234002566180649));
#21885=CARTESIAN_POINT('Ctrl Pts',(85.966909786743,-2.22577877307914,-3.76298563408145));
#21886=CARTESIAN_POINT('Ctrl Pts',(86.1624926478755,1.89758606638183,-3.93869508048168));
#21887=CARTESIAN_POINT('Ctrl Pts',(86.3580755090077,4.32997322046552,-0.604552785471028));
#21888=CARTESIAN_POINT('Ctrl Pts',(86.5536583701403,2.90383257018886,3.26831889543747));
#21889=CARTESIAN_POINT('Ctrl Pts',(86.7492412312724,-1.10997267862275,4.22872470736441));
#21890=CARTESIAN_POINT('Ctrl Pts',(86.944824092405,-4.13465859302386,1.42082739257919));
#21891=CARTESIAN_POINT('Ctrl Pts',(87.1404069535373,-3.47486555857972,-2.65319829001405));
#21892=CARTESIAN_POINT('Ctrl Pts',(87.3359898146697,0.281451183056565,-4.36290468157959));
#21893=CARTESIAN_POINT('Ctrl Pts',(87.5315726758021,3.78696123245258,-2.18473740738487));
#21894=CARTESIAN_POINT('Ctrl Pts',(87.7271555369346,3.91783218275379,1.9402940550498));
#21895=CARTESIAN_POINT('Ctrl Pts',(87.9227383980667,0.557443592764954,4.33628983310282));
#21896=CARTESIAN_POINT('Ctrl Pts',(88.1183212591992,-3.29969622743145,2.8681288762098));
#21897=CARTESIAN_POINT('Ctrl Pts',(88.3139041203315,-4.21640546044272,-1.15588017897761));
#21898=CARTESIAN_POINT('Ctrl Pts',(88.5094869814639,-1.37579714471017,-4.14986124489519));
#21899=CARTESIAN_POINT('Ctrl Pts',(88.7050698425962,2.69082777801989,-3.44581501570436));
#21900=CARTESIAN_POINT('Ctrl Pts',(88.9006527037287,4.3595691252797,0.328865435888209));
#21901=CARTESIAN_POINT('Ctrl Pts',(89.096235564861,2.14347426037042,3.8104913715631));
#21902=CARTESIAN_POINT('Ctrl Pts',(89.2918184259934,-1.98284718286635,3.89650187854686));
#21903=CARTESIAN_POINT('Ctrl Pts',(89.4874012871258,-4.34194185465522,0.510277334438133));
#21904=CARTESIAN_POINT('Ctrl Pts',(89.6829841482581,-2.83239658155217,-3.33070154424358));
#21905=CARTESIAN_POINT('Ctrl Pts',(89.8785670093905,1.20228468473967,-4.20355112330852));
#21906=CARTESIAN_POINT('Ctrl Pts',(90.0741498705228,4.16327978139733,-1.3306792676446));
#21907=CARTESIAN_POINT('Ctrl Pts',(90.2697327316552,3.41900400969726,2.72829116198692));
#21908=CARTESIAN_POINT('Ctrl Pts',(90.4653155927876,-0.381695766530438,
4.35539546557527));
#21909=CARTESIAN_POINT('Ctrl Pts',(90.6283013103979,-3.24743768367674,2.47771290020874));
#21910=CARTESIAN_POINT('Ctrl Pts',(90.7586898844862,-3.86502839597435,0.035034771608743));
#21911=CARTESIAN_POINT('Ctrl Pts',(90.8238841715303,-3.57617155510303,-1.18182635806204));
#21912=CARTESIAN_POINT('Ctrl Pts',(90.8564813150523,-3.29409091190402,-1.72156682552866));
#21913=CARTESIAN_POINT('Ctrl Pts',(90.4430005297901,0.0295740726440573,
3.72695441077288));
#21914=CARTESIAN_POINT('Ctrl Pts',(90.4430005297901,-0.0884458352819757,
3.73973311544785));
#21915=CARTESIAN_POINT('Ctrl Pts',(90.4430005297901,-0.206685143677292,
3.74654596528331));
#21916=CARTESIAN_POINT('Ctrl Pts',(90.4430005297901,-0.324736322595996,
3.74724091818273));
#21917=CARTESIAN_POINT('Ctrl Pts',(90.4430005297901,-0.439404897079654,
3.7479159581022));
#21918=CARTESIAN_POINT('Ctrl Pts',(90.4430005297901,-0.553896885543204,
3.74281974148777));
#21919=CARTESIAN_POINT('Ctrl Pts',(90.4430005297901,-0.66791598104826,3.73223833786101));
#21920=CARTESIAN_POINT('Ctrl Pts',(90.4430005297901,-0.783952175660468,
3.72146973980235));
#21921=CARTESIAN_POINT('Ctrl Pts',(90.4430005297901,-0.899499226843573,
3.7050200613725));
#21922=CARTESIAN_POINT('Ctrl Pts',(90.4430005297901,-1.01425304689082,3.68313712188346));
#21923=CARTESIAN_POINT('Ctrl Pts',(90.4430005297901,-1.13104622386595,3.66086528793991));
#21924=CARTESIAN_POINT('Ctrl Pts',(90.4430005297901,-1.24701846212934,3.63296523737056));
#21925=CARTESIAN_POINT('Ctrl Pts',(90.4430005297901,-1.36184717318808,3.59964481501033));
#21926=CARTESIAN_POINT('Ctrl Pts',(90.4430005297901,-1.37934384898826,3.59456771693801));
#21927=CARTESIAN_POINT('Ctrl Pts',(90.4430005297901,-1.39681395895273,3.58936467583838));
#21928=CARTESIAN_POINT('Ctrl Pts',(90.4430005297901,-1.41425634058431,3.584036323652));
#21929=CARTESIAN_POINT('Ctrl Pts',(90.4430005297901,-1.43024624853253,3.57915167757697));
#21930=CARTESIAN_POINT('Ctrl Pts',(90.4430005297901,-1.44620373585888,3.57416449842206));
#21931=CARTESIAN_POINT('Ctrl Pts',(90.4430005297901,-1.46212623027145,3.56907619712215));
#21932=CARTESIAN_POINT('Ctrl Pts',(90.4430005297901,-1.57729676935156,3.53227151134062));
#21933=CARTESIAN_POINT('Ctrl Pts',(90.4430005297901,-1.6906653553074,3.4901716855535));
#21934=CARTESIAN_POINT('Ctrl Pts',(90.4430005297901,-1.8019109939639,3.44308149795093));
#21935=CARTESIAN_POINT('Ctrl Pts',(90.4430005297901,-1.91505125573011,3.39518931793994));
#21936=CARTESIAN_POINT('Ctrl Pts',(90.4430005297901,-2.02599639340762,3.34213517090997));
#21937=CARTESIAN_POINT('Ctrl Pts',(90.4430005297901,-2.13440929064491,3.28418473248124));
#21938=CARTESIAN_POINT('Ctrl Pts',(90.4430005297901,-2.24357700600436,3.22583081769288));
#21939=CARTESIAN_POINT('Ctrl Pts',(90.4430005297901,-2.35017791442109,3.16251190946834));
#21940=CARTESIAN_POINT('Ctrl Pts',(90.4430005297901,-2.45385647085219,3.09444766228528));
#21941=CARTESIAN_POINT('Ctrl Pts',(90.4430005297901,-2.51004735209134,3.05755874174328));
#21942=CARTESIAN_POINT('Ctrl Pts',(90.4430005297901,-2.56537957209502,3.01927509056427));
#21943=CARTESIAN_POINT('Ctrl Pts',(90.4430005297901,-2.61979383101806,2.97962587081534));
#21944=CARTESIAN_POINT('Ctrl Pts',(90.4430005297901,-2.6583589385645,2.95152521385496));
#21945=CARTESIAN_POINT('Ctrl Pts',(90.4430005297901,-2.69646291239529,2.92273854683793));
#21946=CARTESIAN_POINT('Ctrl Pts',(90.4430005297901,-2.73408385528245,2.89327509668863));
#21947=CARTESIAN_POINT('Ctrl Pts',(90.4430005297901,-2.75355183901951,2.87802843022242));
#21948=CARTESIAN_POINT('Ctrl Pts',(90.4430005297901,-2.77289124006853,2.86259967027211));
#21949=CARTESIAN_POINT('Ctrl Pts',(90.4430005297901,-2.79207491946629,2.84701017273444));
#21950=CARTESIAN_POINT('Ctrl Pts',(90.4430005297901,-2.89080728506944,2.76677593098424));
#21951=CARTESIAN_POINT('Ctrl Pts',(90.4430005297901,-2.98557254574996,2.68216713774138));
#21952=CARTESIAN_POINT('Ctrl Pts',(90.4430005297901,-3.0760218382525,2.59346212800552));
#21953=CARTESIAN_POINT('Ctrl Pts',(90.4430005297901,-3.16657121142245,2.5046589676227));
#21954=CARTESIAN_POINT('Ctrl Pts',(90.4430005297901,-3.25279589353019,2.41175014113957));
#21955=CARTESIAN_POINT('Ctrl Pts',(90.4430005297901,-3.33432693640993,2.31496642130862));
#21956=CARTESIAN_POINT('Ctrl Pts',(90.4430005297901,-3.41466240181752,2.21960194537565));
#21957=CARTESIAN_POINT('Ctrl Pts',(90.4430005297901,-3.49044160687377,2.1204749177954));
#21958=CARTESIAN_POINT('Ctrl Pts',(90.4430005297901,-3.56128171283007,2.01776553973377));
#21959=CARTESIAN_POINT('Ctrl Pts',(90.4430005297901,-3.57213897168619,2.0020238593747));
#21960=CARTESIAN_POINT('Ctrl Pts',(90.4430005297901,-3.58288014117297,1.98619795895379));
#21961=CARTESIAN_POINT('Ctrl Pts',(90.4430005297901,-3.5935037628077,1.97028841204376));
#21962=CARTESIAN_POINT('Ctrl Pts',(90.4430005297901,-3.65258853086704,1.88180522604296));
#21963=CARTESIAN_POINT('Ctrl Pts',(90.4430005297901,-3.70803921479688,1.79073595284717));
#21964=CARTESIAN_POINT('Ctrl Pts',(90.4430005297901,-3.75982007731666,1.69733475008557));
#21965=CARTESIAN_POINT('Ctrl Pts',(90.4430005297901,-3.76811332474678,1.68237556927863));
#21966=CARTESIAN_POINT('Ctrl Pts',(90.4430005297901,-3.77631159693478,1.66735785530935));
#21967=CARTESIAN_POINT('Ctrl Pts',(90.4430005297901,-3.78440902583728,1.65229362110775));
#21968=CARTESIAN_POINT('Ctrl Pts',(90.4430005297901,-3.84295084533117,1.54338402893199));
#21969=CARTESIAN_POINT('Ctrl Pts',(90.4430005297901,-3.89630994738891,1.43189315586789));
#21970=CARTESIAN_POINT('Ctrl Pts',(90.4430005297901,-3.94451322877546,1.318276879715));
#21971=CARTESIAN_POINT('Ctrl Pts',(90.4430005297901,-3.99420842084563,1.20114413473779));
#21972=CARTESIAN_POINT('Ctrl Pts',(90.4430005297901,-4.03842411533983,1.08175183814539));
#21973=CARTESIAN_POINT('Ctrl Pts',(90.4430005297901,-4.07715067449774,0.960560639470474));
#21974=CARTESIAN_POINT('Ctrl Pts',(90.4430005297901,-4.11629615156748,0.83805847578899));
#21975=CARTESIAN_POINT('Ctrl Pts',(90.4430005297901,-4.14983341986074,0.713717519612734));
#21976=CARTESIAN_POINT('Ctrl Pts',(90.4430005297901,-4.17770772803754,0.587984615666701));
#21977=CARTESIAN_POINT('Ctrl Pts',(90.4430005297901,-4.20559840491458,0.462177877270582));
#21978=CARTESIAN_POINT('Ctrl Pts',(90.4430005297901,-4.22781973772143,0.334976713975839));
#21979=CARTESIAN_POINT('Ctrl Pts',(90.4430005297901,-4.24426791493627,0.206812112669376));
#21980=CARTESIAN_POINT('Ctrl Pts',(90.4430005297901,-4.24661469917405,0.18852591218294));
#21981=CARTESIAN_POINT('Ctrl Pts',(90.4430005297901,-4.24884387475331,0.170220083948819));
#21982=CARTESIAN_POINT('Ctrl Pts',(90.4430005297901,-4.250955053885,0.151895867868593));
#21983=CARTESIAN_POINT('Ctrl Pts',(90.4430005297901,-4.25302188555422,0.133956570563174));
#21984=CARTESIAN_POINT('Ctrl Pts',(90.4430005297901,-4.25497512784509,0.116003677579542));
#21985=CARTESIAN_POINT('Ctrl Pts',(90.4430005297901,-4.25681383615619,0.0980463316274623));
#21986=CARTESIAN_POINT('Ctrl Pts',(90.4430005297901,-4.25874402274224,0.0791955829424459));
#21987=CARTESIAN_POINT('Ctrl Pts',(90.4430005297901,-4.26054829999988,0.060337316736268));
#21988=CARTESIAN_POINT('Ctrl Pts',(90.4430005297901,-4.26222661848669,0.0414729768254014));
#21989=CARTESIAN_POINT('Ctrl Pts',(90.4430005297901,-4.27381294533361,-0.0887576138975155));
#21990=CARTESIAN_POINT('Ctrl Pts',(90.4430005297901,-4.27940028200127,-0.219276168333582));
#21991=CARTESIAN_POINT('Ctrl Pts',(90.4430005297901,-4.27910474674529,-0.349707946362895));
#21992=CARTESIAN_POINT('Ctrl Pts',(90.4430005297901,-4.27880600451492,-0.481555093161264));
#21993=CARTESIAN_POINT('Ctrl Pts',(90.4430005297901,-4.27249612571316,-0.613314293186454));
#21994=CARTESIAN_POINT('Ctrl Pts',(90.4430005297901,-4.26024353120833,-0.744611026749141));
#21995=CARTESIAN_POINT('Ctrl Pts',(90.4430005297901,-4.25441728433827,-0.807044104304067));
#21996=CARTESIAN_POINT('Ctrl Pts',(90.4430005297901,-4.24724656795236,-0.869372726950488));
#21997=CARTESIAN_POINT('Ctrl Pts',(90.4430005297901,-4.23873461501024,-0.931556866122163));
#21998=CARTESIAN_POINT('Ctrl Pts',(90.4430005297901,-4.23512308808359,-0.95794090449223));
#21999=CARTESIAN_POINT('Ctrl Pts',(90.4430005297901,-4.23126959330347,-0.984301416906839));
#22000=CARTESIAN_POINT('Ctrl Pts',(90.4430005297901,-4.22717812966963,-1.01061216318249));
#22001=CARTESIAN_POINT('Ctrl Pts',(90.4430005297901,-4.2065986047243,-1.14295176283902));
#22002=CARTESIAN_POINT('Ctrl Pts',(90.4430005297901,-4.17998717842944,-1.27415495162273));
#22003=CARTESIAN_POINT('Ctrl Pts',(90.4430005297901,-4.14743840993115,-1.40383584322983));
#22004=CARTESIAN_POINT('Ctrl Pts',(90.4430005297901,-4.11495992046892,-1.5332367289111));
#22005=CARTESIAN_POINT('Ctrl Pts',(90.4430005297901,-4.0765696800258,-1.66112266042091));
#22006=CARTESIAN_POINT('Ctrl Pts',(90.4430005297901,-4.03231018303459,-1.78711174601695));
#22007=CARTESIAN_POINT('Ctrl Pts',(90.4430005297901,-4.00078732768196,-1.87684470710418));
#22008=CARTESIAN_POINT('Ctrl Pts',(90.4430005297901,-3.96628611270671,-1.96561551665267));
#22009=CARTESIAN_POINT('Ctrl Pts',(90.4430005297901,-3.92880598357854,-2.05328335682083));
#22010=CARTESIAN_POINT('Ctrl Pts',(82.4430005297902,1.9774016913413,3.97328893098977));
#22011=CARTESIAN_POINT('Ctrl Pts',(82.4430005297901,2.09010205945685,3.90686165204003));
#22012=CARTESIAN_POINT('Ctrl Pts',(82.4430005297901,2.1994288641269,3.83533535974094));
#22013=CARTESIAN_POINT('Ctrl Pts',(82.4430005297901,2.30496647500185,3.75870816478726));
#22014=CARTESIAN_POINT('Ctrl Pts',(82.4430005297901,2.31220701604365,3.75345105933091));
#22015=CARTESIAN_POINT('Ctrl Pts',(82.4430005297901,2.31942970874689,3.74816992928515));
#22016=CARTESIAN_POINT('Ctrl Pts',(82.4430005297901,2.32663441280679,3.74286476721894));
#22017=CARTESIAN_POINT('Ctrl Pts',(82.4430005297901,2.43415121558717,3.66369509434307));
#22018=CARTESIAN_POINT('Ctrl Pts',(82.4430005297901,2.53766541991209,3.57917623912721));
#22019=CARTESIAN_POINT('Ctrl Pts',(82.4430005297901,2.63699553330001,3.48971947438876));
#22020=CARTESIAN_POINT('Ctrl Pts',(82.4430005297901,2.69497714530243,3.43750119689823));
#22021=CARTESIAN_POINT('Ctrl Pts',(82.4430005297901,2.75153231248618,3.38359974223897));
#22022=CARTESIAN_POINT('Ctrl Pts',(82.4430005297901,2.80661797434521,3.32809262431144));
#22023=CARTESIAN_POINT('Ctrl Pts',(82.4430005297901,2.82333285684607,3.31124985755857));
#22024=CARTESIAN_POINT('Ctrl Pts',(82.4430005297901,2.83991240093079,3.29425923599673));
#22025=CARTESIAN_POINT('Ctrl Pts',(82.4430005297901,2.85635530402485,3.2771228831448));
#22026=CARTESIAN_POINT('Ctrl Pts',(82.4430005297901,2.87182248494779,3.26100340178533));
#22027=CARTESIAN_POINT('Ctrl Pts',(82.4430005297901,2.88716274481627,3.24476121188179));
#22028=CARTESIAN_POINT('Ctrl Pts',(82.4430005297901,2.9023727429123,3.22840114134904));
#22029=CARTESIAN_POINT('Ctrl Pts',(82.4430005297901,2.99230521077527,3.1316686165891));
#22030=CARTESIAN_POINT('Ctrl Pts',(82.4430005297901,3.07771715590702,3.03078619893305));
#22031=CARTESIAN_POINT('Ctrl Pts',(82.4430005297901,3.15844240805742,2.92616122323708));
#22032=CARTESIAN_POINT('Ctrl Pts',(82.4430005297901,3.2395838873707,2.82099679110536));
#22033=CARTESIAN_POINT('Ctrl Pts',(82.4430005297901,3.31599056868566,2.71205028408578));
#22034=CARTESIAN_POINT('Ctrl Pts',(82.4430005297901,3.3874469961184,2.59971212324649));
#22035=CARTESIAN_POINT('Ctrl Pts',(82.4430005297901,3.41263912962364,2.56010703736026));
#22036=CARTESIAN_POINT('Ctrl Pts',(82.4430005297901,3.43721553345861,2.52008024072263));
#22037=CARTESIAN_POINT('Ctrl Pts',(82.4430005297901,3.46116526677622,2.47964845206219));
#22038=CARTESIAN_POINT('Ctrl Pts',(82.4430005297901,3.47596320889565,2.45466665955337));
#22039=CARTESIAN_POINT('Ctrl Pts',(82.4430005297901,3.4905218915381,2.42953025043779));
#22040=CARTESIAN_POINT('Ctrl Pts',(82.4430005297901,3.50483857765273,2.4042431483245));
#22041=CARTESIAN_POINT('Ctrl Pts',(82.4430005297901,3.51750213823568,2.3818759086564));
#22042=CARTESIAN_POINT('Ctrl Pts',(82.4430005297901,3.52997604592584,2.35939102284286));
#22043=CARTESIAN_POINT('Ctrl Pts',(82.4430005297901,3.54224655904972,2.33681381979864));
#22044=CARTESIAN_POINT('Ctrl Pts',(82.4430005297901,3.60511418791248,2.22114015502084));
#22045=CARTESIAN_POINT('Ctrl Pts',(82.4430005297901,3.66273152318934,2.10289696968469));
#22046=CARTESIAN_POINT('Ctrl Pts',(82.4430005297901,3.71493478777603,1.98247901087182));
#22047=CARTESIAN_POINT('Ctrl Pts',(82.4430005297901,3.7664679243965,1.86360684507541));
#22048=CARTESIAN_POINT('Ctrl Pts',(82.4430005297901,3.81272526802198,1.74261452974662));
#22049=CARTESIAN_POINT('Ctrl Pts',(82.4430005297901,3.85350025988324,1.61986682033174));
#22050=CARTESIAN_POINT('Ctrl Pts',(82.4430005297901,3.89507059812238,1.49472482604712));
#22051=CARTESIAN_POINT('Ctrl Pts',(82.4430005297901,3.9309430977877,1.36775746124));
#22052=CARTESIAN_POINT('Ctrl Pts',(82.4430005297901,3.96084235932242,1.2393481640155));
#22053=CARTESIAN_POINT('Ctrl Pts',(82.4430005297901,3.98903875393377,1.11825222282973));
#22054=CARTESIAN_POINT('Ctrl Pts',(82.4430005297901,4.01192267483145,0.99587330142771));
#22055=CARTESIAN_POINT('Ctrl Pts',(82.4430005297901,4.02921301288842,0.872540673797174));
#22056=CARTESIAN_POINT('Ctrl Pts',(82.4430005297901,4.03025722954013,0.865092237390287));
#22057=CARTESIAN_POINT('Ctrl Pts',(82.4430005297901,4.0312810292029,0.85764032654507));
#22058=CARTESIAN_POINT('Ctrl Pts',(82.4430005297901,4.03228434397425,0.850185015481214));
#22059=CARTESIAN_POINT('Ctrl Pts',(82.4430005297901,4.03459129039469,0.83304283471883));
#22060=CARTESIAN_POINT('Ctrl Pts',(82.4430005297901,4.03678865170643,0.81589217044497));
#22061=CARTESIAN_POINT('Ctrl Pts',(82.4430005297901,4.03887577431093,0.798735610694986));
#22062=CARTESIAN_POINT('Ctrl Pts',(82.4430005297901,4.05392301973049,0.675044283430583));
#22063=CARTESIAN_POINT('Ctrl Pts',(82.4430005297901,4.06324834973385,0.551017529409657));
#22064=CARTESIAN_POINT('Ctrl Pts',(82.4430005297901,4.06666460622878,0.426983323700702));
#22065=CARTESIAN_POINT('Ctrl Pts',(82.4430005297901,4.06939901272037,0.327705082218145));
#22066=CARTESIAN_POINT('Ctrl Pts',(82.4430005297901,4.06834683332187,0.228421806362535));
#22067=CARTESIAN_POINT('Ctrl Pts',(82.4430005297901,4.06338801735055,0.129303333680082));
#22068=CARTESIAN_POINT('Ctrl Pts',(82.4430005297901,4.05712578276322,0.00413169362238594));
#22069=CARTESIAN_POINT('Ctrl Pts',(82.4430005297901,4.04463442778872,-0.120778201880177));
#22070=CARTESIAN_POINT('Ctrl Pts',(82.4430005297901,4.02608868523045,-0.244998516667174));
#22071=CARTESIAN_POINT('Ctrl Pts',(82.4430005297901,4.00761010244444,-0.368768991927616));
#22072=CARTESIAN_POINT('Ctrl Pts',(82.4430005297901,3.98312043438457,-0.491855671889886));
#22073=CARTESIAN_POINT('Ctrl Pts',(82.4430005297901,3.95274824392976,-0.613809207916153));
#22074=CARTESIAN_POINT('Ctrl Pts',(82.4430005297901,3.94615948295374,-0.640265077151297));
#22075=CARTESIAN_POINT('Ctrl Pts',(82.4430005297901,3.93929375074547,-0.666667446927112));
#22076=CARTESIAN_POINT('Ctrl Pts',(82.4430005297901,3.93215207449842,-0.693011663701303));
#22077=CARTESIAN_POINT('Ctrl Pts',(82.4430005297901,3.92670631144765,-0.713099995536515));
#22078=CARTESIAN_POINT('Ctrl Pts',(82.4430005297901,3.92110068729186,-0.733151964085459));
#22079=CARTESIAN_POINT('Ctrl Pts',(82.4430005297901,3.9153411470454,-0.753147780879801));
#22080=CARTESIAN_POINT('Ctrl Pts',(82.4430005297901,3.88128865297465,-0.871370313181259));
#22081=CARTESIAN_POINT('Ctrl Pts',(82.4430005297901,3.84181409822679,-0.987802709833606));
#22082=CARTESIAN_POINT('Ctrl Pts',(82.4430005297901,3.79712203089279,-1.10205584095973));
#22083=CARTESIAN_POINT('Ctrl Pts',(82.4430005297901,3.75260677405727,-1.21585696450885));
#22084=CARTESIAN_POINT('Ctrl Pts',(82.4430005297901,3.70291471512788,-1.32749679081321));
#22085=CARTESIAN_POINT('Ctrl Pts',(82.4430005297901,3.6482030112339,-1.43656648416229));
#22086=CARTESIAN_POINT('Ctrl Pts',(82.4430005297901,3.59845450992584,-1.5357418597412));
#22087=CARTESIAN_POINT('Ctrl Pts',(82.4430005297901,3.54455500137787,-1.63279237552513));
#22088=CARTESIAN_POINT('Ctrl Pts',(82.4430005297901,3.48659512784045,-1.72738526130349));
#22089=CARTESIAN_POINT('Ctrl Pts',(82.4430005297901,3.42673021387979,-1.82508725102155));
#22090=CARTESIAN_POINT('Ctrl Pts',(82.4430005297901,3.36253323060098,-1.92016776201095));
#22091=CARTESIAN_POINT('Ctrl Pts',(82.4430005297901,3.29416366019009,-2.01234893030668));
#22092=CARTESIAN_POINT('Ctrl Pts',(82.4430005297901,3.28199925485566,-2.02874992695784));
#22093=CARTESIAN_POINT('Ctrl Pts',(82.4430005297901,3.26970271301344,-2.04505905011743));
#22094=CARTESIAN_POINT('Ctrl Pts',(82.4430005297901,3.25727487268005,-2.06127461217243));
#22095=CARTESIAN_POINT('Ctrl Pts',(82.4430005297901,3.24649498934229,-2.07533995760012));
#22096=CARTESIAN_POINT('Ctrl Pts',(82.4430005297901,3.23562112293146,-2.08932859706152));
#22097=CARTESIAN_POINT('Ctrl Pts',(82.4430005297901,3.22465780066578,-2.10323500148988));
#22098=CARTESIAN_POINT('Ctrl Pts',(82.4430005297901,3.15047393396632,-2.19733338037383));
#22099=CARTESIAN_POINT('Ctrl Pts',(82.4430005297901,3.07214423094065,-2.28773884705976));
#22100=CARTESIAN_POINT('Ctrl Pts',(82.4430005297901,2.98991394061097,-2.37420105586575));
#22101=CARTESIAN_POINT('Ctrl Pts',(82.4430005297901,2.90806315296147,-2.46026423117879));
#22102=CARTESIAN_POINT('Ctrl Pts',(82.4430005297901,2.82234707694838,-2.54242092981904));
#22103=CARTESIAN_POINT('Ctrl Pts',(82.4430005297901,2.73297569134897,-2.62038408617641));
#22104=CARTESIAN_POINT('Ctrl Pts',(82.4430005297901,2.64463815606218,-2.69744536288816));
#22105=CARTESIAN_POINT('Ctrl Pts',(82.4430005297901,2.55272879793543,-2.77040993934337));
#22106=CARTESIAN_POINT('Ctrl Pts',(82.4430005297901,2.45742821326915,-2.83895504479805));
#22107=CARTESIAN_POINT('Ctrl Pts',(82.4430005297901,2.36212762860286,-2.90750015025273));
#22108=CARTESIAN_POINT('Ctrl Pts',(82.4430005297901,2.26343528680515,-2.97162624539521));
#22109=CARTESIAN_POINT('Ctrl Pts',(82.4430005297901,2.16151778945159,-3.03095833168066));
#22110=CARTESIAN_POINT('Origin',(81.4430005297901,0.,0.));
#22111=CARTESIAN_POINT('',(82.4430005297901,-5.42440960677665,-6.64298586220318E-16));
#22112=CARTESIAN_POINT('Origin',(82.4430005297901,0.,0.));
#22113=CARTESIAN_POINT('',(81.4430005297901,-5.42440960677665,-6.64298586220318E-16));
#22114=CARTESIAN_POINT('',(81.4430005297901,-5.42440960677665,-6.64298586220318E-16));
#22115=CARTESIAN_POINT('Origin',(81.4430005297901,0.,0.));
#22116=CARTESIAN_POINT('Origin',(82.4430005297901,0.,0.));
#22117=CARTESIAN_POINT('Origin',(90.4430005297901,0.,0.));
#22118=CARTESIAN_POINT('Origin',(81.4430005297901,0.,0.));
#28036=UNCERTAINTY_MEASURE_WITH_UNIT(LENGTH_MEASURE(0.01),#28056,
'DISTANCE_ACCURACY_VALUE',
'Maximum model space distance between geometric entities at asserted c
onnectivities');
#28043=UNCERTAINTY_MEASURE_WITH_UNIT(LENGTH_MEASURE(0.01),#28056,
'DISTANCE_ACCURACY_VALUE',
'Maximum model space distance between geometric entities at asserted c
onnectivities');
#28048=(
GEOMETRIC_REPRESENTATION_CONTEXT(3)
GLOBAL_UNCERTAINTY_ASSIGNED_CONTEXT((#28036))
GLOBAL_UNIT_ASSIGNED_CONTEXT((#28056,#28058,#28059))
REPRESENTATION_CONTEXT('','3D')
);
#28055=(
GEOMETRIC_REPRESENTATION_CONTEXT(3)
GLOBAL_UNCERTAINTY_ASSIGNED_CONTEXT((#28043))
GLOBAL_UNIT_ASSIGNED_CONTEXT((#28056,#28058,#28059))
REPRESENTATION_CONTEXT('','3D')
);
#28056=(
LENGTH_UNIT()
NAMED_UNIT(*)
SI_UNIT(.MILLI.,.METRE.)
);
#28058=(
NAMED_UNIT(*)
PLANE_ANGLE_UNIT()
SI_UNIT($,.RADIAN.)
);
#28059=(
NAMED_UNIT(*)
SI_UNIT($,.STERADIAN.)
SOLID_ANGLE_UNIT()
);
#28064=SHAPE_DEFINITION_REPRESENTATION(#28075,#28096);
#28075=PRODUCT_DEFINITION_SHAPE('',$,#28108);
#28096=SHAPE_REPRESENTATION('',(#3962),#28048);
#28103=PRODUCT_DEFINITION_CONTEXT('part definition',#28138,'design');
#28108=PRODUCT_DEFINITION('Screw','Screw',#28119,#28103);
#28119=PRODUCT_DEFINITION_FORMATION('',$,#28144);
#28138=APPLICATION_CONTEXT(
'Core Data for Automotive Mechanical Design Process');
#28139=PRODUCT_CONTEXT('part definition',#28138,'mechanical');
#28144=PRODUCT('Screw','Screw',$,(#28139));
#28152=PRESENTATION_STYLE_ASSIGNMENT((#28155));
#28155=SURFACE_STYLE_USAGE(.BOTH.,#28158);
#28158=SURFACE_SIDE_STYLE('',(#28161));
#28161=SURFACE_STYLE_FILL_AREA(#28164);
#28164=FILL_AREA_STYLE('Opaque(160,160,160)',(#28167));
#28167=FILL_AREA_STYLE_COLOUR('Opaque(160,160,160)',#28170);
#28170=COLOUR_RGB('Opaque(160,160,160)', 0.66274510, 0.83137255, 0.94901961);
ENDSEC;
END-ISO-10303-21;
